ISO-10303-21;
HEADER;
FILE_DESCRIPTION (('STEP AP203'),
    '1' );
FILE_NAME ('Part3_SlicingGear.step',
    '2026-10-06T15:07:10',
    ( '' ),
    ( '' ),
    'SwSTEP 2.0',
    'SolidWorks 2024',
    '' );
FILE_SCHEMA (( 'AUTOMOTIVE_DESIGN' ));
ENDSEC;

DATA;
#5=DIRECTION ( 'NONE',  ( 1.000000000000000000, -0.000000000000000000, 0.000000000000000000 ) ) ;
#7=AXIS2_PLACEMENT_3D ( 'NONE', #248, #30174, #22638 ) ;
#28=DIRECTION ( 'NONE',  ( -1.000000000000000000, -0.000000000000000000, 0.000000000000000000 ) ) ;
#37=B_SPLINE_CURVE_WITH_KNOTS ( 'NONE', 3,
 ( #24439, #32167, #19463, #16927, #1731, #20453, #20272, #30474 ),
 .UNSPECIFIED., .F., .F.,
 ( 4, 2, 2, 4 ),
 ( 2.304311362529957687E-07, 0.001227991214883143506, 0.001841871606756588465, 0.002455751998630033642 ),
 .UNSPECIFIED. ) ;
#40=AXIS2_PLACEMENT_3D ( 'NONE', #21836, #32050, #26400 ) ;
#45=VECTOR ( 'NONE', #11499, 1000.000000000000000 ) ;
#48=LINE ( 'NONE', #23124, #20445 ) ;
#52=AXIS2_PLACEMENT_3D ( 'NONE', #22887, #28230, #10168 ) ;
#64=ORIENTED_EDGE ( 'NONE', *, *, #2032, .F. ) ;
#70=VECTOR ( 'NONE', #32626, 1000.000000000000000 ) ;
#94=ORIENTED_EDGE ( 'NONE', *, *, #25211, .F. ) ;
#99=CARTESIAN_POINT ( 'NONE',  ( 2.274274201627632941, 1.975651141464536797, -10.82112760146234720 ) ) ;
#104=DIRECTION ( 'NONE',  ( 0.000000000000000000, 0.000000000000000000, 1.000000000000000000 ) ) ;
#111=AXIS2_PLACEMENT_3D ( 'NONE', #29332, #11295, #4258 ) ;
#118=CARTESIAN_POINT ( 'NONE',  ( 0.000000000000000000, 0.000000000000000000, 0.000000000000000000 ) ) ;
#125=CARTESIAN_POINT ( 'NONE',  ( -4.599999999999996980, 0.000000000000000000, -10.00000000000000178 ) ) ;
#127=CARTESIAN_POINT ( 'NONE',  ( -7.000050800000000351, 7.347880794884120722E-16, 6.000000000000000888 ) ) ;
#134=CARTESIAN_POINT ( 'NONE',  ( 3.063284526839887167, 0.000000000000000000, 0.000000000000000000 ) ) ;
#141=VECTOR ( 'NONE', #13151, 1000.000000000000000 ) ;
#153=CARTESIAN_POINT ( 'NONE',  ( 2.592584512317751333, -0.9926283730658966853, -10.27797909967270584 ) ) ;
#158=AXIS2_PLACEMENT_3D ( 'NONE', #14423, #2390, #20600 ) ;
#165=CARTESIAN_POINT ( 'NONE',  ( 0.7632845268449858223, 8.461683424485162419, -2.223716399040675196 ) ) ;
#166=CARTESIAN_POINT ( 'NONE',  ( 2.857987933988741958, 0.6743480930095439030, 9.536462466408304195 ) ) ;
#175=LINE ( 'NONE', #20570, #28869 ) ;
#178=EDGE_CURVE ( 'NONE', #11731, #23666, #11346, .T. ) ;
#191=VECTOR ( 'NONE', #32403, 1000.000000000000000 ) ;
#192=CARTESIAN_POINT ( 'NONE',  ( 2.326025872504024150, -9.559203939530167560, 5.234065033669340394 ) ) ;
#197=ORIENTED_EDGE ( 'NONE', *, *, #20307, .T. ) ;
#200=AXIS2_PLACEMENT_3D ( 'NONE', #7022, #17038, #24913 ) ;
#203=CIRCLE ( 'NONE', #12966, 11.00000000000000000 ) ;
#212=ORIENTED_EDGE ( 'NONE', *, *, #20307, .F. ) ;
#213=CARTESIAN_POINT ( 'NONE',  ( 0.000000000000000000, 9.620177616658057929, -5.227991826303984624 ) ) ;
#214=CARTESIAN_POINT ( 'NONE',  ( 0.7212198416586443894, 5.676697589981204217, -6.922088825865619022 ) ) ;
#216=CYLINDRICAL_SURFACE ( 'NONE', #29485, 8.749000000000002331 ) ;
#224=ADVANCED_FACE ( 'NONE', ( #25945 ), #18072, .T. ) ;
#226=CARTESIAN_POINT ( 'NONE',  ( 9.101556641444268791, 0.000000000000000000, 0.000000000000000000 ) ) ;
#231=AXIS2_PLACEMENT_3D ( 'NONE', #18970, #26981, #26340 ) ;
#232=CARTESIAN_POINT ( 'NONE',  ( 2.274274201627632053, 10.82112760146237029, 1.975651141464422000 ) ) ;
#236=DIRECTION ( 'NONE',  ( -1.000000000000000000, 0.000000000000000000, 0.000000000000000000 ) ) ;
#243=ORIENTED_EDGE ( 'NONE', *, *, #2990, .F. ) ;
#246=AXIS2_PLACEMENT_3D ( 'NONE', #21103, #12004, #13369 ) ;
#248=CARTESIAN_POINT ( 'NONE',  ( 3.249999999999999556, 9.241976615262160522, -1.699438267350404930 ) ) ;
#273=LINE ( 'NONE', #20493, #10381 ) ;
#283=CARTESIAN_POINT ( 'NONE',  ( 0.3045634402742546376, 4.096074720329792918, 9.425384029459841884 ) ) ;
#286=CARTESIAN_POINT ( 'NONE',  ( -5.750050799999999462, 7.347880794884122694E-16, 6.000000000000002665 ) ) ;
#287=AXIS2_PLACEMENT_3D ( 'NONE', #26971, #13593, #8899 ) ;
#312=CARTESIAN_POINT ( 'NONE',  ( 2.376564509656898139, 9.436969261173645762, 5.239665997526921082 ) ) ;
#342=ORIENTED_EDGE ( 'NONE', *, *, #15050, .F. ) ;
#348=CARTESIAN_POINT ( 'NONE',  ( 0.000000000000000000, 1.999317321091499400, 10.76487093102065451 ) ) ;
#352=CARTESIAN_POINT ( 'NONE',  ( 2.795120667414443094, 7.433119754671809964, -6.320583870825271511 ) ) ;
#353=EDGE_CURVE ( 'NONE', #9758, #29455, #29513, .T. ) ;
#355=CARTESIAN_POINT ( 'NONE',  ( 0.000000000000000000, 0.000000000000000000, 0.000000000000000000 ) ) ;
#367=CARTESIAN_POINT ( 'NONE',  ( 1.624999999999999778, 1.464956435139542767, 10.90201369670499254 ) ) ;
#386=CARTESIAN_POINT ( 'NONE',  ( 1.624999999999999778, 4.762163868918273479, 9.915734732513236338 ) ) ;
#391=CARTESIAN_POINT ( 'NONE',  ( 0.7632845268398871230, 0.000000000000000000, 0.000000000000000000 ) ) ;
#400=CARTESIAN_POINT ( 'NONE',  ( 2.437082316315989150, 1.217322776604855550, -10.59788678609682755 ) ) ;
#414=ADVANCED_FACE ( 'NONE', ( #24506 ), #19854, .T. ) ;
#415=CARTESIAN_POINT ( 'NONE',  ( 3.249999999999999556, -4.472189673936727949, -8.264486777890155622 ) ) ;
#448=VERTEX_POINT ( 'NONE', #22027 ) ;
#461=EDGE_CURVE ( 'NONE', #19227, #4581, #203, .T. ) ;
#465=DIRECTION ( 'NONE',  ( 1.000000000000000000, 0.000000000000000000, 0.000000000000000000 ) ) ;
#475=CARTESIAN_POINT ( 'NONE',  ( 3.249999999999999556, -9.314797388894881180, -1.239665997526989027 ) ) ;
#480=CARTESIAN_POINT ( 'NONE',  ( 3.249999999999999556, -4.472189673936843413, 8.264486777890091673 ) ) ;
#485=ORIENTED_EDGE ( 'NONE', *, *, #21661, .T. ) ;
#492=CARTESIAN_POINT ( 'NONE',  ( 2.437082469501525850, 2.117184480729110252, 10.45536235038312789 ) ) ;
#493=CARTESIAN_POINT ( 'NONE',  ( 2.693711038332267105, -9.791507810136474532, 2.271851790478933264 ) ) ;
#495=DIRECTION ( 'NONE',  ( -1.000000000000000000, -0.000000000000000000, 0.000000000000000000 ) ) ;
#499=ORIENTED_EDGE ( 'NONE', *, *, #31059, .T. ) ;
#504=AXIS2_PLACEMENT_3D ( 'NONE', #2462, #12630, #10109 ) ;
#514=AXIS2_PLACEMENT_3D ( 'NONE', #118, #18332, #28539 ) ;
#520=APPLICATION_CONTEXT ( 'configuration controlled 3d designs of mechanical parts and assemblies' ) ;
#521=CARTESIAN_POINT ( 'NONE',  ( 0.3749740905865333596, -7.612528756000540575, 6.632019415960392905 ) ) ;
#524=ORIENTED_EDGE ( 'NONE', *, *, #21647, .T. ) ;
#529=CARTESIAN_POINT ( 'NONE',  ( 3.249999999999999556, 5.538577986808997267, -6.772677083992326708 ) ) ;
#537=AXIS2_PLACEMENT_3D ( 'NONE', #26514, #11961, #29839 ) ;
#539=CARTESIAN_POINT ( 'NONE',  ( 8.883366670699761071E-16, -1.425064293572414265, 10.85582367538893855 ) ) ;
#552=AXIS2_PLACEMENT_3D ( 'NONE', #1507, #1358, #29414 ) ;
#562=CARTESIAN_POINT ( 'NONE',  ( 0.5664946525141408840, -9.241976615262153416, 2.300561732649529567 ) ) ;
#574=CIRCLE ( 'NONE', #2174, 11.00000000000000000 ) ;
#577=ADVANCED_FACE ( 'NONE', ( #20591 ), #17409, .T. ) ;
#596=VERTEX_POINT ( 'NONE', #15873 ) ;
#600=CARTESIAN_POINT ( 'NONE',  ( 0.1606233661178082250, 7.161985370896794656, -7.854816391752104998 ) ) ;
#602=CIRCLE ( 'NONE', #15549, 6.000000000000000888 ) ;
#613=EDGE_CURVE ( 'NONE', #28731, #7095, #18897, .T. ) ;
#616=CARTESIAN_POINT ( 'NONE',  ( 0.7632845268398871230, 0.000000000000000000, 0.000000000000000000 ) ) ;
#623=CYLINDRICAL_SURFACE ( 'NONE', #32243, 6.000000000000000888 ) ;
#627=ORIENTED_EDGE ( 'NONE', *, *, #2224, .F. ) ;
#640=CIRCLE ( 'NONE', #21982, 8.749000000000002331 ) ;
#643=DIRECTION ( 'NONE',  ( -1.000000000000000000, -0.000000000000000000, 0.000000000000000000 ) ) ;
#644=ORIENTED_EDGE ( 'NONE', *, *, #3720, .T. ) ;
#648=CARTESIAN_POINT ( 'NONE',  ( 2.589202944057205968, -7.715757980413516570, -6.846250362091614861 ) ) ;
#650=ORIENTED_EDGE ( 'NONE', *, *, #29595, .F. ) ;
#655=DIRECTION ( 'NONE',  ( 1.000000000000000000, 0.000000000000000000, 0.000000000000000000 ) ) ;
#660=VERTEX_POINT ( 'NONE', #18554 ) ;
#663=CARTESIAN_POINT ( 'NONE',  ( 0.3076689118644541643, -4.089891983583716417, 9.439351442249007462 ) ) ;
#667=DIRECTION ( 'NONE',  ( -1.000000000000000000, 0.000000000000000000, 0.000000000000000000 ) ) ;
#676=ORIENTED_EDGE ( 'NONE', *, *, #29431, .T. ) ;
#681=VERTEX_POINT ( 'NONE', #28912 ) ;
#684=DIRECTION ( 'NONE',  ( 1.000000000000000000, 0.000000000000000000, 0.000000000000000000 ) ) ;
#689=VERTEX_POINT ( 'NONE', #26432 ) ;
#694=AXIS2_PLACEMENT_3D ( 'NONE', #1892, #22262, #9533 ) ;
#706=CARTESIAN_POINT ( 'NONE',  ( 3.020080181664714924, -8.342499971020062688, 3.262125172866680245 ) ) ;
#721=ORIENTED_EDGE ( 'NONE', *, *, #28942, .F. ) ;
#722=DIRECTION ( 'NONE',  ( -1.000000000000000000, 0.000000000000000000, 0.000000000000000000 ) ) ;
#725=CARTESIAN_POINT ( 'NONE',  ( 0.7632845268398871230, -3.174628368996133876, 8.152713396088751452 ) ) ;
#731=VECTOR ( 'NONE', #17523, 1000.000000000000000 ) ;
#733=CARTESIAN_POINT ( 'NONE',  ( 3.249999999999999556, -9.314797388894900720, 5.239665997526856245 ) ) ;
#734=AXIS2_PLACEMENT_3D ( 'NONE', #26761, #722, #9023 ) ;
#747=ORIENTED_EDGE ( 'NONE', *, *, #22464, .F. ) ;
#762=CARTESIAN_POINT ( 'NONE',  ( 2.274274201625309910, -10.90201369670500853, -1.464956435139685098 ) ) ;
#775=EDGE_LOOP ( 'NONE', ( #2601, #31681, #22240, #22954, #30437 ) ) ;
#780=VERTEX_POINT ( 'NONE', #19708 ) ;
#785=AXIS2_PLACEMENT_3D ( 'NONE', #10480, #20693, #30894 ) ;
#787=ORIENTED_EDGE ( 'NONE', *, *, #30846, .T. ) ;
#790=ADVANCED_FACE ( 'NONE', ( #27408, #9160 ), #14183, .F. ) ;
#795=ORIENTED_EDGE ( 'NONE', *, *, #32126, .F. ) ;
#811=EDGE_CURVE ( 'NONE', #9973, #29226, #28846, .T. ) ;
#815=ORIENTED_EDGE ( 'NONE', *, *, #4615, .T. ) ;
#827=DIRECTION ( 'NONE',  ( -1.000000000000000000, 0.000000000000000000, 0.000000000000000000 ) ) ;
#831=ORIENTED_EDGE ( 'NONE', *, *, #14747, .T. ) ;
#833=CARTESIAN_POINT ( 'NONE',  ( 0.000000000000000000, 9.680994141368845618, -5.222868219166749704 ) ) ;
#834=CARTESIAN_POINT ( 'NONE',  ( 1.624999999999999778, -1.975651141462163807, -10.82112760146738495 ) ) ;
#843=CARTESIAN_POINT ( 'NONE',  ( 0.6791198108364924213, -8.522429291907473115, 3.345077512921551754 ) ) ;
#851=EDGE_CURVE ( 'NONE', #23090, #29352, #14400, .T. ) ;
#858=CARTESIAN_POINT ( 'NONE',  ( 0.3749743548326627818, -10.05686762493553488, 0.8908839545094129342 ) ) ;
#864=CARTESIAN_POINT ( 'NONE',  ( 0.000000000000000000, -6.478011392632841314, -6.807171995660652009 ) ) ;
#875=DIRECTION ( 'NONE',  ( 0.000000000000000000, 0.000000000000000000, -1.000000000000000000 ) ) ;
#879=CARTESIAN_POINT ( 'NONE',  ( 0.9499999999999995115, 0.000000000000000000, -6.999999999999998224 ) ) ;
#883=EDGE_LOOP ( 'NONE', ( #21962, #13403, #22343, #14448, #9426 ) ) ;
#886=EDGE_CURVE ( 'NONE', #10135, #4581, #22553, .T. ) ;
#889=CARTESIAN_POINT ( 'NONE',  ( 1.624999999999999778, 1.975651141462238414, 10.82112760146736896 ) ) ;
#894=CARTESIAN_POINT ( 'NONE',  ( 0.000000000000000000, -6.807171995660538322, -6.478011392632959442 ) ) ;
#909=LINE ( 'NONE', #32114, #29425 ) ;
#910=CARTESIAN_POINT ( 'NONE',  ( 9.101556641444268791, 0.000000000000000000, 0.000000000000000000 ) ) ;
#919=ORIENTED_EDGE ( 'NONE', *, *, #1785, .T. ) ;
#927=ORIENTED_EDGE ( 'NONE', *, *, #23648, .F. ) ;
#933=LINE ( 'NONE', #11451, #32119 ) ;
#941=DIRECTION ( 'NONE',  ( -1.000000000000000000, -0.000000000000000000, 0.000000000000000000 ) ) ;
#950=CARTESIAN_POINT ( 'NONE',  ( 0.5640493910588674220, -7.306425354229854285, -6.134141009809413347 ) ) ;
#951=DIRECTION ( 'NONE',  ( 0.000000000000000000, 0.000000000000000000, 1.000000000000000000 ) ) ;
#954=EDGE_LOOP ( 'NONE', ( #32362, #14583, #4659, #24433 ) ) ;
#968=ORIENTED_EDGE ( 'NONE', *, *, #8596, .F. ) ;
#971=CARTESIAN_POINT ( 'NONE',  ( 0.08034252266819512378, 10.71005054582426830, -1.301095883299802525 ) ) ;
#976=ADVANCED_FACE ( 'NONE', ( #2153 ), #5166, .T. ) ;
#979=VERTEX_POINT ( 'NONE', #25394 ) ;
#981=CARTESIAN_POINT ( 'NONE',  ( 3.063284526843251587, -3.174628368989204308, -8.152713396074016572 ) ) ;
#994=CARTESIAN_POINT ( 'NONE',  ( 2.857987972556676137, -8.111531947321635627, -5.059832898186699346 ) ) ;
#1009=DIRECTION ( 'NONE',  ( 0.000000000000000000, -6.938893903907225222E-15, 1.000000000000000000 ) ) ;
#1026=CARTESIAN_POINT ( 'NONE',  ( 3.020080166740162664, -2.264483761671757467, 8.666653390676586355 ) ) ;
#1043=DIRECTION ( 'NONE',  ( 0.000000000000000000, 0.000000000000000000, 1.000000000000000000 ) ) ;
#1055=AXIS2_PLACEMENT_3D ( 'NONE', #15949, #19630, #27138 ) ;
#1059=DIRECTION ( 'NONE',  ( -1.000000000000000000, 0.000000000000000000, -0.000000000000000000 ) ) ;
#1074=VECTOR ( 'NONE', #8549, 1000.000000000000000 ) ;
#1075=EDGE_LOOP ( 'NONE', ( #18603, #16367, #22713, #25854, #6679 ) ) ;
#1090=DIRECTION ( 'NONE',  ( 0.000000000000000000, 0.000000000000000000, 1.000000000000000000 ) ) ;
#1114=DIRECTION ( 'NONE',  ( 0.000000000000000000, 0.000000000000000000, 1.000000000000000000 ) ) ;
#1126=CARTESIAN_POINT ( 'NONE',  ( 3.063284526839887167, -8.734705317681623171, -0.4999240074895356933 ) ) ;
#1127=AXIS2_PLACEMENT_3D ( 'NONE', #23045, #5329, #12525 ) ;
#1128=CARTESIAN_POINT ( 'NONE',  ( 2.661997753583457360, -0.9074203448822719675, 10.09011512947412115 ) ) ;
#1130=VERTEX_POINT ( 'NONE', #1126 ) ;
#1141=DIRECTION ( 'NONE',  ( 0.000000000000000000, 0.000000000000000000, -1.000000000000000000 ) ) ;
#1145=DIRECTION ( 'NONE',  ( 1.000000000000000000, -0.000000000000000000, -0.000000000000000000 ) ) ;
#1148=AXIS2_PLACEMENT_3D ( 'NONE', #3104, #13259, #23460 ) ;
#1154=DIRECTION ( 'NONE',  ( 1.000000000000000000, -0.000000000000000000, -0.000000000000000000 ) ) ;
#1162=ORIENTED_EDGE ( 'NONE', *, *, #10095, .F. ) ;
#1171=ORIENTED_EDGE ( 'NONE', *, *, #17491, .T. ) ;
#1173=CARTESIAN_POINT ( 'NONE',  ( 3.249999999999999556, -8.152713396088739017, -3.174628368996162298 ) ) ;
#1178=DIRECTION ( 'NONE',  ( 0.000000000000000000, 0.000000000000000000, 1.000000000000000000 ) ) ;
#1189=CIRCLE ( 'NONE', #5468, 8.749000000000002331 ) ;
#1196=CIRCLE ( 'NONE', #734, 8.749000000000002331 ) ;
#1197=CARTESIAN_POINT ( 'NONE',  ( 0.6791199890552930274, -5.814932665552347224, -7.071625480714448742 ) ) ;
#1203=ADVANCED_FACE ( 'NONE', ( #17151 ), #4968, .T. ) ;
#1205=CIRCLE ( 'NONE', #12962, 11.00000000000000000 ) ;
#1209=AXIS2_PLACEMENT_3D ( 'NONE', #24034, #13190, #3670 ) ;
#1213=AXIS2_PLACEMENT_3D ( 'NONE', #32282, #22223, #21875 ) ;
#1226=AXIS2_PLACEMENT_3D ( 'NONE', #16802, #13622, #16447 ) ;
#1231=CIRCLE ( 'NONE', #29003, 3.499999999999999556 ) ;
#1238=DIRECTION ( 'NONE',  ( 1.000000000000000000, 0.000000000000000000, 0.000000000000000000 ) ) ;
#1239=LINE ( 'NONE', #3914, #23234 ) ;
#1247=CARTESIAN_POINT ( 'NONE',  ( 3.249999999999999556, 0.000000000000000000, 0.000000000000000000 ) ) ;
#1253=CARTESIAN_POINT ( 'NONE',  ( 2.274274201625317460, -7.593217523260661572, 7.958834565716747633 ) ) ;
#1262=EDGE_LOOP ( 'NONE', ( #12802, #23937, #26982, #20183, #3533, #31501, #28149, #28824, #16780, #16189, #11355, #27700, #28821, #16218, #927, #7872, #1965, #25359, #24449, #23284, #21082, #17252, #5551, #18711, #17175, #19865, #30878, #30833, #4783, #9452, #31844, #12473, #26550, #4502, #24505, #3026, #15582, #10297, #29237, #12506, #28495, #6404, #4976, #14184, #212, #14762 ) ) ;
#1266=CYLINDRICAL_SURFACE ( 'NONE', #8001, 4.000000000000001776 ) ;
#1272=ORIENTED_EDGE ( 'NONE', *, *, #3151, .T. ) ;
#1277=DIRECTION ( 'NONE',  ( -1.000000000000000000, 0.000000000000000000, 0.000000000000000000 ) ) ;
#1286=AXIS2_PLACEMENT_3D ( 'NONE', #12622, #17627, #4771 ) ;
#1298=B_SPLINE_CURVE_WITH_KNOTS ( 'NONE', 3,
 ( #27614, #12390, #32820, #25088, #2392, #27763, #4877, #15058 ),
 .UNSPECIFIED., .F., .F.,
 ( 4, 2, 2, 4 ),
 ( 5.099451029798333178E-07, 0.001229189835658059133, 0.001843529780935598741, 0.002457869726213138782 ),
 .UNSPECIFIED. ) ;
#1315=CARTESIAN_POINT ( 'NONE',  ( 2.274274201625309910, -1.464956435139646462, 10.90201369670501386 ) ) ;
#1329=CARTESIAN_POINT ( 'NONE',  ( 0.000000000000000000, 0.000000000000000000, 0.000000000000000000 ) ) ;
#1358=DIRECTION ( 'NONE',  ( -1.000000000000000000, -0.000000000000000000, -0.000000000000000000 ) ) ;
#1359=VERTEX_POINT ( 'NONE', #2467 ) ;
#1380=CARTESIAN_POINT ( 'NONE',  ( 2.440333653308764728, 9.715096239907470732, -4.424884217119326557 ) ) ;
#1382=CARTESIAN_POINT ( 'NONE',  ( 3.063284526843530031, -4.729683950890320787, 7.360373001715534436 ) ) ;
#1383=ORIENTED_EDGE ( 'NONE', *, *, #30707, .F. ) ;
#1397=CARTESIAN_POINT ( 'NONE',  ( 0.000000000000000000, -6.478011392632939902, 6.807171995660557862 ) ) ;
#1403=CARTESIAN_POINT ( 'NONE',  ( 0.000000000000000000, -10.82112760146737429, 1.975651141462198890 ) ) ;
#1421=CARTESIAN_POINT ( 'NONE',  ( 3.063284526843530031, -4.729683950890320787, 7.360373001715534436 ) ) ;
#1448=ORIENTED_EDGE ( 'NONE', *, *, #21254, .F. ) ;
#1459=ORIENTED_EDGE ( 'NONE', *, *, #31745, .T. ) ;
#1466=CARTESIAN_POINT ( 'NONE',  ( 2.864531114197725881, 5.073635298885146305, 8.105385692883624316 ) ) ;
#1473=ORIENTED_EDGE ( 'NONE', *, *, #11783, .T. ) ;
#1478=CARTESIAN_POINT ( 'NONE',  ( 2.795120570943885774, -9.022485053477835137, 3.714272345030835254 ) ) ;
#1485=ORIENTED_EDGE ( 'NONE', *, *, #23814, .F. ) ;
#1490=CARTESIAN_POINT ( 'NONE',  ( 3.063284526839890276, 7.360373001730978082, -4.729683950898788680 ) ) ;
#1507=CARTESIAN_POINT ( 'NONE',  ( 0.000000000000000000, 0.000000000000000000, 0.000000000000000000 ) ) ;
#1527=ORIENTED_EDGE ( 'NONE', *, *, #21268, .T. ) ;
#1533=DIRECTION ( 'NONE',  ( 0.000000000000000000, 0.000000000000000000, 1.000000000000000000 ) ) ;
#1543=EDGE_CURVE ( 'NONE', #10253, #11257, #13905, .T. ) ;
#1547=CARTESIAN_POINT ( 'NONE',  ( 3.249999999999999556, -2.223716399045632119, 8.461683424509308438 ) ) ;
#1557=VERTEX_POINT ( 'NONE', #9080 ) ;
#1558=CARTESIAN_POINT ( 'NONE',  ( 0.3045634671934224214, 0.9829946734957575316, 10.22982953726899957 ) ) ;
#1570=EDGE_CURVE ( 'NONE', #31361, #23619, #3258, .T. ) ;
#1571=CARTESIAN_POINT ( 'NONE',  ( 2.440333830125739567, -5.258796312403307915, 9.290196408096516478 ) ) ;
#1575=ORIENTED_EDGE ( 'NONE', *, *, #4757, .F. ) ;
#1607=AXIS2_PLACEMENT_3D ( 'NONE', #226, #10895, #13366 ) ;
#1608=VERTEX_POINT ( 'NONE', #27145 ) ;
#1617=B_SPLINE_CURVE_WITH_KNOTS ( 'NONE', 3,
 ( #31590, #5688, #28595, #26426, #994, #15866, #31278, #8677 ),
 .UNSPECIFIED., .F., .F.,
 ( 4, 2, 2, 4 ),
 ( 2.152606640961436226E-07, 0.001262065476475215334, 0.001892990584380772065, 0.002523915692286328796 ),
 .UNSPECIFIED. ) ;
#1623=EDGE_CURVE ( 'NONE', #1608, #15940, #18476, .T. ) ;
#1636=AXIS2_PLACEMENT_3D ( 'NONE', #7760, #5238, #9921 ) ;
#1640=PLANE ( 'NONE',  #23083 ) ;
#1662=ORIENTED_EDGE ( 'NONE', *, *, #25580, .F. ) ;
#1674=CARTESIAN_POINT ( 'NONE',  ( -4.599999999999996092, 0.000000000000000000, 0.000000000000000000 ) ) ;
#1675=DIRECTION ( 'NONE',  ( 0.000000000000000000, 0.000000000000000000, 1.000000000000000000 ) ) ;
#1699=CARTESIAN_POINT ( 'NONE',  ( 1.624999999999999778, 9.915734732513284300, -4.762163868918169563 ) ) ;
#1702=TOROIDAL_SURFACE ( 'NONE', #14492, 3.895301350492843540, 15.00000000000000178 ) ;
#1715=DIRECTION ( 'NONE',  ( 0.000000000000000000, -8.881784197001252323E-16, 1.000000000000000000 ) ) ;
#1722=EDGE_LOOP ( 'NONE', ( #5182, #32473, #8911, #9479 ) ) ;
#1725=AXIS2_PLACEMENT_3D ( 'NONE', #14247, #17432, #6740 ) ;
#1731=CARTESIAN_POINT ( 'NONE',  ( 0.3045634274093902416, -8.853895822767180235, -5.217683548413607930 ) ) ;
#1732=ORIENTED_EDGE ( 'NONE', *, *, #12692, .F. ) ;
#1737=CARTESIAN_POINT ( 'NONE',  ( 2.440333863880882248, -7.210444323286300694, -7.872241054361076351 ) ) ;
#1745=VERTEX_POINT ( 'NONE', #213 ) ;
#1756=VECTOR ( 'NONE', #32491, 1000.000000000000000 ) ;
#1760=CARTESIAN_POINT ( 'NONE',  ( 0.3749743454410877086, -2.260462012960331890, 9.839947797887042213 ) ) ;
#1776=DIRECTION ( 'NONE',  ( 0.000000000000000000, -0.9510565162951500895, -0.3090169943749582204 ) ) ;
#1778=AXIS2_PLACEMENT_3D ( 'NONE', #15682, #31062, #31244 ) ;
#1780=CARTESIAN_POINT ( 'NONE',  ( 3.249999999999999556, -3.174628368996019301, -8.152713396088794084 ) ) ;
#1785=EDGE_CURVE ( 'NONE', #3483, #11786, #17671, .T. ) ;
#1807=AXIS2_PLACEMENT_3D ( 'NONE', #3221, #28474, #5081 ) ;
#1808=ORIENTED_EDGE ( 'NONE', *, *, #19732, .T. ) ;
#1809=EDGE_CURVE ( 'NONE', #18943, #32789, #31602, .T. ) ;
#1823=FACE_OUTER_BOUND ( 'NONE', #30371, .T. ) ;
#1836=CIRCLE ( 'NONE', #20524, 10.94895958125474245 ) ;
#1839=CARTESIAN_POINT ( 'NONE',  ( 2.661997850953047973, 8.696442646092101825, -5.196702353893110526 ) ) ;
#1841=EDGE_LOOP ( 'NONE', ( #15800, #19619, #650, #24516 ) ) ;
#1848=EDGE_CURVE ( 'NONE', #30559, #10039, #18747, .T. ) ;
#1857=ADVANCED_FACE ( 'NONE', ( #24049 ), #21574, .T. ) ;
#1860=ORIENTED_EDGE ( 'NONE', *, *, #25337, .T. ) ;
#1864=CARTESIAN_POINT ( 'NONE',  ( 1.624999999999999778, -1.464956435139619151, 10.90201369670498366 ) ) ;
#1865=DIRECTION ( 'NONE',  ( -1.000000000000000000, 0.000000000000000000, 0.000000000000000000 ) ) ;
#1866=ORIENTED_EDGE ( 'NONE', *, *, #5979, .F. ) ;
#1879=DIRECTION ( 'NONE',  ( 0.000000000000000000, 0.000000000000000000, 1.000000000000000000 ) ) ;
#1883=EDGE_CURVE ( 'NONE', #9751, #2084, #25940, .T. ) ;
#1884=TOROIDAL_SURFACE ( 'NONE', #287, 6.923700951379997193, 9.000000000000000000 ) ;
#1888=DIRECTION ( 'NONE',  ( -1.000000000000000000, 0.000000000000000000, 0.000000000000000000 ) ) ;
#1889=ORIENTED_EDGE ( 'NONE', *, *, #18735, .T. ) ;
#1892=CARTESIAN_POINT ( 'NONE',  ( -7.000050800000000351, 0.000000000000000000, 0.000000000000000000 ) ) ;
#1896=CARTESIAN_POINT ( 'NONE',  ( 2.492101788275272067, -9.149023314703491394, 5.239665997526232744 ) ) ;
#1905=CARTESIAN_POINT ( 'NONE',  ( 2.661997913519439596, 9.876677602395393052, -2.255009087902827503 ) ) ;
#1912=CYLINDRICAL_SURFACE ( 'NONE', #11887, 4.000000000000002665 ) ;
#1913=DIRECTION ( 'NONE',  ( 1.000000000000000000, 0.000000000000000000, 0.000000000000000000 ) ) ;
#1918=CARTESIAN_POINT ( 'NONE',  ( -3.683682291401270757E-13, 9.884132761439586190, -4.709950686175258916 ) ) ;
#1943=CARTESIAN_POINT ( 'NONE',  ( 1.624999999999999778, -7.958834565716711218, -7.593217523260671342 ) ) ;
#1965=ORIENTED_EDGE ( 'NONE', *, *, #32430, .T. ) ;
#1969=LINE ( 'NONE', #17339, #20889 ) ;
#1971=VERTEX_POINT ( 'NONE', #27224 ) ;
#1994=VERTEX_POINT ( 'NONE', #19713 ) ;
#2004=ORIENTED_EDGE ( 'NONE', *, *, #27657, .F. ) ;
#2006=CARTESIAN_POINT ( 'NONE',  ( 2.857987933988744622, 9.536462466408302419, -0.6743480930095767656 ) ) ;
#2019=ADVANCED_FACE ( 'NONE', ( #29912 ), #14335, .F. ) ;
#2029=CARTESIAN_POINT ( 'NONE',  ( 0.000000000000000000, 7.944914065997111585, 7.533794289458081828 ) ) ;
#2031=ORIENTED_EDGE ( 'NONE', *, *, #11415, .T. ) ;
#2032=EDGE_CURVE ( 'NONE', #7398, #5630, #9695, .T. ) ;
#2036=ORIENTED_EDGE ( 'NONE', *, *, #30254, .T. ) ;
#2038=ORIENTED_EDGE ( 'NONE', *, *, #13264, .T. ) ;
#2042=VERTEX_POINT ( 'NONE', #30411 ) ;
#2046=ORIENTED_EDGE ( 'NONE', *, *, #9841, .T. ) ;
#2047=CARTESIAN_POINT ( 'NONE',  ( 0.000000000000000000, -8.264486777890077462, -4.472189673936872722 ) ) ;
#2048=CARTESIAN_POINT ( 'NONE',  ( 3.249999999999999556, -8.475820894093002877, 4.057423117305364535 ) ) ;
#2055=CARTESIAN_POINT ( 'NONE',  ( 2.357329973329929551, -9.815384016743289308, -4.593471141847171424 ) ) ;
#2060=DIRECTION ( 'NONE',  ( 0.000000000000000000, 0.000000000000000000, -1.000000000000000000 ) ) ;
#2070=CARTESIAN_POINT ( 'NONE',  ( 0.000000000000000000, -1.464956435139465052, -10.90201369670500142 ) ) ;
#2071=ORIENTED_EDGE ( 'NONE', *, *, #26877, .F. ) ;
#2082=CARTESIAN_POINT ( 'NONE',  ( 0.7632845268398871230, 8.152713396088806519, -3.174628368995990879 ) ) ;
#2084=VERTEX_POINT ( 'NONE', #165 ) ;
#2085=CARTESIAN_POINT ( 'NONE',  ( 2.440333710190582650, 2.130583817697960569, -10.46055952248790533 ) ) ;
#2100=CARTESIAN_POINT ( 'NONE',  ( 0.1574692293610879257, 4.391622967208396844, 9.672096048330979912 ) ) ;
#2104=DIRECTION ( 'NONE',  ( 1.000000000000000000, 0.000000000000000000, 0.000000000000000000 ) ) ;
#2109=CARTESIAN_POINT ( 'NONE',  ( -10.00000000000000000, 0.000000000000000000, 0.000000000000000000 ) ) ;
#2119=EDGE_CURVE ( 'NONE', #23619, #22462, #4826, .T. ) ;
#2144=EDGE_LOOP ( 'NONE', ( #32983, #26016, #28137, #342 ) ) ;
#2153=FACE_OUTER_BOUND ( 'NONE', #10144, .T. ) ;
#2159=CARTESIAN_POINT ( 'NONE',  ( 3.249999999999999556, -4.057423117305452465, 8.475820894092962021 ) ) ;
#2163=ORIENTED_EDGE ( 'NONE', *, *, #5095, .T. ) ;
#2166=FACE_OUTER_BOUND ( 'NONE', #3125, .T. ) ;
#2171=B_SPLINE_CURVE_WITH_KNOTS ( 'NONE', 3,
 ( #28398, #16179, #5668, #31402, #648, #28878, #15511, #26060 ),
 .UNSPECIFIED., .F., .F.,
 ( 4, 2, 2, 4 ),
 ( 2.737843117611516695E-07, 0.001261207499628693753, 0.001891674357287160451, 0.002522141214945628450 ),
 .UNSPECIFIED. ) ;
#2174=AXIS2_PLACEMENT_3D ( 'NONE', #20918, #16378, #6032 ) ;
#2185=ORIENTED_EDGE ( 'NONE', *, *, #12245, .F. ) ;
#2189=CARTESIAN_POINT ( 'NONE',  ( 2.864531314636033166, 6.140839842381263125, -7.330015575757827584 ) ) ;
#2198=EDGE_CURVE ( 'NONE', #19976, #24335, #6493, .T. ) ;
#2199=VERTEX_POINT ( 'NONE', #23530 ) ;
#2202=AXIS2_PLACEMENT_3D ( 'NONE', #7305, #22852, #14974 ) ;
#2214=CARTESIAN_POINT ( 'NONE',  ( 2.274274201625313907, -9.915734732513202587, -4.762163868918404930 ) ) ;
#2219=CARTESIAN_POINT ( 'NONE',  ( 3.249999999999999556, 8.461683424509315543, 2.223716399045601921 ) ) ;
#2224=EDGE_CURVE ( 'NONE', #22885, #32298, #26393, .T. ) ;
#2226=CARTESIAN_POINT ( 'NONE',  ( 2.274274201625327230, 10.90201369670498543, 1.464956435139579183 ) ) ;
#2235=EDGE_CURVE ( 'NONE', #32250, #14334, #11327, .T. ) ;
#2236=CARTESIAN_POINT ( 'NONE',  ( 3.063284526839887167, 0.000000000000000000, 0.000000000000000000 ) ) ;
#2238=AXIS2_PLACEMENT_3D ( 'NONE', #2944, #16567, #13733 ) ;
#2245=ORIENTED_EDGE ( 'NONE', *, *, #26632, .T. ) ;
#2257=CARTESIAN_POINT ( 'NONE',  ( 2.274274201625315683, -4.762163868918371179, 9.915734732513216798 ) ) ;
#2264=CYLINDRICAL_SURFACE ( 'NONE', #4901, 4.000000000000001776 ) ;
#2267=AXIS2_PLACEMENT_3D ( 'NONE', #19979, #27136, #6902 ) ;
#2268=CARTESIAN_POINT ( 'NONE',  ( 0.000000000000000000, -1.975651141462165139, -10.82112760146738317 ) ) ;
#2270=CARTESIAN_POINT ( 'NONE',  ( 0.3786097929198382617, 8.648460131863847877, 5.187364053035338429 ) ) ;
#2286=AXIS2_PLACEMENT_3D ( 'NONE', #29302, #21628, #6390 ) ;
#2296=FACE_OUTER_BOUND ( 'NONE', #18324, .T. ) ;
#2311=CARTESIAN_POINT ( 'NONE',  ( 2.274274201625317016, -1.975651141462152482, -10.82112760146740982 ) ) ;
#2317=CARTESIAN_POINT ( 'NONE',  ( 8.883366670699761071E-16, -1.425064293572414265, 10.85582367538893855 ) ) ;
#2323=VERTEX_POINT ( 'NONE', #4135 ) ;
#2326=B_SPLINE_CURVE_WITH_KNOTS ( 'NONE', 3,
 ( #4626, #20172, #26017, #10467, #23334, #2465 ),
 .UNSPECIFIED., .F., .F.,
 ( 4, 2, 4 ),
 ( 0.0008064882591616886988, 0.001631107178945768489, 0.002455726098729848171 ),
 .UNSPECIFIED. ) ;
#2332=ORIENTED_EDGE ( 'NONE', *, *, #22581, .T. ) ;
#2333=CARTESIAN_POINT ( 'NONE',  ( 0.7632845268398871230, -8.152713396088739017, -3.174628368996162298 ) ) ;
#2340=CIRCLE ( 'NONE', #27406, 10.99999999999999822 ) ;
#2346=AXIS2_PLACEMENT_3D ( 'NONE', #27753, #13689, #11033 ) ;
#2354=ORIENTED_EDGE ( 'NONE', *, *, #9148, .T. ) ;
#2356=CARTESIAN_POINT ( 'NONE',  ( 3.249999999999999556, 6.478011392632983423, -6.807171995660517005 ) ) ;
#2365=CARTESIAN_POINT ( 'NONE',  ( 3.063284526839887167, 0.000000000000000000, 0.000000000000000000 ) ) ;
#2373=PRODUCT_DEFINITION_FORMATION_WITH_SPECIFIED_SOURCE ( 'ANY', '', #12431, .NOT_KNOWN. ) ;
#2377=CARTESIAN_POINT ( 'NONE',  ( 3.020080256209070502, 6.926136578651395759, -5.680439424473750165 ) ) ;
#2379=DIRECTION ( 'NONE',  ( -1.000000000000000000, -0.000000000000000000, 0.000000000000000000 ) ) ;
#2380=ORIENTED_EDGE ( 'NONE', *, *, #17335, .T. ) ;
#2386=ORIENTED_EDGE ( 'NONE', *, *, #7504, .T. ) ;
#2390=DIRECTION ( 'NONE',  ( 1.000000000000000000, 0.000000000000000000, 0.000000000000000000 ) ) ;
#2392=CARTESIAN_POINT ( 'NONE',  ( 0.5640492482744796643, 5.053269777826659315, 8.091724846332267518 ) ) ;
#2398=CARTESIAN_POINT ( 'NONE',  ( 2.864530965498453874, 9.276519854389890796, -2.320611941139828716 ) ) ;
#2401=CARTESIAN_POINT ( 'NONE',  ( 2.440333863880882248, -7.872241054361043489, 7.210444323286330004 ) ) ;
#2413=ORIENTED_EDGE ( 'NONE', *, *, #18188, .F. ) ;
#2429=EDGE_LOOP ( 'NONE', ( #22197, #11013, #30995, #28304 ) ) ;
#2447=DIRECTION ( 'NONE',  ( 0.000000000000000000, 1.000000000000000000, -1.224646799147353207E-16 ) ) ;
#2456=DIRECTION ( 'NONE',  ( -1.000000000000000000, 0.000000000000000000, 0.000000000000000000 ) ) ;
#2460=CARTESIAN_POINT ( 'NONE',  ( 3.249999999999999556, -3.174628368996134320, 8.152713396088753228 ) ) ;
#2462=CARTESIAN_POINT ( 'NONE',  ( 3.249999999999999556, -9.241976615262169403, 1.699438267350338982 ) ) ;
#2465=CARTESIAN_POINT ( 'NONE',  ( -3.687551352559800218E-13, 10.76487093102146098, 1.999317321091203192 ) ) ;
#2467=CARTESIAN_POINT ( 'NONE',  ( 0.000000000000000000, 1.425064293572489094, -10.85582367538892790 ) ) ;
#2468=CARTESIAN_POINT ( 'NONE',  ( 4.546085788309846232E-16, -9.884132761439026638, -4.709950686174718903 ) ) ;
#2482=CARTESIAN_POINT ( 'NONE',  ( 3.063284526839887167, 8.152713396088806519, -3.174628368995990879 ) ) ;
#2483=CARTESIAN_POINT ( 'NONE',  ( 0.7632845268398871230, -0.4999240074895051067, 8.734705317681624948 ) ) ;
#2486=VERTEX_POINT ( 'NONE', #17342 ) ;
#2488=VERTEX_POINT ( 'NONE', #28350 ) ;
#2519=CARTESIAN_POINT ( 'NONE',  ( 0.1606233060840195348, 4.384181225613662747, -9.683549581718697397 ) ) ;
#2527=CARTESIAN_POINT ( 'NONE',  ( 2.494186907641620987, -10.32103073665143533, 2.161749562925007417 ) ) ;
#2534=CARTESIAN_POINT ( 'NONE',  ( 3.063284526839890720, 5.538577986808988385, -6.772677083992317826 ) ) ;
#2537=ORIENTED_EDGE ( 'NONE', *, *, #16337, .T. ) ;
#2540=EDGE_LOOP ( 'NONE', ( #27901, #4885, #17701, #14869 ) ) ;
#2551=CARTESIAN_POINT ( 'NONE',  ( 10.25005080000000035, 0.000000000000000000, 0.000000000000000000 ) ) ;
#2552=EDGE_CURVE ( 'NONE', #30559, #31355, #1836, .T. ) ;
#2555=CARTESIAN_POINT ( 'NONE',  ( 1.615481217893400349E-16, -4.709950686174685153, 9.884132761439042625 ) ) ;
#2563=ORIENTED_EDGE ( 'NONE', *, *, #12056, .T. ) ;
#2576=CARTESIAN_POINT ( 'NONE',  ( 0.6791198108364936425, -3.345077512921525553, -8.522429291907481996 ) ) ;
#2583=CARTESIAN_POINT ( 'NONE',  ( 3.063284526839891608, 8.734705317681621395, 0.4999240074894719665 ) ) ;
#2592=CARTESIAN_POINT ( 'NONE',  ( 2.274274201625327230, -7.593217523260523016, -7.958834565716851550 ) ) ;
#2597=CARTESIAN_POINT ( 'NONE',  ( 0.5988559074951336214, 7.987249520745825393, 5.028194040378882512 ) ) ;
#2601=ORIENTED_EDGE ( 'NONE', *, *, #11514, .F. ) ;
#2604=CYLINDRICAL_SURFACE ( 'NONE', #11414, 8.749000000000002331 ) ;
#2608=CARTESIAN_POINT ( 'NONE',  ( 2.976845970491569293, 7.079702685456871869, 5.822399416825323470 ) ) ;
#2616=ADVANCED_FACE ( 'NONE', ( #8301 ), #18494, .F. ) ;
#2629=CARTESIAN_POINT ( 'NONE',  ( 3.063284526839890276, 4.729683950898869504, 7.360373001730925679 ) ) ;
#2646=CARTESIAN_POINT ( 'NONE',  ( 0.5664946525141408840, -9.241976615262153416, 2.300561732649529567 ) ) ;
#2647=ORIENTED_EDGE ( 'NONE', *, *, #1785, .F. ) ;
#2652=ADVANCED_FACE ( 'NONE', ( #16303 ), #23194, .T. ) ;
#2654=DIRECTION ( 'NONE',  ( 1.000000000000000000, -0.000000000000000000, -0.000000000000000000 ) ) ;
#2670=VERTEX_POINT ( 'NONE', #11460 ) ;
#2677=CARTESIAN_POINT ( 'NONE',  ( 0.3045634274091702509, 5.217683548413707406, -8.853895822767748669 ) ) ;
#2685=LINE ( 'NONE', #7865, #18264 ) ;
#2710=FACE_OUTER_BOUND ( 'NONE', #26412, .T. ) ;
#2712=ORIENTED_EDGE ( 'NONE', *, *, #19321, .F. ) ;
#2724=ORIENTED_EDGE ( 'NONE', *, *, #28904, .F. ) ;
#2738=CIRCLE ( 'NONE', #30518, 8.749000000000002331 ) ;
#2744=ORIENTED_EDGE ( 'NONE', *, *, #11590, .F. ) ;
#2762=CIRCLE ( 'NONE', #26767, 10.99999999999999822 ) ;
#2765=CYLINDRICAL_SURFACE ( 'NONE', #23991, 4.000000000000001776 ) ;
#2775=ADVANCED_FACE ( 'NONE', ( #9428 ), #14426, .T. ) ;
#2777=AXIS2_PLACEMENT_3D ( 'NONE', #19085, #16554, #26764 ) ;
#2779=DIRECTION ( 'NONE',  ( 0.000000000000000000, 0.000000000000000000, 1.000000000000000000 ) ) ;
#2784=CARTESIAN_POINT ( 'NONE',  ( 0.7632845268398871230, 0.000000000000000000, 0.000000000000000000 ) ) ;
#2804=B_SPLINE_CURVE_WITH_KNOTS ( 'NONE', 3,
 ( #16658, #31559, #1466, #29207, #11324, #13972, #6297, #16333 ),
 .UNSPECIFIED., .F., .F.,
 ( 4, 2, 2, 4 ),
 ( 2.304311362529371646E-07, 0.001261163669367344363, 0.001891630288482889968, 0.002522096907598435789 ),
 .UNSPECIFIED. ) ;
#2813=CIRCLE ( 'NONE', #26364, 8.749000000000002331 ) ;
#2819=VECTOR ( 'NONE', #7274, 1000.000000000000000 ) ;
#2829=EDGE_CURVE ( 'NONE', #6812, #26011, #12807, .T. ) ;
#2834=VERTEX_POINT ( 'NONE', #7413 ) ;
#2836=CIRCLE ( 'NONE', #27919, 4.000000000000002665 ) ;
#2837=VERTEX_POINT ( 'NONE', #2257 ) ;
#2838=CARTESIAN_POINT ( 'NONE',  ( 3.063284526839887167, 3.174628368996073924, 8.152713396088772768 ) ) ;
#2840=EDGE_CURVE ( 'NONE', #2670, #31785, #21365, .T. ) ;
#2846=DIRECTION ( 'NONE',  ( -1.000000000000000000, 0.000000000000000000, 0.000000000000000000 ) ) ;
#2850=ADVANCED_FACE ( 'NONE', ( #27814 ), #30509, .T. ) ;
#2865=AXIS2_PLACEMENT_3D ( 'NONE', #14796, #7619, #2104 ) ;
#2867=ORIENTED_EDGE ( 'NONE', *, *, #25337, .F. ) ;
#2870=CARTESIAN_POINT ( 'NONE',  ( -3.688478485700421711E-13, 5.227991826304162259, -9.620177616658798669 ) ) ;
#2872=ADVANCED_FACE ( 'NONE', ( #20148 ), #25137, .F. ) ;
#2873=DIRECTION ( 'NONE',  ( -1.000000000000000000, 0.000000000000000000, 0.000000000000000000 ) ) ;
#2882=DIRECTION ( 'NONE',  ( -1.000000000000000000, 0.000000000000000000, 0.000000000000000000 ) ) ;
#2894=EDGE_LOOP ( 'NONE', ( #17490, #29724, #32738, #4422, #31929 ) ) ;
#2896=DIRECTION ( 'NONE',  ( -0.000000000000000000, -1.000000000000000000, -0.000000000000000000 ) ) ;
#2910=DIRECTION ( 'NONE',  ( 0.000000000000000000, 0.000000000000000000, 1.000000000000000000 ) ) ;
#2919=DIRECTION ( 'NONE',  ( -1.000000000000000000, 0.000000000000000000, 0.000000000000000000 ) ) ;
#2927=FACE_OUTER_BOUND ( 'NONE', #14693, .T. ) ;
#2930=DIRECTION ( 'NONE',  ( 0.000000000000000000, 1.776356839400250149E-14, 1.000000000000000000 ) ) ;
#2932=ORIENTED_EDGE ( 'NONE', *, *, #5346, .T. ) ;
#2938=CARTESIAN_POINT ( 'NONE',  ( 2.976845687893346248, 0.5490754078163789798, -9.149921655307444723 ) ) ;
#2944=CARTESIAN_POINT ( 'NONE',  ( 0.7632845268398871230, 0.000000000000000000, 0.000000000000000000 ) ) ;
#2947=ORIENTED_EDGE ( 'NONE', *, *, #31869, .T. ) ;
#2949=DIRECTION ( 'NONE',  ( -1.000000000000000000, 0.000000000000000000, 0.000000000000000000 ) ) ;
#2955=FACE_OUTER_BOUND ( 'NONE', #12591, .T. ) ;
#2963=CARTESIAN_POINT ( 'NONE',  ( 0.000000000000000000, 7.958834565716766285, 7.593217523260605617 ) ) ;
#2968=VERTEX_POINT ( 'NONE', #7265 ) ;
#2971=B_SPLINE_CURVE_WITH_KNOTS ( 'NONE', 3,
 ( #25547, #30258, #17687, #12521, #23225, #32772, #9850, #12672 ),
 .UNSPECIFIED., .F., .F.,
 ( 4, 2, 2, 4 ),
 ( 5.099451029798776812E-07, 0.001229189835658058482, 0.001843529780935597657, 0.002457869726213138782 ),
 .UNSPECIFIED. ) ;
#2973=DIRECTION ( 'NONE',  ( -1.000000000000000000, 0.000000000000000000, 0.000000000000000000 ) ) ;
#2990=EDGE_CURVE ( 'NONE', #5275, #660, #22414, .T. ) ;
#2996=PLANE ( 'NONE',  #31604 ) ;
#2998=CARTESIAN_POINT ( 'NONE',  ( 3.249999999999999556, 0.4999240074895661690, -8.734705317681621395 ) ) ;
#3006=EDGE_LOOP ( 'NONE', ( #2724, #5127, #7346, #7588, #3939 ) ) ;
#3009=ORIENTED_EDGE ( 'NONE', *, *, #8201, .T. ) ;
#3010=CARTESIAN_POINT ( 'NONE',  ( 0.6728001046013577513, 8.512517952453869441, 3.357496170308674976 ) ) ;
#3018=CARTESIAN_POINT ( 'NONE',  ( -18.30155664144426453, 0.000000000000000000, 0.000000000000000000 ) ) ;
#3026=ORIENTED_EDGE ( 'NONE', *, *, #25928, .T. ) ;
#3028=CARTESIAN_POINT ( 'NONE',  ( 3.063284526839889832, 3.174628368996186278, -8.152713396088721254 ) ) ;
#3042=ORIENTED_EDGE ( 'NONE', *, *, #13464, .F. ) ;
#3050=CARTESIAN_POINT ( 'NONE',  ( 0.6728002192067955578, 5.823680980834268439, -7.058361986476028527 ) ) ;
#3056=DIRECTION ( 'NONE',  ( -1.000000000000000000, 0.000000000000000000, 0.000000000000000000 ) ) ;
#3063=FACE_OUTER_BOUND ( 'NONE', #13917, .T. ) ;
#3076=DIRECTION ( 'NONE',  ( 1.000000000000000000, 0.000000000000000000, 0.000000000000000000 ) ) ;
#3084=CARTESIAN_POINT ( 'NONE',  ( 2.589202797589366334, 1.003524335601164497, -10.26630467377257538 ) ) ;
#3104=CARTESIAN_POINT ( 'NONE',  ( 2.274274201625327230, 0.000000000000000000, 0.000000000000000000 ) ) ;
#3125=EDGE_LOOP ( 'NONE', ( #11539, #1171, #30153, #4557, #22792, #21877, #19127, #29576, #2386, #23598, #20895, #1473, #5775, #31632, #16603, #31539, #9229, #31468, #24458, #29399, #13134, #1272, #8593, #21645, #676, #23607, #26554, #12686, #15520, #23753, #20477, #4167, #13745, #31599, #23372, #26961, #5485, #11854, #26760, #2932, #627, #13449, #18862, #24194, #33073, #17565 ) ) ;
#3139=FACE_OUTER_BOUND ( 'NONE', #32296, .T. ) ;
#3151=EDGE_CURVE ( 'NONE', #9751, #14334, #16077, .T. ) ;
#3153=CARTESIAN_POINT ( 'NONE',  ( 0.000000000000000000, 9.884132761439062165, 4.709950686174647849 ) ) ;
#3158=CARTESIAN_POINT ( 'NONE',  ( 3.249999999999999556, 0.000000000000000000, 3.499999999999999556 ) ) ;
#3168=VERTEX_POINT ( 'NONE', #9900 ) ;
#3172=DIRECTION ( 'NONE',  ( 0.000000000000000000, 0.000000000000000000, 1.000000000000000000 ) ) ;
#3180=ADVANCED_FACE ( 'NONE', ( #23103 ), #30446, .T. ) ;
#3190=CARTESIAN_POINT ( 'NONE',  ( 0.7632845268398876781, -8.734705317681624948, 0.4999240074894106822 ) ) ;
#3198=CIRCLE ( 'NONE', #22998, 6.000000000000000888 ) ;
#3221=CARTESIAN_POINT ( 'NONE',  ( -10.00000000000000000, 0.000000000000000000, 0.000000000000000000 ) ) ;
#3227=ORIENTED_EDGE ( 'NONE', *, *, #7500, .T. ) ;
#3233=ADVANCED_FACE ( 'NONE', ( #2710 ), #23580, .T. ) ;
#3236=AXIS2_PLACEMENT_3D ( 'NONE', #27896, #12821, #5013 ) ;
#3237=AXIS2_PLACEMENT_3D ( 'NONE', #21058, #31260, #18530 ) ;
#3241=ORIENTED_EDGE ( 'NONE', *, *, #27316, .F. ) ;
#3242=AXIS2_PLACEMENT_3D ( 'NONE', #8034, #16031, #28757 ) ;
#3244=B_SPLINE_CURVE_WITH_KNOTS ( 'NONE', 3,
 ( #29955, #7044, #4386, #12071, #14571, #17255, #1896, #14227 ),
 .UNSPECIFIED., .F., .F.,
 ( 4, 2, 2, 4 ),
 ( 2.304311362623472242E-07, 0.001064743401393353391, 0.001596999886521901450, 0.002129256371650449509 ),
 .UNSPECIFIED. ) ;
#3248=CARTESIAN_POINT ( 'NONE',  ( 3.020080181661098706, 3.262125172874016155, 8.342499971033864981 ) ) ;
#3258=CIRCLE ( 'NONE', #18727, 10.99999999999999822 ) ;
#3264=AXIS2_PLACEMENT_3D ( 'NONE', #2109, #9800, #9298 ) ;
#3265=CIRCLE ( 'NONE', #5913, 4.000000000000001776 ) ;
#3275=VERTEX_POINT ( 'NONE', #23272 ) ;
#3276=ORIENTED_EDGE ( 'NONE', *, *, #31346, .F. ) ;
#3297=VECTOR ( 'NONE', #16441, 1000.000000000000000 ) ;
#3301=FACE_OUTER_BOUND ( 'NONE', #9678, .T. ) ;
#3317=CARTESIAN_POINT ( 'NONE',  ( 2.274274201625327230, -1.464956435139465496, -10.90201369670500142 ) ) ;
#3328=CARTESIAN_POINT ( 'NONE',  ( 0.1574692421720930435, 7.165523657698311233, 7.841623826006798303 ) ) ;
#3345=LINE ( 'NONE', #23543, #29036 ) ;
#3348=EDGE_CURVE ( 'NONE', #5364, #12775, #22030, .T. ) ;
#3352=CARTESIAN_POINT ( 'NONE',  ( 2.357329994281668117, 2.053141773251463853, 10.64078702437730151 ) ) ;
#3370=ORIENTED_EDGE ( 'NONE', *, *, #5111, .F. ) ;
#3378=ORIENTED_EDGE ( 'NONE', *, *, #12056, .F. ) ;
#3392=AXIS2_PLACEMENT_3D ( 'NONE', #12466, #32881, #9949 ) ;
#3409=ORIENTED_EDGE ( 'NONE', *, *, #6084, .F. ) ;
#3416=CIRCLE ( 'NONE', #1286, 8.749000000000002331 ) ;
#3433=DIRECTION ( 'NONE',  ( 0.000000000000000000, 0.000000000000000000, 1.000000000000000000 ) ) ;
#3441=VERTEX_POINT ( 'NONE', #16842 ) ;
#3453=ADVANCED_FACE ( 'NONE', ( #6804 ), #22349, .F. ) ;
#3457=EDGE_LOOP ( 'NONE', ( #30596, #21004, #18198, #23573, #22052 ) ) ;
#3465=CARTESIAN_POINT ( 'NONE',  ( 3.249999999999999556, 0.000000000000000000, 0.000000000000000000 ) ) ;
#3479=DIRECTION ( 'NONE',  ( 0.000000000000000000, 0.000000000000000000, 1.000000000000000000 ) ) ;
#3483=VERTEX_POINT ( 'NONE', #125 ) ;
#3503=CARTESIAN_POINT ( 'NONE',  ( 0.3749740905863469531, 6.632019415960888509, 7.612528756000761732 ) ) ;
#3507=LINE ( 'NONE', #13662, #26692 ) ;
#3524=DIRECTION ( 'NONE',  ( -1.000000000000000000, -0.000000000000000000, 0.000000000000000000 ) ) ;
#3526=ORIENTED_EDGE ( 'NONE', *, *, #25048, .T. ) ;
#3533=ORIENTED_EDGE ( 'NONE', *, *, #27058, .T. ) ;
#3540=DIRECTION ( 'NONE',  ( 1.000000000000000000, 0.000000000000000000, 0.000000000000000000 ) ) ;
#3542=VERTEX_POINT ( 'NONE', #2629 ) ;
#3555=DIRECTION ( 'NONE',  ( -1.000000000000000000, -0.000000000000000000, -0.000000000000000000 ) ) ;
#3561=DIRECTION ( 'NONE',  ( -1.000000000000000000, 0.000000000000000000, -0.000000000000000000 ) ) ;
#3571=ORIENTED_EDGE ( 'NONE', *, *, #8596, .T. ) ;
#3573=DIRECTION ( 'NONE',  ( -1.000000000000000000, 0.000000000000000000, 0.000000000000000000 ) ) ;
#3583=CARTESIAN_POINT ( 'NONE',  ( 3.063284526839887167, 0.000000000000000000, 0.000000000000000000 ) ) ;
#3586=CARTESIAN_POINT ( 'NONE',  ( 0.000000000000000000, 8.264486777890107660, 4.472189673936814991 ) ) ;
#3600=ORIENTED_EDGE ( 'NONE', *, *, #17718, .F. ) ;
#3607=ORIENTED_EDGE ( 'NONE', *, *, #32615, .T. ) ;
#3615=CARTESIAN_POINT ( 'NONE',  ( -3.449949199999996274, 0.000000000000000000, -6.000000000000000888 ) ) ;
#3622=CARTESIAN_POINT ( 'NONE',  ( -1.361091220733346370E-15, -7.944914065997057406, -7.533794289458144000 ) ) ;
#3634=ORIENTED_EDGE ( 'NONE', *, *, #24801, .F. ) ;
#3647=CARTESIAN_POINT ( 'NONE',  ( 0.08034255810681192878, 7.347818361010405752, 7.899847910286047714 ) ) ;
#3649=CARTESIAN_POINT ( 'NONE',  ( 2.976845824368060445, -4.933977349953521774, -7.725179967474431919 ) ) ;
#3650=ADVANCED_FACE ( 'NONE', ( #13459 ), #8610, .F. ) ;
#3652=VERTEX_POINT ( 'NONE', #13628 ) ;
#3655=CARTESIAN_POINT ( 'NONE',  ( 0.7632845268398871230, 0.000000000000000000, 0.000000000000000000 ) ) ;
#3661=DIRECTION ( 'NONE',  ( 0.000000000000000000, 0.000000000000000000, 1.000000000000000000 ) ) ;
#3668=CARTESIAN_POINT ( 'NONE',  ( 0.7632845268398871230, 7.360373001730917686, 4.729683950898899703 ) ) ;
#3670=DIRECTION ( 'NONE',  ( 0.000000000000000000, 0.000000000000000000, 1.000000000000000000 ) ) ;
#3672=ORIENTED_EDGE ( 'NONE', *, *, #30420, .F. ) ;
#3692=DIRECTION ( 'NONE',  ( -1.000000000000000000, 0.000000000000000000, -0.000000000000000000 ) ) ;
#3693=CARTESIAN_POINT ( 'NONE',  ( 0.7632845268398888994, -6.772677083992417302, 5.538577986808867593 ) ) ;
#3694=CARTESIAN_POINT ( 'NONE',  ( 2.661997781067675817, -3.981025027156562590, 9.315861390595092217 ) ) ;
#3700=CARTESIAN_POINT ( 'NONE',  ( 0.08034255810714203971, -7.347818361009576194, -7.899847910285872743 ) ) ;
#3702=EDGE_CURVE ( 'NONE', #30241, #17653, #25895, .T. ) ;
#3707=DIRECTION ( 'NONE',  ( 0.000000000000000000, 0.000000000000000000, -1.000000000000000000 ) ) ;
#3718=VERTEX_POINT ( 'NONE', #32850 ) ;
#3720=EDGE_CURVE ( 'NONE', #2084, #25735, #5358, .T. ) ;
#3726=B_SPLINE_CURVE_WITH_KNOTS ( 'NONE', 3,
 ( #3153, #18175, #28383, #30762, #23364, #3010, #13311, #7833 ),
 .UNSPECIFIED., .F., .F.,
 ( 4, 2, 2, 4 ),
 ( 5.099451029799059509E-07, 0.001229189756374614957, 0.001843529662010432151, 0.002457869567646249562 ),
 .UNSPECIFIED. ) ;
#3730=CIRCLE ( 'NONE', #20815, 8.749000000000002331 ) ;
#3732=CARTESIAN_POINT ( 'NONE',  ( 2.976845773540292228, 3.349682859779612443, -8.532418605434688885 ) ) ;
#3754=ORIENTED_EDGE ( 'NONE', *, *, #21592, .F. ) ;
#3755=ORIENTED_EDGE ( 'NONE', *, *, #17169, .T. ) ;
#3764=CARTESIAN_POINT ( 'NONE',  ( 2.274274201625327230, 4.762163868918412923, -9.915734732513168836 ) ) ;
#3779=CIRCLE ( 'NONE', #12305, 4.000000000000001776 ) ;
#3782=VERTEX_POINT ( 'NONE', #11068 ) ;
#3785=DIRECTION ( 'NONE',  ( -1.000000000000000000, 0.000000000000000000, 0.000000000000000000 ) ) ;
#3809=EDGE_CURVE ( 'NONE', #28731, #689, #8568, .T. ) ;
#3820=ORIENTED_EDGE ( 'NONE', *, *, #24763, .T. ) ;
#3884=CIRCLE ( 'NONE', #20975, 8.749000000000002331 ) ;
#3890=ORIENTED_EDGE ( 'NONE', *, *, #18641, .T. ) ;
#3891=CARTESIAN_POINT ( 'NONE',  ( 0.000000000000000000, 9.884132761439062165, 4.709950686174647849 ) ) ;
#3894=ORIENTED_EDGE ( 'NONE', *, *, #9492, .F. ) ;
#3899=CIRCLE ( 'NONE', #17777, 4.000000000000001776 ) ;
#3904=EDGE_CURVE ( 'NONE', #27107, #5903, #18192, .T. ) ;
#3913=DIRECTION ( 'NONE',  ( 0.000000000000000000, 0.000000000000000000, -1.000000000000000000 ) ) ;
#3914=CARTESIAN_POINT ( 'NONE',  ( 3.249999999999999556, -7.360373001730951437, 4.729683950898845524 ) ) ;
#3916=CARTESIAN_POINT ( 'NONE',  ( 0.000000000000000000, 9.314797388894893615, 1.239665997526919972 ) ) ;
#3917=CARTESIAN_POINT ( 'NONE',  ( 0.7632845268398871230, -5.538577986808947529, 6.772677083992368452 ) ) ;
#3925=AXIS2_PLACEMENT_3D ( 'NONE', #9934, #20149, #30012 ) ;
#3932=AXIS2_PLACEMENT_3D ( 'NONE', #20891, #31109, #16204 ) ;
#3939=ORIENTED_EDGE ( 'NONE', *, *, #9360, .F. ) ;
#3944=CARTESIAN_POINT ( 'NONE',  ( 0.5704035945089810378, 2.319683995708331725, -9.255216539914508544 ) ) ;
#3958=DIRECTION ( 'NONE',  ( 1.000000000000000000, -0.000000000000000000, -0.000000000000000000 ) ) ;
#3959=CARTESIAN_POINT ( 'NONE',  ( -3.671580638170519912E-13, 9.620177616658855513, 5.227991826304058343 ) ) ;
#3972=CARTESIAN_POINT ( 'NONE',  ( 0.7632845268398882332, -4.729683950898921019, 7.360373001730893705 ) ) ;
#3978=VERTEX_POINT ( 'NONE', #29278 ) ;
#3998=CARTESIAN_POINT ( 'NONE',  ( 0.7212197595562506169, 8.936767016196059288, 0.5238431420062442667 ) ) ;
#4008=CARTESIAN_POINT ( 'NONE',  ( 0.5032040568799869273, -5.109302080992267570, -8.283195248923467702 ) ) ;
#4013=ORIENTED_EDGE ( 'NONE', *, *, #11774, .T. ) ;
#4029=CARTESIAN_POINT ( 'NONE',  ( 2.274274201625309910, -10.90201369670500853, -1.464956435139685098 ) ) ;
#4033=VERTEX_POINT ( 'NONE', #6364 ) ;
#4040=FACE_OUTER_BOUND ( 'NONE', #954, .T. ) ;
#4041=EDGE_CURVE ( 'NONE', #32002, #4375, #5389, .T. ) ;
#4048=ADVANCED_FACE ( 'NONE', ( #4553 ), #29449, .F. ) ;
#4053=DIRECTION ( 'NONE',  ( 1.000000000000000000, -0.000000000000000000, -0.000000000000000000 ) ) ;
#4064=ORIENTED_EDGE ( 'NONE', *, *, #11126, .F. ) ;
#4082=ORIENTED_EDGE ( 'NONE', *, *, #32280, .T. ) ;
#4083=CARTESIAN_POINT ( 'NONE',  ( 2.589202944057205968, -6.846250362091585551, 7.715757980413542327 ) ) ;
#4086=EDGE_LOOP ( 'NONE', ( #19106, #17914, #27843, #25051, #22770 ) ) ;
#4099=DIRECTION ( 'NONE',  ( -1.000000000000000000, -0.000000000000000000, -0.000000000000000000 ) ) ;
#4135=CARTESIAN_POINT ( 'NONE',  ( 0.7632845268398871230, -7.360373001730951437, 4.729683950898845524 ) ) ;
#4137=CARTESIAN_POINT ( 'NONE',  ( 2.437082530871043762, -5.244446742619423674, -9.289394354155845690 ) ) ;
#4144=CARTESIAN_POINT ( 'NONE',  ( 2.274274201620947622, 4.762163868927166810, 9.915734732518528105 ) ) ;
#4145=CARTESIAN_POINT ( 'NONE',  ( 3.063284526843245370, -8.152713396074034335, 3.174628368989241611 ) ) ;
#4153=ADVANCED_FACE ( 'NONE', ( #32809 ), #32317, .T. ) ;
#4162=VERTEX_POINT ( 'NONE', #22755 ) ;
#4167=ORIENTED_EDGE ( 'NONE', *, *, #32280, .F. ) ;
#4168=EDGE_LOOP ( 'NONE', ( #11446, #28406 ) ) ;
#4169=CARTESIAN_POINT ( 'NONE',  ( 3.020080146450413228, 8.942241244976921521, -0.5244911560323413102 ) ) ;
#4178=VERTEX_POINT ( 'NONE', #17726 ) ;
#4181=DIRECTION ( 'NONE',  ( 1.000000000000000000, -0.000000000000000000, -0.000000000000000000 ) ) ;
#4186=ADVANCED_FACE ( 'NONE', ( #4374 ), #19269, .T. ) ;
#4187=CARTESIAN_POINT ( 'NONE',  ( 3.063284526843251587, -3.174628368989204308, -8.152713396074016572 ) ) ;
#4195=CARTESIAN_POINT ( 'NONE',  ( -7.000050800000000351, 0.000000000000000000, -6.000000000000000888 ) ) ;
#4196=DIRECTION ( 'NONE',  ( -1.000000000000000000, 0.000000000000000000, 0.000000000000000000 ) ) ;
#4197=DIRECTION ( 'NONE',  ( 1.000000000000000000, -0.000000000000000000, -0.000000000000000000 ) ) ;
#4216=ADVANCED_FACE ( 'NONE', ( #24921 ), #6861, .T. ) ;
#4219=EDGE_CURVE ( 'NONE', #16746, #19457, #19742, .T. ) ;
#4222=ORIENTED_EDGE ( 'NONE', *, *, #29987, .F. ) ;
#4238=CARTESIAN_POINT ( 'NONE',  ( 2.592584839945471842, -5.238191131136688661, 8.898511132913965227 ) ) ;
#4240=EDGE_CURVE ( 'NONE', #29734, #12461, #18299, .T. ) ;
#4243=AXIS2_PLACEMENT_3D ( 'NONE', #10289, #28024, #23475 ) ;
#4251=CARTESIAN_POINT ( 'NONE',  ( 2.857987896741710276, 2.305585824582336407, -9.278099925253918911 ) ) ;
#4258=DIRECTION ( 'NONE',  ( 0.000000000000000000, 0.000000000000000000, 1.000000000000000000 ) ) ;
#4277=EDGE_CURVE ( 'NONE', #30410, #32250, #10192, .T. ) ;
#4278=B_SPLINE_CURVE_WITH_KNOTS ( 'NONE', 3,
 ( #23321, #23804, #11096, #21294, #28997, #6098, #16278, #26491 ),
 .UNSPECIFIED., .F., .F.,
 ( 4, 2, 2, 4 ),
 ( 2.024520226828571228E-07, 0.001261135997420231077, 0.001891602770119004849, 0.002522069542817778620 ),
 .UNSPECIFIED. ) ;
#4279=VERTEX_POINT ( 'NONE', #5691 ) ;
#4282=CARTESIAN_POINT ( 'NONE',  ( 3.249999999999999556, 4.729683950898872169, 7.360373001730934561 ) ) ;
#4311=CARTESIAN_POINT ( 'NONE',  ( 3.063284526846072442, -8.461683424479964799, -2.223716399039827429 ) ) ;
#4316=ORIENTED_EDGE ( 'NONE', *, *, #32615, .F. ) ;
#4327=CIRCLE ( 'NONE', #13370, 10.99999999999999822 ) ;
#4329=ORIENTED_EDGE ( 'NONE', *, *, #32340, .F. ) ;
#4343=DIRECTION ( 'NONE',  ( -1.000000000000000000, 0.000000000000000000, 0.000000000000000000 ) ) ;
#4349=CARTESIAN_POINT ( 'NONE',  ( -5.749676575031998027, 0.000000000000000000, 0.000000000000000000 ) ) ;
#4351=ORIENTED_EDGE ( 'NONE', *, *, #9757, .F. ) ;
#4357=AXIS2_PLACEMENT_3D ( 'NONE', #11728, #23792, #24282 ) ;
#4359=CIRCLE ( 'NONE', #8096, 8.749000000000002331 ) ;
#4368=ORIENTED_EDGE ( 'NONE', *, *, #11514, .T. ) ;
#4374=FACE_OUTER_BOUND ( 'NONE', #20381, .T. ) ;
#4375=VERTEX_POINT ( 'NONE', #13833 ) ;
#4376=CIRCLE ( 'NONE', #19337, 10.94895958125474245 ) ;
#4380=ORIENTED_EDGE ( 'NONE', *, *, #28017, .F. ) ;
#4384=ORIENTED_EDGE ( 'NONE', *, *, #7055, .T. ) ;
#4386=CARTESIAN_POINT ( 'NONE',  ( 2.898814881667754584, -7.987392794009419816, 5.028251054972114886 ) ) ;
#4388=CIRCLE ( 'NONE', #21467, 4.000000000000001776 ) ;
#4390=AXIS2_PLACEMENT_3D ( 'NONE', #475, #643, #17877 ) ;
#4422=ORIENTED_EDGE ( 'NONE', *, *, #33077, .F. ) ;
#4449=LINE ( 'NONE', #1943, #6629 ) ;
#4450=CARTESIAN_POINT ( 'NONE',  ( 3.008223337240918838, 8.722904517541643088, 2.275671791456698845 ) ) ;
#4453=CARTESIAN_POINT ( 'NONE',  ( 3.249999999999999556, 3.174628368996075256, 8.152713396088774545 ) ) ;
#4476=EDGE_CURVE ( 'NONE', #3441, #1994, #24673, .T. ) ;
#4493=CARTESIAN_POINT ( 'NONE',  ( 0.7632845268430009655, 4.729683950891516275, 7.360373001717795738 ) ) ;
#4502=ORIENTED_EDGE ( 'NONE', *, *, #32372, .T. ) ;
#4508=FACE_OUTER_BOUND ( 'NONE', #5786, .T. ) ;
#4516=DIRECTION ( 'NONE',  ( 1.000000000000000000, -0.000000000000000000, -0.000000000000000000 ) ) ;
#4521=CARTESIAN_POINT ( 'NONE',  ( 3.063284526839887167, 8.734705317681626724, -0.4999240074894737984 ) ) ;
#4529=CARTESIAN_POINT ( 'NONE',  ( 3.063284526839887167, -8.734705317681623171, -0.4999240074895356933 ) ) ;
#4534=EDGE_CURVE ( 'NONE', #22777, #3718, #2326, .T. ) ;
#4541=DIRECTION ( 'NONE',  ( -1.000000000000000000, 0.000000000000000000, 0.000000000000000000 ) ) ;
#4553=FACE_OUTER_BOUND ( 'NONE', #22215, .T. ) ;
#4555=DIRECTION ( 'NONE',  ( 1.000000000000000000, -0.000000000000000000, -0.000000000000000000 ) ) ;
#4557=ORIENTED_EDGE ( 'NONE', *, *, #8931, .F. ) ;
#4568=ORIENTED_EDGE ( 'NONE', *, *, #25358, .T. ) ;
#4570=CARTESIAN_POINT ( 'NONE',  ( 2.589202905186824388, -9.453729690310135325, -4.126870756446575861 ) ) ;
#4574=DIRECTION ( 'NONE',  ( -1.000000000000000000, 0.000000000000000000, 0.000000000000000000 ) ) ;
#4581=VERTEX_POINT ( 'NONE', #15461 ) ;
#4586=EDGE_LOOP ( 'NONE', ( #33037, #14307, #27680, #25195 ) ) ;
#4599=CARTESIAN_POINT ( 'NONE',  ( 2.274274201627632941, 1.975651141464536797, -10.82112760146234720 ) ) ;
#4602=CARTESIAN_POINT ( 'NONE',  ( 0.7632845268449801601, 2.223716399040764014, 8.461683424485153537 ) ) ;
#4615=EDGE_CURVE ( 'NONE', #2199, #10723, #933, .T. ) ;
#4619=VERTEX_POINT ( 'NONE', #13615 ) ;
#4626=CARTESIAN_POINT ( 'NONE',  ( 0.5664946525207626982, 9.241976615239526183, 2.300561732649596181 ) ) ;
#4630=DIRECTION ( 'NONE',  ( 0.000000000000000000, 0.000000000000000000, 1.000000000000000000 ) ) ;
#4640=CARTESIAN_POINT ( 'NONE',  ( 0.1606232843943643518, 1.177222770082358316, -10.56438947504860337 ) ) ;
#4644=DIRECTION ( 'NONE',  ( -1.000000000000000000, 0.000000000000000000, 0.000000000000000000 ) ) ;
#4659=ORIENTED_EDGE ( 'NONE', *, *, #17436, .F. ) ;
#4662=EDGE_CURVE ( 'NONE', #14763, #12234, #23967, .T. ) ;
#4679=EDGE_CURVE ( 'NONE', #14707, #25174, #6112, .T. ) ;
#4696=DIRECTION ( 'NONE',  ( -1.000000000000000000, -0.000000000000000000, 0.000000000000000000 ) ) ;
#4719=DIRECTION ( 'NONE',  ( 1.000000000000000000, 0.000000000000000000, 0.000000000000000000 ) ) ;
#4725=DIRECTION ( 'NONE',  ( 0.000000000000000000, 0.000000000000000000, 1.000000000000000000 ) ) ;
#4739=CARTESIAN_POINT ( 'NONE',  ( 0.000000000000000000, -9.915734732513254102, 4.762163868918234400 ) ) ;
#4749=FACE_OUTER_BOUND ( 'NONE', #23268, .T. ) ;
#4750=VERTEX_POINT ( 'NONE', #2583 ) ;
#4754=DIRECTION ( 'NONE',  ( -1.000000000000000000, 0.000000000000000000, 0.000000000000000000 ) ) ;
#4757=EDGE_CURVE ( 'NONE', #31656, #6932, #7021, .T. ) ;
#4771=DIRECTION ( 'NONE',  ( 0.000000000000000000, -7.993605777301127091E-15, 1.000000000000000000 ) ) ;
#4773=ORIENTED_EDGE ( 'NONE', *, *, #4679, .F. ) ;
#4783=ORIENTED_EDGE ( 'NONE', *, *, #32746, .T. ) ;
#4784=AXIS2_PLACEMENT_3D ( 'NONE', #3465, #6418, #1090 ) ;
#4791=CARTESIAN_POINT ( 'NONE',  ( 1.624999999999999778, 10.90201369670498721, 1.464956435139580515 ) ) ;
#4792=ADVANCED_FACE ( 'NONE', ( #4749 ), #17601, .T. ) ;
#4799=CARTESIAN_POINT ( 'NONE',  ( 0.3076688720830444423, -0.9727984658975878940, 10.24120291391358251 ) ) ;
#4801=UNCERTAINTY_MEASURE_WITH_UNIT (LENGTH_MEASURE( 1.000000000000000082E-05 ), #20670, 'distance_accuracy_value', 'NONE');
#4803=AXIS2_PLACEMENT_3D ( 'NONE', #27803, #9924, #25316 ) ;
#4812=DIRECTION ( 'NONE',  ( -1.000000000000000000, 0.000000000000000000, 0.000000000000000000 ) ) ;
#4819=CIRCLE ( 'NONE', #25097, 10.94895958125474245 ) ;
#4820=EDGE_CURVE ( 'NONE', #22329, #7687, #21957, .T. ) ;
#4822=CARTESIAN_POINT ( 'NONE',  ( 0.5704035945090664139, -9.255216539914215446, -2.319683995708284652 ) ) ;
#4823=DIRECTION ( 'NONE',  ( -1.000000000000000000, 0.000000000000000000, 0.000000000000000000 ) ) ;
#4824=B_SPLINE_CURVE_WITH_KNOTS ( 'NONE', 3,
 ( #25922, #15365, #28590, #25571, #18051, #492, #3352, #23548 ),
 .UNSPECIFIED., .F., .F.,
 ( 4, 2, 2, 4 ),
 ( 2.049880227661072699E-07, 0.001261138121172437291, 0.001891604687747272832, 0.002522071254322108373 ),
 .UNSPECIFIED. ) ;
#4826=LINE ( 'NONE', #14841, #731 ) ;
#4842=FACE_OUTER_BOUND ( 'NONE', #22849, .T. ) ;
#4849=FACE_OUTER_BOUND ( 'NONE', #24306, .T. ) ;
#4850=AXIS2_PLACEMENT_3D ( 'NONE', #6559, #11724, #24778 ) ;
#4860=ORIENTED_EDGE ( 'NONE', *, *, #11126, .T. ) ;
#4867=ORIENTED_EDGE ( 'NONE', *, *, #178, .T. ) ;
#4877=CARTESIAN_POINT ( 'NONE',  ( 0.7212197917577920503, 4.829101774917357481, 7.537903528354168436 ) ) ;
#4884=CARTESIAN_POINT ( 'NONE',  ( 2.274274201625327230, 0.000000000000000000, 0.000000000000000000 ) ) ;
#4885=ORIENTED_EDGE ( 'NONE', *, *, #11774, .F. ) ;
#4890=CYLINDRICAL_SURFACE ( 'NONE', #4952, 4.000000000000001776 ) ;
#4901=AXIS2_PLACEMENT_3D ( 'NONE', #4935, #27504, #32694 ) ;
#4903=AXIS2_PLACEMENT_3D ( 'NONE', #31334, #28980, #16266 ) ;
#4904=DIRECTION ( 'NONE',  ( 1.000000000000000000, 0.000000000000000000, 0.000000000000000000 ) ) ;
#4911=ORIENTED_EDGE ( 'NONE', *, *, #18960, .T. ) ;
#4920=DIRECTION ( 'NONE',  ( 0.000000000000000000, 0.000000000000000000, 1.000000000000000000 ) ) ;
#4925=LINE ( 'NONE', #23148, #28853 ) ;
#4932=AXIS2_PLACEMENT_3D ( 'NONE', #21106, #20614, #17755 ) ;
#4933=TOROIDAL_SURFACE ( 'NONE', #25739, 6.923700951379999857, 9.000000000000001776 ) ;
#4935=CARTESIAN_POINT ( 'NONE',  ( 3.249999999999999556, 4.472189673936902032, -8.264486777890061475 ) ) ;
#4948=CIRCLE ( 'NONE', #30062, 8.749000000000002331 ) ;
#4952=AXIS2_PLACEMENT_3D ( 'NONE', #17759, #236, #10717 ) ;
#4953=ORIENTED_EDGE ( 'NONE', *, *, #26490, .F. ) ;
#4955=CARTESIAN_POINT ( 'NONE',  ( 3.063284526839890720, 6.772677083992379110, 5.538577986808916442 ) ) ;
#4968=CYLINDRICAL_SURFACE ( 'NONE', #32610, 4.000000000000001776 ) ;
#4969=CARTESIAN_POINT ( 'NONE',  ( 0.6728001045953906356, -8.512517952473988458, -3.357496170320755091 ) ) ;
#4976=ORIENTED_EDGE ( 'NONE', *, *, #12245, .T. ) ;
#4982=CIRCLE ( 'NONE', #28463, 4.000000000000001776 ) ;
#4985=VECTOR ( 'NONE', #10184, 1000.000000000000000 ) ;
#4987=CARTESIAN_POINT ( 'NONE',  ( 0.000000000000000000, 0.000000000000000000, 0.000000000000000000 ) ) ;
#4992=ORIENTED_EDGE ( 'NONE', *, *, #26574, .F. ) ;
#4997=DIRECTION ( 'NONE',  ( -1.000000000000000000, 0.000000000000000000, -0.000000000000000000 ) ) ;
#5005=DIRECTION ( 'NONE',  ( -1.000000000000000000, 0.000000000000000000, 0.000000000000000000 ) ) ;
#5013=DIRECTION ( 'NONE',  ( 0.000000000000000000, 0.000000000000000000, 1.000000000000000000 ) ) ;
#5014=CARTESIAN_POINT ( 'NONE',  ( 0.6791197550704926034, -8.860977624947322440, -2.303133748654038193 ) ) ;
#5019=FACE_OUTER_BOUND ( 'NONE', #9252, .T. ) ;
#5028=ORIENTED_EDGE ( 'NONE', *, *, #24682, .F. ) ;
#5030=ORIENTED_EDGE ( 'NONE', *, *, #20956, .T. ) ;
#5033=CARTESIAN_POINT ( 'NONE',  ( 0.3749742512055983523, 5.190538276686016417, -8.659825570211875601 ) ) ;
#5034=AXIS2_PLACEMENT_3D ( 'NONE', #9061, #22291, #19778 ) ;
#5038=ADVANCED_FACE ( 'NONE', ( #31473 ), #23932, .T. ) ;
#5043=ORIENTED_EDGE ( 'NONE', *, *, #10053, .F. ) ;
#5044=CARTESIAN_POINT ( 'NONE',  ( 0.1255855353732055757, -9.314797388894898944, 5.239665997526856245 ) ) ;
#5046=CARTESIAN_POINT ( 'NONE',  ( -18.30155664144426453, 0.000000000000000000, 0.000000000000000000 ) ) ;
#5060=DIRECTION ( 'NONE',  ( 0.000000000000000000, -0.5877852522924804646, 0.8090169943749422332 ) ) ;
#5061=CYLINDRICAL_SURFACE ( 'NONE', #18724, 3.499999999999999556 ) ;
#5067=CARTESIAN_POINT ( 'NONE',  ( 2.274274201625327230, -9.915734732513254102, 4.762163868918234400 ) ) ;
#5081=DIRECTION ( 'NONE',  ( 0.000000000000000000, 0.000000000000000000, 1.000000000000000000 ) ) ;
#5084=EDGE_LOOP ( 'NONE', ( #24274, #24959, #5640, #12656 ) ) ;
#5087=ORIENTED_EDGE ( 'NONE', *, *, #29999, .T. ) ;
#5095=EDGE_CURVE ( 'NONE', #14743, #29348, #30105, .T. ) ;
#5101=DIRECTION ( 'NONE',  ( 0.000000000000000000, 0.000000000000000000, -1.000000000000000000 ) ) ;
#5103=CARTESIAN_POINT ( 'NONE',  ( 4.888486331236938389E-17, -10.76487093102066517, 1.999317321091457655 ) ) ;
#5106=CARTESIAN_POINT ( 'NONE',  ( 0.5704039292222269353, 7.316743080999716931, -6.124150562935458453 ) ) ;
#5108=DIRECTION ( 'NONE',  ( 0.000000000000000000, 0.000000000000000000, 1.000000000000000000 ) ) ;
#5111=EDGE_CURVE ( 'NONE', #14007, #17751, #29285, .T. ) ;
#5114=DIRECTION ( 'NONE',  ( 1.000000000000000000, 0.000000000000000000, 0.000000000000000000 ) ) ;
#5127=ORIENTED_EDGE ( 'NONE', *, *, #16827, .F. ) ;
#5128=EDGE_LOOP ( 'NONE', ( #29622, #11412, #25999, #26651 ) ) ;
#5149=VERTEX_POINT ( 'NONE', #19889 ) ;
#5153=EDGE_LOOP ( 'NONE', ( #17784, #28964, #21202, #17131, #11812 ) ) ;
#5166=CYLINDRICAL_SURFACE ( 'NONE', #3236, 11.00000000000000000 ) ;
#5171=CYLINDRICAL_SURFACE ( 'NONE', #11261, 4.000000000000001776 ) ;
#5178=LINE ( 'NONE', #25561, #7598 ) ;
#5182=ORIENTED_EDGE ( 'NONE', *, *, #24672, .F. ) ;
#5191=B_SPLINE_CURVE_WITH_KNOTS ( 'NONE', 3,
 ( #6701, #16889, #27087, #23767, #18740, #13714, #1026, #21417 ),
 .UNSPECIFIED., .F., .F.,
 ( 4, 2, 2, 4 ),
 ( 2.333100269151217215E-07, 0.001262083418509045343, 0.001893008472750110603, 0.002523933526991176297 ),
 .UNSPECIFIED. ) ;
#5220=DIRECTION ( 'NONE',  ( -1.000000000000000000, 0.000000000000000000, 0.000000000000000000 ) ) ;
#5222=CARTESIAN_POINT ( 'NONE',  ( 2.866494652514124830, 9.241976615262203154, 2.300561732649596181 ) ) ;
#5233=DIRECTION ( 'NONE',  ( 1.000000000000000000, 0.000000000000000000, 0.000000000000000000 ) ) ;
#5238=DIRECTION ( 'NONE',  ( -1.000000000000000000, 0.000000000000000000, 0.000000000000000000 ) ) ;
#5253=B_SPLINE_CURVE_WITH_KNOTS ( 'NONE', 3,
 ( #15717, #843, #21220, #17898, #23387, #23070, #31105, #31418 ),
 .UNSPECIFIED., .F., .F.,
 ( 4, 2, 2, 4 ),
 ( 2.213836054330188222E-07, 0.001227982086136106352, 0.001841862437401445242, 0.002455742788666784131 ),
 .UNSPECIFIED. ) ;
#5254=DIRECTION ( 'NONE',  ( -1.000000000000000000, 0.000000000000000000, 0.000000000000000000 ) ) ;
#5258=EDGE_CURVE ( 'NONE', #16869, #18943, #1189, .T. ) ;
#5260=ADVANCED_FACE ( 'NONE', ( #30916 ), #5810, .T. ) ;
#5263=DIRECTION ( 'NONE',  ( 0.000000000000000000, 0.000000000000000000, -1.000000000000000000 ) ) ;
#5266=DIRECTION ( 'NONE',  ( -1.000000000000000000, 0.000000000000000000, 0.000000000000000000 ) ) ;
#5267=ADVANCED_FACE ( 'NONE', ( #25721, #7990 ), #23371, .T. ) ;
#5275=VERTEX_POINT ( 'NONE', #3158 ) ;
#5278=DIRECTION ( 'NONE',  ( 0.000000000000000000, 0.000000000000000000, -1.000000000000000000 ) ) ;
#5281=CYLINDRICAL_SURFACE ( 'NONE', #504, 4.000000000000001776 ) ;
#5287=CARTESIAN_POINT ( 'NONE',  ( 0.1606233060821306291, -9.683549581721070609, -4.384181225617457045 ) ) ;
#5323=CARTESIAN_POINT ( 'NONE',  ( 0.000000000000000000, -10.76487093102063319, -1.999317321091613753 ) ) ;
#5329=DIRECTION ( 'NONE',  ( -1.000000000000000000, -0.000000000000000000, 0.000000000000000000 ) ) ;
#5346=EDGE_CURVE ( 'NONE', #3542, #32298, #2804, .T. ) ;
#5355=CARTESIAN_POINT ( 'NONE',  ( 2.274274201625327230, 7.593217523260696211, -7.958834565716686349 ) ) ;
#5356=ORIENTED_EDGE ( 'NONE', *, *, #17554, .F. ) ;
#5357=ADVANCED_FACE ( 'NONE', ( #13799 ), #23587, .T. ) ;
#5358=CIRCLE ( 'NONE', #1636, 8.749000000000002331 ) ;
#5362=EDGE_CURVE ( 'NONE', #32789, #26634, #32674, .T. ) ;
#5364=VERTEX_POINT ( 'NONE', #26543 ) ;
#5378=DIRECTION ( 'NONE',  ( 0.000000000000000000, 0.000000000000000000, 1.000000000000000000 ) ) ;
#5385=CIRCLE ( 'NONE', #12826, 10.99999999999999822 ) ;
#5389=CIRCLE ( 'NONE', #6434, 8.749000000000002331 ) ;
#5408=EDGE_LOOP ( 'NONE', ( #24903, #28709, #22377, #1383 ) ) ;
#5409=CARTESIAN_POINT ( 'NONE',  ( 2.274274201625327230, 0.000000000000000000, 0.000000000000000000 ) ) ;
#5411=CYLINDRICAL_SURFACE ( 'NONE', #20846, 4.000000000000001776 ) ;
#5414=CARTESIAN_POINT ( 'NONE',  ( 0.7632845268398871230, 0.000000000000000000, 0.000000000000000000 ) ) ;
#5440=AXIS2_PLACEMENT_3D ( 'NONE', #18104, #10079, #32857 ) ;
#5464=CIRCLE ( 'NONE', #19346, 11.00000000000000000 ) ;
#5467=VECTOR ( 'NONE', #14067, 1000.000000000000000 ) ;
#5468=AXIS2_PLACEMENT_3D ( 'NONE', #10348, #8168, #15505 ) ;
#5472=CARTESIAN_POINT ( 'NONE',  ( 3.249999999999999556, 1.239665997527021002, -9.314797388894877628 ) ) ;
#5476=CARTESIAN_POINT ( 'NONE',  ( 0.1606232843927795639, -1.177222770084728420, 10.56438947505148462 ) ) ;
#5477=CARTESIAN_POINT ( 'NONE',  ( 0.7632845268398871230, 0.000000000000000000, 0.000000000000000000 ) ) ;
#5485=ORIENTED_EDGE ( 'NONE', *, *, #6821, .F. ) ;
#5487=CIRCLE ( 'NONE', #2286, 7.000000000000000888 ) ;
#5496=CARTESIAN_POINT ( 'NONE',  ( 2.274274201625327230, -5.222868219166924675, 9.680994141368751471 ) ) ;
#5500=CARTESIAN_POINT ( 'NONE',  ( 3.249999999999999556, 0.000000000000000000, 0.000000000000000000 ) ) ;
#5505=AXIS2_PLACEMENT_3D ( 'NONE', #26999, #1277, #24463 ) ;
#5507=CARTESIAN_POINT ( 'NONE',  ( -7.000050800000000351, 0.000000000000000000, 0.000000000000000000 ) ) ;
#5509=ORIENTED_EDGE ( 'NONE', *, *, #24743, .F. ) ;
#5512=CYLINDRICAL_SURFACE ( 'NONE', #20345, 4.000000000000001776 ) ;
#5517=CYLINDRICAL_SURFACE ( 'NONE', #5886, 4.000000000000001776 ) ;
#5534=ADVANCED_FACE ( 'NONE', ( #25179 ), #32553, .T. ) ;
#5551=ORIENTED_EDGE ( 'NONE', *, *, #28395, .F. ) ;
#5561=CARTESIAN_POINT ( 'NONE',  ( 3.249999999999999556, -6.478011392632841314, -6.807171995660652009 ) ) ;
#5605=CARTESIAN_POINT ( 'NONE',  ( 2.592584690691857485, 4.120115534666347834, 9.468199583002062880 ) ) ;
#5609=LINE ( 'NONE', #17969, #21975 ) ;
#5621=CARTESIAN_POINT ( 'NONE',  ( 3.249999999999999556, -8.734705317681630277, 0.4999240074894127361 ) ) ;
#5630=VERTEX_POINT ( 'NONE', #27855 ) ;
#5637=CLOSED_SHELL ( 'NONE', ( #3180, #4186, #13472, #2775, #15268, #6455, #28005, #4216, #25217, #14351, #2850, #28656, #16459, #31166, #30218, #9999, #10671, #24046, #2019, #7520, #30745, #15080, #16719, #31941, #17002, #29711, #28618, #12670, #5777, #3650, #2872, #7373, #3453, #2616, #790, #26572, #29192, #5038, #15690, #9585, #5534, #21526, #577, #20590, #21388, #14893, #13032, #30471, #8676, #22583, #28385, #976, #24336, #3233, #9997, #414, #16082, #26635, #32968, #27102, #16902, #9777, #16353, #23392, #13708, #18540, #32727, #13938, #19814, #15162, #8503, #6719, #1203, #11843, #23250, #2652, #26346, #5260, #10407, #17129, #19885, #224, #4153, #1857, #9338, #31907, #4792, #25475, #28266, #20231, #6307, #13053, #28159, #18965, #5807, #20065, #14346, #15062, #21522, #21735, #30863, #14239, #12459, #30092, #10712, #9455, #21562, #9727, #26906, #6478, #17088, #30227, #26005, #32485, #21631, #29819, #30722, #5267, #4048, #5357, #25717, #28867, #14419, #23671 ) ) ;
#5638=DIRECTION ( 'NONE',  ( 0.000000000000000000, 0.000000000000000000, -1.000000000000000000 ) ) ;
#5640=ORIENTED_EDGE ( 'NONE', *, *, #20703, .T. ) ;
#5642=FACE_OUTER_BOUND ( 'NONE', #3006, .T. ) ;
#5658=ORIENTED_EDGE ( 'NONE', *, *, #20956, .F. ) ;
#5668=CARTESIAN_POINT ( 'NONE',  ( 2.864531314636031389, -7.330015575757862223, -6.140839842381257796 ) ) ;
#5670=DIRECTION ( 'NONE',  ( -1.000000000000000000, -0.000000000000000000, -0.000000000000000000 ) ) ;
#5679=EDGE_CURVE ( 'NONE', #2042, #10135, #5385, .T. ) ;
#5681=CARTESIAN_POINT ( 'NONE',  ( 0.1606232872998192840, 2.144970499002737174, 10.41111328664649527 ) ) ;
#5688=CARTESIAN_POINT ( 'NONE',  ( 2.440333830125739567, -9.290196408096495162, -5.258796312403343443 ) ) ;
#5691=CARTESIAN_POINT ( 'NONE',  ( 0.000000000000000000, -7.944914065997164876, 7.533794289458026761 ) ) ;
#5700=EDGE_LOOP ( 'NONE', ( #8199, #3042, #17537, #6401 ) ) ;
#5705=CARTESIAN_POINT ( 'NONE',  ( 0.3045634274093889649, -5.217683548413573291, 8.853895822767199775 ) ) ;
#5744=VERTEX_POINT ( 'NONE', #12639 ) ;
#5751=CARTESIAN_POINT ( 'NONE',  ( 2.970200448035948959, 3.362738345043210675, 8.521880193026261097 ) ) ;
#5755=DIRECTION ( 'NONE',  ( 0.000000000000000000, 0.5877852522924743583, -0.8090169943749467851 ) ) ;
#5775=ORIENTED_EDGE ( 'NONE', *, *, #31346, .T. ) ;
#5776=DIRECTION ( 'NONE',  ( 1.000000000000000000, -0.000000000000000000, -0.000000000000000000 ) ) ;
#5777=ADVANCED_FACE ( 'NONE', ( #8125 ), #22997, .F. ) ;
#5778=VERTEX_POINT ( 'NONE', #10307 ) ;
#5786=EDGE_LOOP ( 'NONE', ( #18692, #15602, #15292, #31182, #29945 ) ) ;
#5807=ADVANCED_FACE ( 'NONE', ( #18002 ), #15468, .T. ) ;
#5810=CYLINDRICAL_SURFACE ( 'NONE', #4390, 4.000000000000001776 ) ;
#5815=DIRECTION ( 'NONE',  ( 0.000000000000000000, 0.000000000000000000, 1.000000000000000000 ) ) ;
#5822=CARTESIAN_POINT ( 'NONE',  ( 1.615481217893400349E-16, -4.709950686174685153, 9.884132761439042625 ) ) ;
#5830=ORIENTED_EDGE ( 'NONE', *, *, #21647, .F. ) ;
#5831=CARTESIAN_POINT ( 'NONE',  ( 0.7632845268398871230, 0.4999240074894433228, 8.734705317681628500 ) ) ;
#5842=DIRECTION ( 'NONE',  ( 1.000000000000000000, 0.000000000000000000, 0.000000000000000000 ) ) ;
#5845=DIRECTION ( 'NONE',  ( 1.000000000000000000, 0.000000000000000000, 0.000000000000000000 ) ) ;
#5851=EDGE_CURVE ( 'NONE', #20387, #22777, #19108, .T. ) ;
#5861=AXIS2_PLACEMENT_3D ( 'NONE', #9446, #9607, #31024 ) ;
#5867=DIRECTION ( 'NONE',  ( -0.000000000000000000, -1.000000000000000000, -0.000000000000000000 ) ) ;
#5869=AXIS2_PLACEMENT_3D ( 'NONE', #22809, #27652, #17609 ) ;
#5877=ORIENTED_EDGE ( 'NONE', *, *, #32540, .T. ) ;
#5881=DIRECTION ( 'NONE',  ( -1.000000000000000000, 0.000000000000000000, -0.000000000000000000 ) ) ;
#5886=AXIS2_PLACEMENT_3D ( 'NONE', #480, #31404, #5815 ) ;
#5903=VERTEX_POINT ( 'NONE', #3764 ) ;
#5905=CIRCLE ( 'NONE', #19805, 4.000000000000001776 ) ;
#5913=AXIS2_PLACEMENT_3D ( 'NONE', #22511, #16982, #15157 ) ;
#5917=VERTEX_POINT ( 'NONE', #26512 ) ;
#5937=AXIS2_PLACEMENT_3D ( 'NONE', #12358, #6846, #15023 ) ;
#5951=CARTESIAN_POINT ( 'NONE',  ( 3.250000000000000000, 0.000000000000000000, 0.000000000000000000 ) ) ;
#5958=AXIS2_PLACEMENT_3D ( 'NONE', #27472, #4574, #12728 ) ;
#5959=DIRECTION ( 'NONE',  ( 0.000000000000000000, 0.000000000000000000, 1.000000000000000000 ) ) ;
#5971=VECTOR ( 'NONE', #26093, 1000.000000000000000 ) ;
#5975=CARTESIAN_POINT ( 'NONE',  ( 2.589202797589355232, -1.003524335601107209, 10.26630467377260914 ) ) ;
#5979=EDGE_CURVE ( 'NONE', #16174, #7245, #21341, .T. ) ;
#6007=FACE_OUTER_BOUND ( 'NONE', #8856, .T. ) ;
#6032=DIRECTION ( 'NONE',  ( 0.000000000000000000, 0.000000000000000000, 1.000000000000000000 ) ) ;
#6039=VECTOR ( 'NONE', #19525, 1000.000000000000000 ) ;
#6059=LINE ( 'NONE', #889, #16630 ) ;
#6084=EDGE_CURVE ( 'NONE', #19227, #6218, #31091, .T. ) ;
#6085=B_SPLINE_CURVE_WITH_KNOTS ( 'NONE', 3,
 ( #14625, #25331, #10089, #15118 ),
 .UNSPECIFIED., .F., .F.,
 ( 4, 4 ),
 ( 5.099451029762119343E-07, 0.0003283404404905848075 ),
 .UNSPECIFIED. ) ;
#6086=B_SPLINE_CURVE_WITH_KNOTS ( 'NONE', 3,
 ( #7538, #16224, #8518, #21399, #5705, #23267, #6191, #18421 ),
 .UNSPECIFIED., .F., .F.,
 ( 4, 2, 2, 4 ),
 ( 2.304311362529957687E-07, 0.001227991214883143506, 0.001841871606756588899, 0.002455751998630034509 ),
 .UNSPECIFIED. ) ;
#6089=EDGE_CURVE ( 'NONE', #7759, #19976, #17453, .T. ) ;
#6092=DIRECTION ( 'NONE',  ( 0.000000000000000000, 0.000000000000000000, 1.000000000000000000 ) ) ;
#6093=CIRCLE ( 'NONE', #246, 8.749000000000002331 ) ;
#6095=CARTESIAN_POINT ( 'NONE',  ( -3.691545173129016004E-13, 1.425064293572904539, 10.85582367538961535 ) ) ;
#6098=CARTESIAN_POINT ( 'NONE',  ( 2.437082316315989594, 10.59788678609684176, 1.217322776604743639 ) ) ;
#6105=ORIENTED_EDGE ( 'NONE', *, *, #1570, .T. ) ;
#6112=LINE ( 'NONE', #16608, #3297 ) ;
#6113=ORIENTED_EDGE ( 'NONE', *, *, #26910, .F. ) ;
#6119=CARTESIAN_POINT ( 'NONE',  ( 0.6420652513406681638, 8.983930386558810710, 2.300561732648136015 ) ) ;
#6142=CARTESIAN_POINT ( 'NONE',  ( 0.000000000000000000, 0.000000000000000000, 0.000000000000000000 ) ) ;
#6151=DIRECTION ( 'NONE',  ( -1.000000000000000000, 0.000000000000000000, 0.000000000000000000 ) ) ;
#6157=ORIENTED_EDGE ( 'NONE', *, *, #28789, .F. ) ;
#6163=CARTESIAN_POINT ( 'NONE',  ( 0.5032040285305349192, -3.698073368203369515, 9.002252291025278907 ) ) ;
#6166=DIRECTION ( 'NONE',  ( -1.000000000000000000, -0.000000000000000000, 0.000000000000000000 ) ) ;
#6184=ORIENTED_EDGE ( 'NONE', *, *, #28994, .F. ) ;
#6190=DIRECTION ( 'NONE',  ( 0.000000000000000000, 0.000000000000000000, -1.000000000000000000 ) ) ;
#6191=CARTESIAN_POINT ( 'NONE',  ( 0.08034253656914167041, -5.242601083769347525, 9.429377841196169285 ) ) ;
#6194=CYLINDRICAL_SURFACE ( 'NONE', #25112, 8.749000000000002331 ) ;
#6204=CARTESIAN_POINT ( 'NONE',  ( 0.000000000000000000, -9.915734732513184824, -4.762163868918376508 ) ) ;
#6218=VERTEX_POINT ( 'NONE', #8892 ) ;
#6233=CARTESIAN_POINT ( 'NONE',  ( 2.357329973329943762, 4.593471141847181194, -9.815384016743262663 ) ) ;
#6250=ORIENTED_EDGE ( 'NONE', *, *, #17613, .T. ) ;
#6261=VERTEX_POINT ( 'NONE', #31659 ) ;
#6272=CARTESIAN_POINT ( 'NONE',  ( 1.624999999999999778, 9.915734732513218574, 4.762163868918307230 ) ) ;
#6273=DIRECTION ( 'NONE',  ( 0.000000000000000000, 0.000000000000000000, 1.000000000000000000 ) ) ;
#6279=ORIENTED_EDGE ( 'NONE', *, *, #21148, .T. ) ;
#6297=CARTESIAN_POINT ( 'NONE',  ( 2.357330042320760821, 5.240837896778964833, 9.485534025193812724 ) ) ;
#6303=B_SPLINE_CURVE_WITH_KNOTS ( 'NONE', 3,
 ( #28877, #10840, #29212, #8332, #13660, #21353, #971, #26547 ),
 .UNSPECIFIED., .F., .F.,
 ( 4, 2, 2, 4 ),
 ( 2.024520226885745157E-07, 0.001227962984611326042, 0.001841843250905642743, 0.002455723517199959443 ),
 .UNSPECIFIED. ) ;
#6304=FACE_OUTER_BOUND ( 'NONE', #32273, .T. ) ;
#6305=CARTESIAN_POINT ( 'NONE',  ( 2.864530965498449433, -2.320611941139863355, -9.276519854389901454 ) ) ;
#6307=ADVANCED_FACE ( 'NONE', ( #14887 ), #19756, .T. ) ;
#6314=VERTEX_POINT ( 'NONE', #7052 ) ;
#6318=CARTESIAN_POINT ( 'NONE',  ( 0.000000000000000000, 1.239665997527021002, -9.314797388894877628 ) ) ;
#6327=EDGE_CURVE ( 'NONE', #23697, #11749, #6563, .T. ) ;
#6336=CARTESIAN_POINT ( 'NONE',  ( 3.063284526845908129, -0.4999240074859571670, -8.734705317652709411 ) ) ;
#6337=DIRECTION ( 'NONE',  ( -1.000000000000000000, -0.000000000000000000, -0.000000000000000000 ) ) ;
#6352=CARTESIAN_POINT ( 'NONE',  ( 0.7632845268398873451, -5.538577986808840059, -6.772677083992440394 ) ) ;
#6356=EDGE_CURVE ( 'NONE', #22691, #25765, #3198, .T. ) ;
#6362=ORIENTED_EDGE ( 'NONE', *, *, #9891, .F. ) ;
#6364=CARTESIAN_POINT ( 'NONE',  ( 3.063284526839887167, -7.360373001730951437, 4.729683950898845524 ) ) ;
#6380=ORIENTED_EDGE ( 'NONE', *, *, #31638, .F. ) ;
#6387=CARTESIAN_POINT ( 'NONE',  ( -1.348815490713419493E-16, -7.533794289458111137, 7.944914065997086716 ) ) ;
#6390=DIRECTION ( 'NONE',  ( 0.000000000000000000, 0.000000000000000000, -1.000000000000000000 ) ) ;
#6401=ORIENTED_EDGE ( 'NONE', *, *, #11590, .T. ) ;
#6404=ORIENTED_EDGE ( 'NONE', *, *, #16688, .T. ) ;
#6410=DIRECTION ( 'NONE',  ( -1.000000000000000000, 0.000000000000000000, -0.000000000000000000 ) ) ;
#6418=DIRECTION ( 'NONE',  ( -1.000000000000000000, 0.000000000000000000, 0.000000000000000000 ) ) ;
#6426=AXIS2_PLACEMENT_3D ( 'NONE', #11986, #11800, #6790 ) ;
#6434=AXIS2_PLACEMENT_3D ( 'NONE', #21756, #4053, #19249 ) ;
#6445=ORIENTED_EDGE ( 'NONE', *, *, #17263, .T. ) ;
#6455=ADVANCED_FACE ( 'NONE', ( #27956 ), #5061, .F. ) ;
#6457=CARTESIAN_POINT ( 'NONE',  ( 3.063284526839887167, -5.538577986808947529, 6.772677083992368452 ) ) ;
#6468=B_SPLINE_CURVE_WITH_KNOTS ( 'NONE', 3,
 ( #5103, #15279, #12934, #25481, #23156, #562 ),
 .UNSPECIFIED., .F., .F.,
 ( 4, 2, 4 ),
 ( 5.099451029765178191E-07, 0.0008274240357315270017, 0.001654338126360077339 ),
 .UNSPECIFIED. ) ;
#6475=AXIS2_PLACEMENT_3D ( 'NONE', #3583, #13743, #3433 ) ;
#6478=ADVANCED_FACE ( 'NONE', ( #18915 ), #6194, .T. ) ;
#6491=EDGE_CURVE ( 'NONE', #5364, #3782, #574, .T. ) ;
#6493=B_SPLINE_CURVE_WITH_KNOTS ( 'NONE', 3,
 ( #7992, #31256, #16336, #3503, #26546, #3328, #3647, #26058 ),
 .UNSPECIFIED., .F., .F.,
 ( 4, 2, 2, 4 ),
 ( 2.737843117574324537E-07, 0.001228034957219864380, 0.001841915543673917259, 0.002455796130127970572 ),
 .UNSPECIFIED. ) ;
#6504=CARTESIAN_POINT ( 'NONE',  ( 0.3045634671936401361, -0.9829946734953967091, -10.22982953726848621 ) ) ;
#6518=ORIENTED_EDGE ( 'NONE', *, *, #18269, .F. ) ;
#6520=ORIENTED_EDGE ( 'NONE', *, *, #23890, .T. ) ;
#6547=CIRCLE ( 'NONE', #16162, 10.99999999999999822 ) ;
#6548=EDGE_CURVE ( 'NONE', #22217, #28781, #5905, .T. ) ;
#6556=ORIENTED_EDGE ( 'NONE', *, *, #12216, .F. ) ;
#6558=CARTESIAN_POINT ( 'NONE',  ( 0.000000000000000000, 7.958834565716875531, -7.593217523260492818 ) ) ;
#6559=CARTESIAN_POINT ( 'NONE',  ( 0.7632845268398871230, 0.000000000000000000, 0.000000000000000000 ) ) ;
#6563=LINE ( 'NONE', #1547, #17586 ) ;
#6569=EDGE_LOOP ( 'NONE', ( #30161, #24456, #11194, #7851 ) ) ;
#6576=PLANE ( 'NONE',  #10754 ) ;
#6578=ORIENTED_EDGE ( 'NONE', *, *, #26574, .T. ) ;
#6581=CARTESIAN_POINT ( 'NONE',  ( 2.795120667416423732, -6.320583870820068562, -7.433119754668543244 ) ) ;
#6587=CIRCLE ( 'NONE', #10342, 11.00000000000000000 ) ;
#6591=AXIS2_PLACEMENT_3D ( 'NONE', #19240, #29439, #17040 ) ;
#6602=DIRECTION ( 'NONE',  ( 0.000000000000000000, 0.000000000000000000, 1.000000000000000000 ) ) ;
#6606=CARTESIAN_POINT ( 'NONE',  ( 2.274274201625327230, 0.000000000000000000, 0.000000000000000000 ) ) ;
#6615=B_SPLINE_CURVE_WITH_KNOTS ( 'NONE', 3,
 ( #20464, #17945, #20940, #25968 ),
 .UNSPECIFIED., .F., .F.,
 ( 4, 4 ),
 ( 2.049880227751699666E-07, 0.0008064882591616613769 ),
 .UNSPECIFIED. ) ;
#6629=VECTOR ( 'NONE', #27505, 1000.000000000000000 ) ;
#6679=ORIENTED_EDGE ( 'NONE', *, *, #19361, .F. ) ;
#6701=CARTESIAN_POINT ( 'NONE',  ( 2.274274201625327230, -1.975651141462315907, 10.82112760146735475 ) ) ;
#6705=DIRECTION ( 'NONE',  ( 0.000000000000000000, 0.000000000000000000, 1.000000000000000000 ) ) ;
#6709=DIRECTION ( 'NONE',  ( 0.000000000000000000, 1.000000000000000000, -1.224646799147353207E-16 ) ) ;
#6715=CARTESIAN_POINT ( 'NONE',  ( 2.857987933995207896, -9.536462466387789050, 0.6743480930025419484 ) ) ;
#6718=VERTEX_POINT ( 'NONE', #7497 ) ;
#6719=ADVANCED_FACE ( 'NONE', ( #22569 ), #25236, .T. ) ;
#6732=CARTESIAN_POINT ( 'NONE',  ( 0.000000000000000000, 8.572527594031471218E-16, 6.999999999999998224 ) ) ;
#6733=CARTESIAN_POINT ( 'NONE',  ( 0.000000000000000000, -10.90201369670497478, -1.464956435139655566 ) ) ;
#6739=DIRECTION ( 'NONE',  ( 0.000000000000000000, 0.000000000000000000, -1.000000000000000000 ) ) ;
#6740=DIRECTION ( 'NONE',  ( 0.000000000000000000, 0.000000000000000000, 1.000000000000000000 ) ) ;
#6741=CARTESIAN_POINT ( 'NONE',  ( 2.970200582152834112, -5.831559621424813322, -7.065646041987135639 ) ) ;
#6743=DIRECTION ( 'NONE',  ( 0.000000000000000000, 0.000000000000000000, 1.000000000000000000 ) ) ;
#6749=VERTEX_POINT ( 'NONE', #15204 ) ;
#6751=CARTESIAN_POINT ( 'NONE',  ( 2.274274201625327230, -5.222868219166924675, 9.680994141368751471 ) ) ;
#6755=EDGE_CURVE ( 'NONE', #17637, #31361, #175, .T. ) ;
#6760=ORIENTED_EDGE ( 'NONE', *, *, #31170, .F. ) ;
#6765=CARTESIAN_POINT ( 'NONE',  ( 2.857987972553724720, 5.059832898189586814, -8.111531947331014791 ) ) ;
#6772=DIRECTION ( 'NONE',  ( 1.000000000000000000, 0.000000000000000000, 0.000000000000000000 ) ) ;
#6775=DIRECTION ( 'NONE',  ( -0.000000000000000000, -1.000000000000000000, -0.000000000000000000 ) ) ;
#6782=ORIENTED_EDGE ( 'NONE', *, *, #23043, .F. ) ;
#6790=DIRECTION ( 'NONE',  ( 0.000000000000000000, 0.000000000000000000, 1.000000000000000000 ) ) ;
#6795=FACE_OUTER_BOUND ( 'NONE', #15768, .T. ) ;
#6804=FACE_OUTER_BOUND ( 'NONE', #1722, .T. ) ;
#6807=CARTESIAN_POINT ( 'NONE',  ( 0.7632845268448539278, 8.734705317657757817, 0.4999240074866477257 ) ) ;
#6812=VERTEX_POINT ( 'NONE', #12683 ) ;
#6818=DIRECTION ( 'NONE',  ( -1.000000000000000000, 0.000000000000000000, 0.000000000000000000 ) ) ;
#6821=EDGE_CURVE ( 'NONE', #18655, #16275, #14429, .T. ) ;
#6825=ORIENTED_EDGE ( 'NONE', *, *, #18960, .F. ) ;
#6837=CYLINDRICAL_SURFACE ( 'NONE', #10682, 8.749000000000002331 ) ;
#6846=DIRECTION ( 'NONE',  ( 1.000000000000000000, 0.000000000000000000, 0.000000000000000000 ) ) ;
#6852=DIRECTION ( 'NONE',  ( 0.000000000000000000, 0.000000000000000000, 1.000000000000000000 ) ) ;
#6860=CARTESIAN_POINT ( 'NONE',  ( 3.249999999999999556, 3.174628368996190719, -8.152713396088728359 ) ) ;
#6861=CYLINDRICAL_SURFACE ( 'NONE', #25133, 8.749000000000002331 ) ;
#6884=CARTESIAN_POINT ( 'NONE',  ( 2.274274201625327230, -7.958834565716822240, 7.593217523260554103 ) ) ;
#6895=DIRECTION ( 'NONE',  ( -1.000000000000000000, -0.000000000000000000, -0.000000000000000000 ) ) ;
#6899=EDGE_CURVE ( 'NONE', #3652, #1130, #16562, .T. ) ;
#6902=DIRECTION ( 'NONE',  ( 0.000000000000000000, 0.000000000000000000, -1.000000000000000000 ) ) ;
#6905=VERTEX_POINT ( 'NONE', #1382 ) ;
#6914=VECTOR ( 'NONE', #22868, 1000.000000000000000 ) ;
#6920=DIRECTION ( 'NONE',  ( 0.000000000000000000, 0.000000000000000000, 1.000000000000000000 ) ) ;
#6928=EDGE_CURVE ( 'NONE', #5778, #32283, #21912, .T. ) ;
#6932=VERTEX_POINT ( 'NONE', #31642 ) ;
#6940=AXIS2_PLACEMENT_3D ( 'NONE', #25327, #17798, #9770 ) ;
#6970=FACE_OUTER_BOUND ( 'NONE', #21958, .T. ) ;
#6976=AXIS2_PLACEMENT_3D ( 'NONE', #2356, #17697, #27912 ) ;
#6984=VECTOR ( 'NONE', #11011, 1000.000000000000000 ) ;
#6991=DIRECTION ( 'NONE',  ( 0.000000000000000000, 0.000000000000000000, -1.000000000000000000 ) ) ;
#6992=DIRECTION ( 'NONE',  ( -1.000000000000000000, 0.000000000000000000, 0.000000000000000000 ) ) ;
#7004=CARTESIAN_POINT ( 'NONE',  ( 2.357329895872517511, -10.75444571268657334, -1.335530315079643593 ) ) ;
#7005=DIRECTION ( 'NONE',  ( 0.000000000000000000, 1.687538997430237626E-14, 1.000000000000000000 ) ) ;
#7011=VECTOR ( 'NONE', #23159, 1000.000000000000000 ) ;
#7012=CIRCLE ( 'NONE', #28380, 8.749000000000002331 ) ;
#7013=CARTESIAN_POINT ( 'NONE',  ( 3.063284526839887167, 5.538577986808899567, 6.772677083992407532 ) ) ;
#7021=CIRCLE ( 'NONE', #5440, 10.99999999999999822 ) ;
#7022=CARTESIAN_POINT ( 'NONE',  ( 0.9499999999999995115, 0.000000000000000000, 0.000000000000000000 ) ) ;
#7026=CARTESIAN_POINT ( 'NONE',  ( 0.000000000000000000, 9.915734732513282523, -4.762163868918167786 ) ) ;
#7031=CARTESIAN_POINT ( 'NONE',  ( 2.661997627134204070, 6.664939678585267480, -7.629706518865775777 ) ) ;
#7044=CARTESIAN_POINT ( 'NONE',  ( 2.990310703069061216, -7.668352627376187058, 4.902153806112375278 ) ) ;
#7048=EDGE_CURVE ( 'NONE', #10288, #28142, #22502, .T. ) ;
#7052=CARTESIAN_POINT ( 'NONE',  ( -3.672954038633582391E-13, 4.709950686175357504, 9.884132761439534676 ) ) ;
#7055=EDGE_CURVE ( 'NONE', #10039, #20330, #14130, .T. ) ;
#7064=AXIS2_PLACEMENT_3D ( 'NONE', #28918, #31780, #20907 ) ;
#7091=ORIENTED_EDGE ( 'NONE', *, *, #21484, .F. ) ;
#7095=VERTEX_POINT ( 'NONE', #13633 ) ;
#7106=CIRCLE ( 'NONE', #2238, 8.749000000000002331 ) ;
#7116=AXIS2_PLACEMENT_3D ( 'NONE', #23848, #465, #23357 ) ;
#7119=CARTESIAN_POINT ( 'NONE',  ( 0.1606232872981965543, -2.144970499001195297, -10.41111328665008529 ) ) ;
#7152=ORIENTED_EDGE ( 'NONE', *, *, #2840, .F. ) ;
#7159=EDGE_CURVE ( 'NONE', #4619, #32326, #18683, .T. ) ;
#7161=CARTESIAN_POINT ( 'NONE',  ( 2.274274201625327230, 0.000000000000000000, 0.000000000000000000 ) ) ;
#7171=DIRECTION ( 'NONE',  ( 0.000000000000000000, 0.000000000000000000, 1.000000000000000000 ) ) ;
#7197=CARTESIAN_POINT ( 'NONE',  ( 0.7212197813471269425, 3.259817272365183705, -8.337493976377229998 ) ) ;
#7219=VERTEX_POINT ( 'NONE', #32208 ) ;
#7224=VERTEX_POINT ( 'NONE', #32698 ) ;
#7227=CARTESIAN_POINT ( 'NONE',  ( 0.000000000000000000, -8.475820894092944258, -4.057423117305486215 ) ) ;
#7235=DIRECTION ( 'NONE',  ( -1.000000000000000000, 0.000000000000000000, 0.000000000000000000 ) ) ;
#7239=CARTESIAN_POINT ( 'NONE',  ( 0.000000000000000000, 0.000000000000000000, 0.000000000000000000 ) ) ;
#7243=FACE_OUTER_BOUND ( 'NONE', #2144, .T. ) ;
#7245=VERTEX_POINT ( 'NONE', #24828 ) ;
#7249=ORIENTED_EDGE ( 'NONE', *, *, #31592, .T. ) ;
#7254=ORIENTED_EDGE ( 'NONE', *, *, #23933, .F. ) ;
#7258=VERTEX_POINT ( 'NONE', #2268 ) ;
#7260=ORIENTED_EDGE ( 'NONE', *, *, #20402, .T. ) ;
#7265=CARTESIAN_POINT ( 'NONE',  ( 2.274274201625317016, -1.975651141462152482, -10.82112760146740982 ) ) ;
#7272=CARTESIAN_POINT ( 'NONE',  ( 0.1255855353822278031, 9.314797388872380068, 5.239665997526921970 ) ) ;
#7274=DIRECTION ( 'NONE',  ( -1.000000000000000000, -0.000000000000000000, 0.000000000000000000 ) ) ;
#7280=CARTESIAN_POINT ( 'NONE',  ( 3.063284526839887167, 0.000000000000000000, 8.749000000000002331 ) ) ;
#7283=DIRECTION ( 'NONE',  ( 0.000000000000000000, 0.000000000000000000, -1.000000000000000000 ) ) ;
#7305=CARTESIAN_POINT ( 'NONE',  ( 0.000000000000000000, -1.699438267350438014, 9.241976615262153416 ) ) ;
#7308=CARTESIAN_POINT ( 'NONE',  ( 0.7632845268398871230, 3.174628368996073924, 8.152713396088772768 ) ) ;
#7326=CARTESIAN_POINT ( 'NONE',  ( 3.063284526843530919, -7.360373001715506014, -4.729683950890343880 ) ) ;
#7329=DIRECTION ( 'NONE',  ( 1.000000000000000000, -0.000000000000000000, 0.000000000000000000 ) ) ;
#7346=ORIENTED_EDGE ( 'NONE', *, *, #11783, .F. ) ;
#7347=CARTESIAN_POINT ( 'NONE',  ( 2.970200582150003488, 5.831559621433202167, 7.065646041994309456 ) ) ;
#7351=CARTESIAN_POINT ( 'NONE',  ( 0.7632845268398871230, 0.000000000000000000, 0.000000000000000000 ) ) ;
#7357=LINE ( 'NONE', #22750, #15634 ) ;
#7358=CARTESIAN_POINT ( 'NONE',  ( 2.274274201627372705, 7.593217523255878731, 7.958834565715730669 ) ) ;
#7360=DIRECTION ( 'NONE',  ( 0.000000000000000000, 0.000000000000000000, 1.000000000000000000 ) ) ;
#7373=ADVANCED_FACE ( 'NONE', ( #31008 ), #8091, .F. ) ;
#7387=LINE ( 'NONE', #2219, #1756 ) ;
#7390=ORIENTED_EDGE ( 'NONE', *, *, #1809, .F. ) ;
#7398=VERTEX_POINT ( 'NONE', #28506 ) ;
#7399=CARTESIAN_POINT ( 'NONE',  ( 3.063284526839887167, 0.000000000000000000, 0.000000000000000000 ) ) ;
#7407=EDGE_CURVE ( 'NONE', #16905, #11786, #602, .T. ) ;
#7409=CARTESIAN_POINT ( 'NONE',  ( 0.000000000000000000, -10.90201369670499609, 1.464956435139502355 ) ) ;
#7411=ORIENTED_EDGE ( 'NONE', *, *, #31869, .F. ) ;
#7413=CARTESIAN_POINT ( 'NONE',  ( 3.063284526842894540, -6.772677083981750279, 5.538577986799005259 ) ) ;
#7417=EDGE_CURVE ( 'NONE', #448, #14334, #9111, .T. ) ;
#7443=CYLINDRICAL_SURFACE ( 'NONE', #26164, 11.00000000000000000 ) ;
#7470=DIRECTION ( 'NONE',  ( -1.000000000000000000, -0.000000000000000000, -0.000000000000000000 ) ) ;
#7471=DIRECTION ( 'NONE',  ( 0.000000000000000000, 0.000000000000000000, 1.000000000000000000 ) ) ;
#7481=AXIS2_PLACEMENT_3D ( 'NONE', #8178, #5670, #25909 ) ;
#7483=AXIS2_PLACEMENT_3D ( 'NONE', #7227, #22769, #19943 ) ;
#7493=AXIS2_PLACEMENT_3D ( 'NONE', #25871, #21016, #10975 ) ;
#7497=CARTESIAN_POINT ( 'NONE',  ( 2.866494652520772846, -9.241976615239517301, 2.300561732649529123 ) ) ;
#7500=EDGE_CURVE ( 'NONE', #31355, #27203, #11830, .T. ) ;
#7501=VERTEX_POINT ( 'NONE', #26146 ) ;
#7502=CARTESIAN_POINT ( 'NONE',  ( 2.274274201625315239, -10.82112760146740449, 1.975651141462185789 ) ) ;
#7504=EDGE_CURVE ( 'NONE', #6218, #26130, #12374, .T. ) ;
#7506=CARTESIAN_POINT ( 'NONE',  ( 3.063284526839890276, 0.4999240074895630048, -8.734705317681616066 ) ) ;
#7520=ADVANCED_FACE ( 'NONE', ( #27120 ), #6576, .F. ) ;
#7524=VERTEX_POINT ( 'NONE', #14898 ) ;
#7534=CIRCLE ( 'NONE', #8606, 10.94895958125474245 ) ;
#7537=CARTESIAN_POINT ( 'NONE',  ( -7.000050800000000351, 0.000000000000000000, -6.000000000000000888 ) ) ;
#7538=CARTESIAN_POINT ( 'NONE',  ( 0.7632845268398882332, -4.729683950898921019, 7.360373001730893705 ) ) ;
#7540=CARTESIAN_POINT ( 'NONE',  ( 0.000000000000000000, -9.314797388894881180, -1.239665997526989027 ) ) ;
#7550=AXIS2_PLACEMENT_3D ( 'NONE', #5414, #17785, #4920 ) ;
#7551=CARTESIAN_POINT ( 'NONE',  ( 2.387425658415018415, 10.57543975281068249, 2.081220874697345291 ) ) ;
#7572=ORIENTED_EDGE ( 'NONE', *, *, #7921, .T. ) ;
#7576=VECTOR ( 'NONE', #20132, 1000.000000000000000 ) ;
#7586=CARTESIAN_POINT ( 'NONE',  ( 0.1574692293610884808, 9.672096048331027873, -4.391622967208299144 ) ) ;
#7588=ORIENTED_EDGE ( 'NONE', *, *, #7824, .T. ) ;
#7591=LINE ( 'NONE', #8081, #14463 ) ;
#7594=DIRECTION ( 'NONE',  ( 1.000000000000000000, 0.000000000000000000, 0.000000000000000000 ) ) ;
#7598=VECTOR ( 'NONE', #18042, 1000.000000000000000 ) ;
#7605=CARTESIAN_POINT ( 'NONE',  ( 0.1921710002436126385, 9.148850822275088390, 5.239665997525987606 ) ) ;
#7612=CIRCLE ( 'NONE', #158, 4.000000000000001776 ) ;
#7619=DIRECTION ( 'NONE',  ( 0.000000000000000000, 0.000000000000000000, 1.000000000000000000 ) ) ;
#7621=AXIS2_PLACEMENT_3D ( 'NONE', #3586, #8758, #6739 ) ;
#7625=AXIS2_PLACEMENT_3D ( 'NONE', #5561, #28, #17746 ) ;
#7626=LINE ( 'NONE', #15302, #22934 ) ;
#7630=( GEOMETRIC_REPRESENTATION_CONTEXT ( 3 ) GLOBAL_UNCERTAINTY_ASSIGNED_CONTEXT ( ( #4801 ) ) GLOBAL_UNIT_ASSIGNED_CONTEXT ( ( #20670, #25662, #15640 ) ) REPRESENTATION_CONTEXT ( 'NONE', 'WORKASPACE' ) );
#7641=VECTOR ( 'NONE', #29249, 1000.000000000000000 ) ;
#7643=VECTOR ( 'NONE', #30739, 1000.000000000000000 ) ;
#7650=VECTOR ( 'NONE', #22214, 1000.000000000000000 ) ;
#7653=CARTESIAN_POINT ( 'NONE',  ( 0.6728000631899144768, -0.5626559339043585295, 9.133409206477402620 ) ) ;
#7659=ORIENTED_EDGE ( 'NONE', *, *, #18586, .T. ) ;
#7680=ORIENTED_EDGE ( 'NONE', *, *, #11185, .T. ) ;
#7687=VERTEX_POINT ( 'NONE', #27628 ) ;
#7696=CIRCLE ( 'NONE', #23188, 8.749000000000002331 ) ;
#7705=DIRECTION ( 'NONE',  ( -1.000000000000000000, 0.000000000000000000, 0.000000000000000000 ) ) ;
#7710=CARTESIAN_POINT ( 'NONE',  ( 3.249999999999999556, 0.000000000000000000, 0.000000000000000000 ) ) ;
#7715=EDGE_CURVE ( 'NONE', #4279, #1557, #27320, .T. ) ;
#7748=LINE ( 'NONE', #386, #31121 ) ;
#7759=VERTEX_POINT ( 'NONE', #10228 ) ;
#7760=CARTESIAN_POINT ( 'NONE',  ( 0.7632845268398871230, 0.000000000000000000, 0.000000000000000000 ) ) ;
#7801=EDGE_LOOP ( 'NONE', ( #13920, #16520, #9221, #1662, #17269, #10732, #18904, #9259, #21243, #2031, #15103, #3672, #21670, #6279, #19785, #10305, #17369, #28034, #2332, #23968, #30902, #5028, #20290, #21339, #21267, #32706, #26252, #20782, #27401, #13496, #5877, #25439, #31561, #1866, #10250, #9100, #7680, #11668, #7572, #16609, #10422, #16607, #18429, #16768, #25241, #5509 ) ) ;
#7815=DIRECTION ( 'NONE',  ( 0.000000000000000000, 0.000000000000000000, 1.000000000000000000 ) ) ;
#7818=CARTESIAN_POINT ( 'NONE',  ( 0.7212197595511942172, -0.5238431420100444491, 8.936767016217512349 ) ) ;
#7821=EDGE_LOOP ( 'NONE', ( #12191, #5658, #19940, #31650 ) ) ;
#7824=EDGE_CURVE ( 'NONE', #27107, #30379, #21415, .T. ) ;
#7833=CARTESIAN_POINT ( 'NONE',  ( 0.7632845268458183785, 8.152713396062706508, 3.174628368984090176 ) ) ;
#7836=B_SPLINE_CURVE_WITH_KNOTS ( 'NONE', 3,
 ( #12538, #32299, #16883, #27079, #20080, #7347, #27585, #7013 ),
 .UNSPECIFIED., .F., .F.,
 ( 4, 2, 2, 4 ),
 ( 2.197717257119807428E-07, 0.001262070444977244840, 0.001892995781603009492, 0.002523921118228774144 ),
 .UNSPECIFIED. ) ;
#7851=ORIENTED_EDGE ( 'NONE', *, *, #16510, .F. ) ;
#7853=CARTESIAN_POINT ( 'NONE',  ( 0.7632845268398871230, 4.729683950898978750, -7.360373001730866171 ) ) ;
#7865=CARTESIAN_POINT ( 'NONE',  ( 1.624999999999999778, 7.593217523260696211, -7.958834565716684573 ) ) ;
#7872=ORIENTED_EDGE ( 'NONE', *, *, #26506, .T. ) ;
#7877=DIRECTION ( 'NONE',  ( 0.000000000000000000, 0.000000000000000000, 1.000000000000000000 ) ) ;
#7879=ORIENTED_EDGE ( 'NONE', *, *, #14733, .F. ) ;
#7885=DIRECTION ( 'NONE',  ( -1.000000000000000000, -0.000000000000000000, -0.000000000000000000 ) ) ;
#7891=CARTESIAN_POINT ( 'NONE',  ( 10.25005080000000035, 4.286263797015736102E-16, -3.499999999999999556 ) ) ;
#7918=VERTEX_POINT ( 'NONE', #24069 ) ;
#7921=EDGE_CURVE ( 'NONE', #5364, #10426, #15417, .T. ) ;
#7959=CARTESIAN_POINT ( 'NONE',  ( 0.000000000000000000, 10.76487093102067583, -1.999317321091388377 ) ) ;
#7978=EDGE_LOOP ( 'NONE', ( #17666, #22365, #13289, #28205 ) ) ;
#7979=DIRECTION ( 'NONE',  ( 0.000000000000000000, 0.000000000000000000, -1.000000000000000000 ) ) ;
#7984=CARTESIAN_POINT ( 'NONE',  ( 3.020080146456704195, -0.5244911560275570261, -8.942241244950251300 ) ) ;
#7990=FACE_OUTER_BOUND ( 'NONE', #4168, .T. ) ;
#7992=CARTESIAN_POINT ( 'NONE',  ( 0.7632845268398871230, 5.538577986808899567, 6.772677083992407532 ) ) ;
#8001=AXIS2_PLACEMENT_3D ( 'NONE', #21643, #29672, #12102 ) ;
#8003=CARTESIAN_POINT ( 'NONE',  ( 0.5664946525207626982, 9.241976615239526183, 2.300561732649596181 ) ) ;
#8007=DIRECTION ( 'NONE',  ( -1.000000000000000000, -0.000000000000000000, -0.000000000000000000 ) ) ;
#8011=CARTESIAN_POINT ( 'NONE',  ( 2.376492135548449625, -9.437149634395570530, 5.239665997527315433 ) ) ;
#8012=CARTESIAN_POINT ( 'NONE',  ( 0.7632845268398871230, 0.000000000000000000, -8.749000000000000554 ) ) ;
#8016=VECTOR ( 'NONE', #15850, 1000.000000000000000 ) ;
#8017=VECTOR ( 'NONE', #23971, 1000.000000000000000 ) ;
#8034=CARTESIAN_POINT ( 'NONE',  ( -10.00000000000000000, 0.000000000000000000, 0.000000000000000000 ) ) ;
#8035=ORIENTED_EDGE ( 'NONE', *, *, #25516, .F. ) ;
#8043=CARTESIAN_POINT ( 'NONE',  ( -10.00000000000000000, 0.000000000000000000, 0.000000000000000000 ) ) ;
#8056=VERTEX_POINT ( 'NONE', #21511 ) ;
#8063=VERTEX_POINT ( 'NONE', #14281 ) ;
#8070=ORIENTED_EDGE ( 'NONE', *, *, #20049, .F. ) ;
#8081=CARTESIAN_POINT ( 'NONE',  ( 3.249999999999999556, 9.241976615262160522, 2.300561732649596625 ) ) ;
#8085=AXIS2_PLACEMENT_3D ( 'NONE', #16901, #4197, #1533 ) ;
#8089=AXIS2_PLACEMENT_3D ( 'NONE', #18689, #8488, #11504 ) ;
#8091=PLANE ( 'NONE',  #21422 ) ;
#8096=AXIS2_PLACEMENT_3D ( 'NONE', #10656, #8167, #15844 ) ;
#8103=LINE ( 'NONE', #5621, #14072 ) ;
#8116=CIRCLE ( 'NONE', #22536, 11.00000000000000000 ) ;
#8123=VECTOR ( 'NONE', #19408, 1000.000000000000000 ) ;
#8125=FACE_OUTER_BOUND ( 'NONE', #27916, .T. ) ;
#8129=DIRECTION ( 'NONE',  ( 0.000000000000000000, 0.8090169943749446757, 0.5877852522924770229 ) ) ;
#8141=CARTESIAN_POINT ( 'NONE',  ( 2.274274201625327230, 0.000000000000000000, 0.000000000000000000 ) ) ;
#8167=DIRECTION ( 'NONE',  ( 1.000000000000000000, -0.000000000000000000, -0.000000000000000000 ) ) ;
#8168=DIRECTION ( 'NONE',  ( 1.000000000000000000, -0.000000000000000000, -0.000000000000000000 ) ) ;
#8178=CARTESIAN_POINT ( 'NONE',  ( 0.000000000000000000, 0.000000000000000000, 0.000000000000000000 ) ) ;
#8190=VERTEX_POINT ( 'NONE', #21987 ) ;
#8199=ORIENTED_EDGE ( 'NONE', *, *, #28741, .F. ) ;
#8201=EDGE_CURVE ( 'NONE', #9973, #3483, #17202, .T. ) ;
#8226=CARTESIAN_POINT ( 'NONE',  ( 0.08034255810714041601, -7.899847910285846098, 7.347818361009607280 ) ) ;
#8231=CARTESIAN_POINT ( 'NONE',  ( 3.249999999999999556, -9.314797388894900720, 1.239665997526854468 ) ) ;
#8233=EDGE_CURVE ( 'NONE', #22601, #681, #24954, .T. ) ;
#8239=CARTESIAN_POINT ( 'NONE',  ( 2.795120570943890215, -3.714272345030796174, -9.022485053477831585 ) ) ;
#8255=CARTESIAN_POINT ( 'NONE',  ( 2.661997753583466242, 0.9074203448823292550, -10.09011512947408562 ) ) ;
#8283=EDGE_CURVE ( 'NONE', #10426, #30241, #15128, .T. ) ;
#8289=DIRECTION ( 'NONE',  ( 0.000000000000000000, 0.000000000000000000, 1.000000000000000000 ) ) ;
#8301=FACE_OUTER_BOUND ( 'NONE', #17440, .T. ) ;
#8303=ORIENTED_EDGE ( 'NONE', *, *, #17613, .F. ) ;
#8310=CARTESIAN_POINT ( 'NONE',  ( 3.249999999999999556, 0.000000000000000000, 0.000000000000000000 ) ) ;
#8316=DIRECTION ( 'NONE',  ( 0.000000000000000000, 0.000000000000000000, -1.000000000000000000 ) ) ;
#8332=CARTESIAN_POINT ( 'NONE',  ( 0.3749743548324790399, 10.05686762493600028, -0.8908839545097162471 ) ) ;
#8342=FACE_OUTER_BOUND ( 'NONE', #10420, .T. ) ;
#8348=CARTESIAN_POINT ( 'NONE',  ( 0.7632845268449801601, 2.223716399040764014, 8.461683424485153537 ) ) ;
#8350=CARTESIAN_POINT ( 'NONE',  ( 0.5032039692105039208, -9.704418393844072455, -0.7352278974791732757 ) ) ;
#8385=CARTESIAN_POINT ( 'NONE',  ( 1.624999999999999778, 5.222868219166995729, -9.680994141368717720 ) ) ;
#8401=LINE ( 'NONE', #26301, #24124 ) ;
#8404=ORIENTED_EDGE ( 'NONE', *, *, #22244, .F. ) ;
#8429=CARTESIAN_POINT ( 'NONE',  ( 2.357329973329945982, 9.815384016743308848, 4.593471141847078165 ) ) ;
#8444=FACE_OUTER_BOUND ( 'NONE', #30651, .T. ) ;
#8445=CARTESIAN_POINT ( 'NONE',  ( 0.7080126359153782190, 8.723904125990792124, 2.275870607900281950 ) ) ;
#8469=ORIENTED_EDGE ( 'NONE', *, *, #17788, .T. ) ;
#8487=DIRECTION ( 'NONE',  ( 0.000000000000000000, 0.000000000000000000, 1.000000000000000000 ) ) ;
#8488=DIRECTION ( 'NONE',  ( 1.000000000000000000, 0.000000000000000000, 0.000000000000000000 ) ) ;
#8503=ADVANCED_FACE ( 'NONE', ( #31495 ), #8578, .T. ) ;
#8518=CARTESIAN_POINT ( 'NONE',  ( 0.5704037183048226156, -5.066169706250006399, 8.085411865508406848 ) ) ;
#8524=CARTESIAN_POINT ( 'NONE',  ( 2.864531019710234272, -3.575186956654052395, 8.868883597856999756 ) ) ;
#8534=DIRECTION ( 'NONE',  ( 1.000000000000000000, 0.000000000000000000, 0.000000000000000000 ) ) ;
#8549=DIRECTION ( 'NONE',  ( -1.000000000000000000, 0.000000000000000000, 0.000000000000000000 ) ) ;
#8555=AXIS2_PLACEMENT_3D ( 'NONE', #27960, #7885, #5378 ) ;
#8560=CIRCLE ( 'NONE', #4850, 8.749000000000002331 ) ;
#8568=CIRCLE ( 'NONE', #27255, 4.000000000000000888 ) ;
#8578=CYLINDRICAL_SURFACE ( 'NONE', #15610, 8.749000000000002331 ) ;
#8580=ORIENTED_EDGE ( 'NONE', *, *, #23315, .F. ) ;
#8582=B_SPLINE_CURVE_WITH_KNOTS ( 'NONE', 3,
 ( #5822, #23724, #663, #6163, #11162, #31573, #16348, #8830 ),
 .UNSPECIFIED., .F., .F.,
 ( 4, 2, 2, 4 ),
 ( 5.099451029780061619E-07, 0.001229189756360173818, 0.001843529661988771310, 0.002457869567617369452 ),
 .UNSPECIFIED. ) ;
#8593=ORIENTED_EDGE ( 'NONE', *, *, #7417, .F. ) ;
#8596=EDGE_CURVE ( 'NONE', #780, #28781, #32709, .T. ) ;
#8598=CARTESIAN_POINT ( 'NONE',  ( 0.3749743454409040222, 2.260462012960326117, -9.839947797887550252 ) ) ;
#8600=ORIENTED_EDGE ( 'NONE', *, *, #11511, .T. ) ;
#8606=AXIS2_PLACEMENT_3D ( 'NONE', #10594, #20798, #31004 ) ;
#8610=PLANE ( 'NONE',  #7493 ) ;
#8612=DIRECTION ( 'NONE',  ( -1.000000000000000000, 0.000000000000000000, 0.000000000000000000 ) ) ;
#8623=EDGE_LOOP ( 'NONE', ( #22761, #32188, #32094, #31803 ) ) ;
#8626=LINE ( 'NONE', #26673, #19418 ) ;
#8629=VERTEX_POINT ( 'NONE', #2226 ) ;
#8635=VERTEX_POINT ( 'NONE', #1918 ) ;
#8640=AXIS2_PLACEMENT_3D ( 'NONE', #10163, #29440, #6705 ) ;
#8641=CIRCLE ( 'NONE', #31618, 6.000000000000000888 ) ;
#8651=AXIS2_PLACEMENT_3D ( 'NONE', #31412, #26556, #8487 ) ;
#8658=AXIS2_PLACEMENT_3D ( 'NONE', #20497, #2447, #25335 ) ;
#8666=CIRCLE ( 'NONE', #19906, 8.749000000000002331 ) ;
#8676=ADVANCED_FACE ( 'NONE', ( #7243 ), #12090, .T. ) ;
#8677=CARTESIAN_POINT ( 'NONE',  ( 3.063284526843530919, -7.360373001715506014, -4.729683950890343880 ) ) ;
#8680=ORIENTED_EDGE ( 'NONE', *, *, #20205, .F. ) ;
#8682=AXIS2_PLACEMENT_3D ( 'NONE', #24073, #5867, #8872 ) ;
#8687=CARTESIAN_POINT ( 'NONE',  ( 0.1574692247322750649, -10.55579611470083279, 1.187839595764553335 ) ) ;
#8696=CYLINDRICAL_SURFACE ( 'NONE', #3242, 11.00000000000000000 ) ;
#8700=CARTESIAN_POINT ( 'NONE',  ( 3.249999999999999556, 9.314797388894909602, -1.239665997526784746 ) ) ;
#8724=CARTESIAN_POINT ( 'NONE',  ( 3.063284526839887167, 8.152713396088806519, -3.174628368995990879 ) ) ;
#8725=DIRECTION ( 'NONE',  ( -1.000000000000000000, -0.000000000000000000, 0.000000000000000000 ) ) ;
#8728=AXIS2_PLACEMENT_3D ( 'NONE', #12756, #10266, #17967 ) ;
#8732=DIRECTION ( 'NONE',  ( -1.000000000000000000, -0.000000000000000000, -0.000000000000000000 ) ) ;
#8738=CIRCLE ( 'NONE', #5034, 10.94895958125474245 ) ;
#8758=DIRECTION ( 'NONE',  ( 1.000000000000000000, 0.000000000000000000, 0.000000000000000000 ) ) ;
#8766=ORIENTED_EDGE ( 'NONE', *, *, #10067, .F. ) ;
#8777=EDGE_CURVE ( 'NONE', #12277, #19429, #48, .T. ) ;
#8787=CARTESIAN_POINT ( 'NONE',  ( 0.7632845268398872340, -2.223716399045631231, 8.461683424509299556 ) ) ;
#8793=CARTESIAN_POINT ( 'NONE',  ( 3.249999999999999556, 6.807171995660584507, 6.478011392632914145 ) ) ;
#8805=DIRECTION ( 'NONE',  ( 0.000000000000000000, 0.000000000000000000, -1.000000000000000000 ) ) ;
#8821=DIRECTION ( 'NONE',  ( 1.000000000000000000, -0.000000000000000000, -0.000000000000000000 ) ) ;
#8822=CARTESIAN_POINT ( 'NONE',  ( 2.274274201625327230, 0.000000000000000000, 0.000000000000000000 ) ) ;
#8830=CARTESIAN_POINT ( 'NONE',  ( 0.7632845268398871230, -3.174628368996133876, 8.152713396088751452 ) ) ;
#8841=ORIENTED_EDGE ( 'NONE', *, *, #21254, .T. ) ;
#8850=ORIENTED_EDGE ( 'NONE', *, *, #5258, .F. ) ;
#8856=EDGE_LOOP ( 'NONE', ( #32668, #30291, #28183, #20874, #10876 ) ) ;
#8860=CARTESIAN_POINT ( 'NONE',  ( 3.250000000000001332, 1.102182119233145856E-15, 7.000000000000000888 ) ) ;
#8871=DIRECTION ( 'NONE',  ( 0.000000000000000000, 0.000000000000000000, 1.000000000000000000 ) ) ;
#8872=DIRECTION ( 'NONE',  ( 0.000000000000000000, 0.000000000000000000, -1.000000000000000000 ) ) ;
#8877=PLANE ( 'NONE',  #2777 ) ;
#8892=CARTESIAN_POINT ( 'NONE',  ( 3.063284526839887167, 2.223716399045691183, -8.461683424509292450 ) ) ;
#8899=DIRECTION ( 'NONE',  ( 0.000000000000000000, 0.000000000000000000, -1.000000000000000000 ) ) ;
#8909=CARTESIAN_POINT ( 'NONE',  ( 0.000000000000000000, -10.85582367538895276, 1.425064293572299023 ) ) ;
#8911=ORIENTED_EDGE ( 'NONE', *, *, #30617, .T. ) ;
#8918=CARTESIAN_POINT ( 'NONE',  ( 3.020080204145388691, -4.831795131253269204, 7.542713057966124346 ) ) ;
#8924=DIRECTION ( 'NONE',  ( -1.000000000000000000, -0.000000000000000000, -0.000000000000000000 ) ) ;
#8931=EDGE_CURVE ( 'NONE', #4375, #6812, #23109, .T. ) ;
#8938=DIRECTION ( 'NONE',  ( 0.000000000000000000, 0.000000000000000000, 1.000000000000000000 ) ) ;
#8950=FACE_OUTER_BOUND ( 'NONE', #21078, .T. ) ;
#8951=ORIENTED_EDGE ( 'NONE', *, *, #28942, .T. ) ;
#8974=SHAPE_REPRESENTATION ( 'Part3_SlicingGear', ( #2865 ), #7630 ) ;
#8980=ORIENTED_EDGE ( 'NONE', *, *, #26233, .F. ) ;
#8987=ORIENTED_EDGE ( 'NONE', *, *, #23011, .F. ) ;
#8994=CARTESIAN_POINT ( 'NONE',  ( 0.000000000000000000, 0.000000000000000000, 0.000000000000000000 ) ) ;
#9002=FACE_OUTER_BOUND ( 'NONE', #15306, .T. ) ;
#9006=CARTESIAN_POINT ( 'NONE',  ( 0.000000000000000000, -6.807171995660629804, 6.478011392632865295 ) ) ;
#9023=DIRECTION ( 'NONE',  ( 0.000000000000000000, 0.000000000000000000, 1.000000000000000000 ) ) ;
#9028=ORIENTED_EDGE ( 'NONE', *, *, #4757, .T. ) ;
#9032=ORIENTED_EDGE ( 'NONE', *, *, #6548, .F. ) ;
#9061=CARTESIAN_POINT ( 'NONE',  ( 0.000000000000000000, 0.000000000000000000, 0.000000000000000000 ) ) ;
#9062=EDGE_CURVE ( 'NONE', #22797, #28496, #29497, .T. ) ;
#9063=CARTESIAN_POINT ( 'NONE',  ( 2.589202905186835046, 9.453729690310147760, 4.126870756446492372 ) ) ;
#9070=B_SPLINE_CURVE_WITH_KNOTS ( 'NONE', 3,
 ( #24541, #31934, #27572, #29410, #2006, #27415, #4169, #4521 ),
 .UNSPECIFIED., .F., .F.,
 ( 4, 2, 2, 4 ),
 ( 2.851296420475814781E-07, 0.001262135616826467023, 0.001893060860418674688, 0.002523986104010882137 ),
 .UNSPECIFIED. ) ;
#9073=FACE_OUTER_BOUND ( 'NONE', #14574, .T. ) ;
#9080=CARTESIAN_POINT ( 'NONE',  ( 0.000000000000000000, -7.958834565716820464, 7.593217523260552326 ) ) ;
#9091=CIRCLE ( 'NONE', #6426, 8.749000000000002331 ) ;
#9100=ORIENTED_EDGE ( 'NONE', *, *, #7048, .T. ) ;
#9111=CIRCLE ( 'NONE', #1148, 11.00000000000000000 ) ;
#9120=AXIS2_PLACEMENT_3D ( 'NONE', #3018, #8821, #13173 ) ;
#9130=VERTEX_POINT ( 'NONE', #8012 ) ;
#9133=CARTESIAN_POINT ( 'NONE',  ( 3.249999999999999556, 7.360373001730919462, 4.729683950898899703 ) ) ;
#9134=CARTESIAN_POINT ( 'NONE',  ( 0.6728000631949152543, 9.133409206458242835, 0.5626559338999654880 ) ) ;
#9144=DIRECTION ( 'NONE',  ( -1.000000000000000000, -0.000000000000000000, 0.000000000000000000 ) ) ;
#9148=EDGE_CURVE ( 'NONE', #32897, #780, #7357, .T. ) ;
#9160=FACE_OUTER_BOUND ( 'NONE', #25938, .T. ) ;
#9163=ORIENTED_EDGE ( 'NONE', *, *, #11199, .T. ) ;
#9175=FACE_OUTER_BOUND ( 'NONE', #29643, .T. ) ;
#9178=CIRCLE ( 'NONE', #26799, 10.99999999999999822 ) ;
#9185=ORIENTED_EDGE ( 'NONE', *, *, #19361, .T. ) ;
#9200=ORIENTED_EDGE ( 'NONE', *, *, #24252, .F. ) ;
#9210=EDGE_CURVE ( 'NONE', #23697, #32838, #14014, .T. ) ;
#9221=ORIENTED_EDGE ( 'NONE', *, *, #13816, .T. ) ;
#9229=ORIENTED_EDGE ( 'NONE', *, *, #9891, .T. ) ;
#9239=DIRECTION ( 'NONE',  ( -1.000000000000000000, -0.000000000000000000, 0.000000000000000000 ) ) ;
#9252=EDGE_LOOP ( 'NONE', ( #20743, #4867, #23701, #9672, #5030 ) ) ;
#9258=CARTESIAN_POINT ( 'NONE',  ( 2.795120501772739185, -5.116149273377877726, 8.308193303464529222 ) ) ;
#9259=ORIENTED_EDGE ( 'NONE', *, *, #31059, .F. ) ;
#9265=DIRECTION ( 'NONE',  ( 0.000000000000000000, 0.000000000000000000, 1.000000000000000000 ) ) ;
#9276=CARTESIAN_POINT ( 'NONE',  ( 3.249999999999999556, 0.000000000000000000, 0.000000000000000000 ) ) ;
#9284=CARTESIAN_POINT ( 'NONE',  ( 0.7212197624700831255, -2.263408446301279131, -8.661246924805441338 ) ) ;
#9298=DIRECTION ( 'NONE',  ( 0.000000000000000000, 0.000000000000000000, 1.000000000000000000 ) ) ;
#9338=ADVANCED_FACE ( 'NONE', ( #6007 ), #31422, .T. ) ;
#9360=EDGE_CURVE ( 'NONE', #7095, #30379, #31682, .T. ) ;
#9370=ORIENTED_EDGE ( 'NONE', *, *, #1623, .F. ) ;
#9374=DIRECTION ( 'NONE',  ( 1.000000000000000000, -0.000000000000000000, -0.000000000000000000 ) ) ;
#9380=ORIENTED_EDGE ( 'NONE', *, *, #10100, .T. ) ;
#9381=DIRECTION ( 'NONE',  ( 0.000000000000000000, 0.000000000000000000, -1.000000000000000000 ) ) ;
#9392=FACE_OUTER_BOUND ( 'NONE', #28631, .T. ) ;
#9397=EDGE_CURVE ( 'NONE', #11731, #24612, #29951, .T. ) ;
#9398=CARTESIAN_POINT ( 'NONE',  ( 2.857988133323936530, -7.318787950819720223, 6.150950518044190574 ) ) ;
#9403=CARTESIAN_POINT ( 'NONE',  ( 0.7632845268398871230, 8.734705317681626724, -0.4999240074894737984 ) ) ;
#9414=DIRECTION ( 'NONE',  ( -1.000000000000000000, -0.000000000000000000, 0.000000000000000000 ) ) ;
#9416=ORIENTED_EDGE ( 'NONE', *, *, #13858, .F. ) ;
#9426=ORIENTED_EDGE ( 'NONE', *, *, #30961, .F. ) ;
#9427=DIRECTION ( 'NONE',  ( -1.000000000000000000, 0.000000000000000000, 0.000000000000000000 ) ) ;
#9428=FACE_OUTER_BOUND ( 'NONE', #22066, .T. ) ;
#9433=CARTESIAN_POINT ( 'NONE',  ( 0.1574692421720941260, 7.841623826006872910, -7.165523657698227744 ) ) ;
#9446=CARTESIAN_POINT ( 'NONE',  ( 0.000000000000000000, 0.000000000000000000, 0.000000000000000000 ) ) ;
#9452=ORIENTED_EDGE ( 'NONE', *, *, #23315, .T. ) ;
#9455=ADVANCED_FACE ( 'NONE', ( #17007 ), #29584, .T. ) ;
#9464=DIRECTION ( 'NONE',  ( 1.000000000000000000, -0.000000000000000000, -0.000000000000000000 ) ) ;
#9467=CARTESIAN_POINT ( 'NONE',  ( 2.274274201625327230, 0.000000000000000000, 0.000000000000000000 ) ) ;
#9477=ORIENTED_EDGE ( 'NONE', *, *, #10053, .T. ) ;
#9479=ORIENTED_EDGE ( 'NONE', *, *, #16510, .T. ) ;
#9485=CARTESIAN_POINT ( 'NONE',  ( 0.000000000000000000, 7.944914065997111585, 7.533794289458081828 ) ) ;
#9492=EDGE_CURVE ( 'NONE', #2199, #7501, #32345, .T. ) ;
#9502=FACE_OUTER_BOUND ( 'NONE', #10974, .T. ) ;
#9521=DIRECTION ( 'NONE',  ( -1.000000000000000000, 0.000000000000000000, 0.000000000000000000 ) ) ;
#9533=DIRECTION ( 'NONE',  ( 0.000000000000000000, 0.000000000000000000, -1.000000000000000000 ) ) ;
#9544=CARTESIAN_POINT ( 'NONE',  ( 3.249999999999999556, 0.000000000000000000, 0.000000000000000000 ) ) ;
#9575=CIRCLE ( 'NONE', #26671, 8.749000000000002331 ) ;
#9577=CARTESIAN_POINT ( 'NONE',  ( 0.7632845268398872340, -2.223716399045631231, 8.461683424509299556 ) ) ;
#9582=CARTESIAN_POINT ( 'NONE',  ( 0.000000000000000000, -4.057423117305330784, -8.475820894093018865 ) ) ;
#9585=ADVANCED_FACE ( 'NONE', ( #30755 ), #12511, .T. ) ;
#9589=CARTESIAN_POINT ( 'NONE',  ( 0.3045633657612876743, 7.698316278340462837, -6.808202580038895668 ) ) ;
#9592=CARTESIAN_POINT ( 'NONE',  ( 0.08467178533536702523, 9.416764032208575941, 5.239665997527495733 ) ) ;
#9600=AXIS2_PLACEMENT_3D ( 'NONE', #29253, #6337, #29757 ) ;
#9607=DIRECTION ( 'NONE',  ( 1.000000000000000000, 0.000000000000000000, 0.000000000000000000 ) ) ;
#9616=ORIENTED_EDGE ( 'NONE', *, *, #28994, .T. ) ;
#9622=AXIS2_PLACEMENT_3D ( 'NONE', #19396, #4516, #6991 ) ;
#9629=DIRECTION ( 'NONE',  ( 0.000000000000000000, 0.000000000000000000, 1.000000000000000000 ) ) ;
#9638=CARTESIAN_POINT ( 'NONE',  ( 3.249999999999999556, 4.729683950898978750, -7.360373001730866171 ) ) ;
#9672=ORIENTED_EDGE ( 'NONE', *, *, #15312, .F. ) ;
#9678=EDGE_LOOP ( 'NONE', ( #32933, #27486, #4064, #795 ) ) ;
#9687=CIRCLE ( 'NONE', #25802, 8.749000000000002331 ) ;
#9694=VECTOR ( 'NONE', #27679, 1000.000000000000000 ) ;
#9695=B_SPLINE_CURVE_WITH_KNOTS ( 'NONE', 3,
 ( #19555, #24730, #31933, #29409, #6504, #25398, #25552, #22880 ),
 .UNSPECIFIED., .F., .F.,
 ( 4, 2, 2, 4 ),
 ( 2.024520226827691372E-07, 0.001227962984610853547, 0.001841843250904936927, 0.002455723517199020090 ),
 .UNSPECIFIED. ) ;
#9696=LINE ( 'NONE', #27592, #24173 ) ;
#9710=CARTESIAN_POINT ( 'NONE',  ( 3.063284526845909017, -8.734705317652711187, 0.4999240074859884198 ) ) ;
#9716=CIRCLE ( 'NONE', #12912, 11.00000000000000000 ) ;
#9722=DIRECTION ( 'NONE',  ( 0.000000000000000000, 0.000000000000000000, 1.000000000000000000 ) ) ;
#9723=CARTESIAN_POINT ( 'NONE',  ( 2.589202987961084279, 10.07394153291405914, -2.218054364314494986 ) ) ;
#9727=ADVANCED_FACE ( 'NONE', ( #23513 ), #29049, .T. ) ;
#9732=AXIS2_PLACEMENT_3D ( 'NONE', #19275, #9239, #26628 ) ;
#9734=CIRCLE ( 'NONE', #26320, 11.00000000000000000 ) ;
#9744=ORIENTED_EDGE ( 'NONE', *, *, #12334, .F. ) ;
#9745=CIRCLE ( 'NONE', #10825, 11.00000000000000000 ) ;
#9751=VERTEX_POINT ( 'NONE', #28860 ) ;
#9757=EDGE_CURVE ( 'NONE', #22601, #7258, #28485, .T. ) ;
#9758=VERTEX_POINT ( 'NONE', #31543 ) ;
#9764=CARTESIAN_POINT ( 'NONE',  ( 0.3045634402742549707, 9.425384029459882740, -4.096074720329697882 ) ) ;
#9770=DIRECTION ( 'NONE',  ( 0.000000000000000000, 0.000000000000000000, 1.000000000000000000 ) ) ;
#9777=ADVANCED_FACE ( 'NONE', ( #26044 ), #16323, .T. ) ;
#9782=DIRECTION ( 'NONE',  ( 0.000000000000000000, 0.000000000000000000, 1.000000000000000000 ) ) ;
#9788=AXIS2_PLACEMENT_3D ( 'NONE', #19722, #14530, #7005 ) ;
#9791=CARTESIAN_POINT ( 'NONE',  ( 0.08034253207385409767, 4.547003328335266659, 9.783802610460128335 ) ) ;
#9800=DIRECTION ( 'NONE',  ( -1.000000000000000000, -0.000000000000000000, -0.000000000000000000 ) ) ;
#9807=AXIS2_PLACEMENT_3D ( 'NONE', #18187, #827, #28573 ) ;
#9818=VERTEX_POINT ( 'NONE', #24482 ) ;
#9838=LINE ( 'NONE', #17864, #7650 ) ;
#9841=EDGE_CURVE ( 'NONE', #22601, #5630, #10835, .T. ) ;
#9850=CARTESIAN_POINT ( 'NONE',  ( 0.7212197917577903850, 7.537903528354217286, -4.829101774917270440 ) ) ;
#9876=CARTESIAN_POINT ( 'NONE',  ( 0.5640493910637699448, 7.306425354220341006, 6.134141009795914812 ) ) ;
#9885=DIRECTION ( 'NONE',  ( 1.000000000000000000, 0.000000000000000000, 0.000000000000000000 ) ) ;
#9891=EDGE_CURVE ( 'NONE', #12410, #2199, #2813, .T. ) ;
#9900=CARTESIAN_POINT ( 'NONE',  ( 2.274274201625309910, -1.464956435139646462, 10.90201369670501386 ) ) ;
#9909=ORIENTED_EDGE ( 'NONE', *, *, #17866, .F. ) ;
#9921=DIRECTION ( 'NONE',  ( 0.000000000000000000, 0.000000000000000000, 1.000000000000000000 ) ) ;
#9924=DIRECTION ( 'NONE',  ( 0.000000000000000000, 1.000000000000000000, -1.224646799147353207E-16 ) ) ;
#9929=CARTESIAN_POINT ( 'NONE',  ( -3.683682291401270757E-13, 9.884132761439586190, -4.709950686175258916 ) ) ;
#9934=CARTESIAN_POINT ( 'NONE',  ( 3.249999999999999556, 0.000000000000000000, 0.000000000000000000 ) ) ;
#9949=DIRECTION ( 'NONE',  ( 0.000000000000000000, 0.3090169943749482284, -0.9510565162951533091 ) ) ;
#9950=ORIENTED_EDGE ( 'NONE', *, *, #4615, .F. ) ;
#9955=CARTESIAN_POINT ( 'NONE',  ( 2.898548264872579328, 7.988558554883838703, 5.028941032539350431 ) ) ;
#9972=CARTESIAN_POINT ( 'NONE',  ( 0.000000000000000000, 1.975651141462238858, 10.82112760146736719 ) ) ;
#9973=VERTEX_POINT ( 'NONE', #28632 ) ;
#9990=CARTESIAN_POINT ( 'NONE',  ( 3.249999999999999556, -6.807171995660629804, 6.478011392632865295 ) ) ;
#9992=CARTESIAN_POINT ( 'NONE',  ( 0.1255855353822278031, 9.314797388872380068, 5.239665997526921970 ) ) ;
#9997=ADVANCED_FACE ( 'NONE', ( #25803 ), #30978, .T. ) ;
#9999=ADVANCED_FACE ( 'NONE', ( #2927 ), #15256, .F. ) ;
#10001=CARTESIAN_POINT ( 'NONE',  ( 0.7632845268398871230, 0.000000000000000000, 0.000000000000000000 ) ) ;
#10008=CARTESIAN_POINT ( 'NONE',  ( -3.687509558818933845E-13, 7.944914065997426889, -7.533794289458821680 ) ) ;
#10018=EDGE_CURVE ( 'NONE', #21952, #6718, #6615, .T. ) ;
#10021=DIRECTION ( 'NONE',  ( 1.000000000000000000, -0.000000000000000000, -0.000000000000000000 ) ) ;
#10039=VERTEX_POINT ( 'NONE', #18091 ) ;
#10049=CARTESIAN_POINT ( 'NONE',  ( 2.437082469501525850, 10.45536235038314921, -2.117184480729003226 ) ) ;
#10052=DIRECTION ( 'NONE',  ( -0.000000000000000000, -1.000000000000000000, -0.000000000000000000 ) ) ;
#10053=EDGE_CURVE ( 'NONE', #16695, #17980, #23593, .T. ) ;
#10067=EDGE_CURVE ( 'NONE', #11832, #16893, #1196, .T. ) ;
#10071=DIRECTION ( 'NONE',  ( 1.000000000000000000, -0.000000000000000000, -0.000000000000000000 ) ) ;
#10076=DIRECTION ( 'NONE',  ( 1.000000000000000000, 0.000000000000000000, 0.000000000000000000 ) ) ;
#10079=DIRECTION ( 'NONE',  ( -1.000000000000000000, -0.000000000000000000, -0.000000000000000000 ) ) ;
#10089=CARTESIAN_POINT ( 'NONE',  ( 0.08473242718134026130, -9.416612898531354858, 5.239665997526856245 ) ) ;
#10095=EDGE_CURVE ( 'NONE', #448, #30410, #10910, .T. ) ;
#10100=EDGE_CURVE ( 'NONE', #22217, #15150, #32158, .T. ) ;
#10109=DIRECTION ( 'NONE',  ( 0.000000000000000000, 0.000000000000000000, 1.000000000000000000 ) ) ;
#10114=VECTOR ( 'NONE', #9427, 1000.000000000000000 ) ;
#10118=CARTESIAN_POINT ( 'NONE',  ( 3.063284526839887167, 8.734705317681626724, -0.4999240074894737984 ) ) ;
#10122=ORIENTED_EDGE ( 'NONE', *, *, #25580, .T. ) ;
#10135=VERTEX_POINT ( 'NONE', #28776 ) ;
#10144=EDGE_LOOP ( 'NONE', ( #15954, #27666, #4329, #1575 ) ) ;
#10151=AXIS2_PLACEMENT_3D ( 'NONE', #8994, #17197, #24535 ) ;
#10163=CARTESIAN_POINT ( 'NONE',  ( 0.000000000000000000, 0.000000000000000000, 0.000000000000000000 ) ) ;
#10168=DIRECTION ( 'NONE',  ( 0.000000000000000000, 0.000000000000000000, 1.000000000000000000 ) ) ;
#10173=CARTESIAN_POINT ( 'NONE',  ( 0.5640492184783271190, 3.576105523027020894, -8.844377740304885549 ) ) ;
#10184=DIRECTION ( 'NONE',  ( -1.000000000000000000, 0.000000000000000000, 0.000000000000000000 ) ) ;
#10191=CARTESIAN_POINT ( 'NONE',  ( 0.3803104029207236003, -8.653113404385461394, 5.199400874759553481 ) ) ;
#10192=CIRCLE ( 'NONE', #18739, 10.99999999999999822 ) ;
#10196=EDGE_CURVE ( 'NONE', #29352, #9973, #22101, .T. ) ;
#10206=CIRCLE ( 'NONE', #31045, 6.999999999999998224 ) ;
#10216=AXIS2_PLACEMENT_3D ( 'NONE', #12750, #26132, #20958 ) ;
#10227=FACE_OUTER_BOUND ( 'NONE', #2894, .T. ) ;
#10228=CARTESIAN_POINT ( 'NONE',  ( 3.063284526839887167, 5.538577986808899567, 6.772677083992407532 ) ) ;
#10232=VECTOR ( 'NONE', #19076, 1000.000000000000000 ) ;
#10250=ORIENTED_EDGE ( 'NONE', *, *, #27657, .T. ) ;
#10252=FACE_OUTER_BOUND ( 'NONE', #11751, .T. ) ;
#10253=VERTEX_POINT ( 'NONE', #19583 ) ;
#10265=DIRECTION ( 'NONE',  ( 0.000000000000000000, 0.000000000000000000, -1.000000000000000000 ) ) ;
#10266=DIRECTION ( 'NONE',  ( 1.000000000000000000, 0.000000000000000000, 0.000000000000000000 ) ) ;
#10275=DIRECTION ( 'NONE',  ( 1.000000000000000000, -0.000000000000000000, -0.000000000000000000 ) ) ;
#10288=VERTEX_POINT ( 'NONE', #14722 ) ;
#10289=CARTESIAN_POINT ( 'NONE',  ( 2.274274201625327230, 0.000000000000000000, 0.000000000000000000 ) ) ;
#10293=ORIENTED_EDGE ( 'NONE', *, *, #6755, .F. ) ;
#10297=ORIENTED_EDGE ( 'NONE', *, *, #17866, .T. ) ;
#10300=AXIS2_PLACEMENT_3D ( 'NONE', #11982, #16973, #24486 ) ;
#10305=ORIENTED_EDGE ( 'NONE', *, *, #25623, .T. ) ;
#10307=CARTESIAN_POINT ( 'NONE',  ( 2.274274201620948510, 9.915734732518576067, -4.762163868927066446 ) ) ;
#10310=LINE ( 'NONE', #20529, #7643 ) ;
#10313=CIRCLE ( 'NONE', #25809, 4.000000000000001776 ) ;
#10314=EDGE_CURVE ( 'NONE', #12294, #9818, #32241, .T. ) ;
#10321=AXIS2_PLACEMENT_3D ( 'NONE', #16388, #3555, #8871 ) ;
#10335=CYLINDRICAL_SURFACE ( 'NONE', #27915, 4.000000000000001776 ) ;
#10338=CARTESIAN_POINT ( 'NONE',  ( 2.970200390942824509, -0.5647484629966927905, -9.143933199822400937 ) ) ;
#10342=AXIS2_PLACEMENT_3D ( 'NONE', #28859, #11308, #5959 ) ;
#10343=VECTOR ( 'NONE', #20667, 1000.000000000000000 ) ;
#10348=CARTESIAN_POINT ( 'NONE',  ( 3.063284526839887167, 0.000000000000000000, 0.000000000000000000 ) ) ;
#10352=CARTESIAN_POINT ( 'NONE',  ( 2.274274201625327230, 10.82112760146739028, -1.975651141462127391 ) ) ;
#10358=DIRECTION ( 'NONE',  ( -1.000000000000000000, -0.000000000000000000, 0.000000000000000000 ) ) ;
#10364=CIRCLE ( 'NONE', #10888, 11.00000000000000000 ) ;
#10367=CARTESIAN_POINT ( 'NONE',  ( -8.049676575031998738, 0.000000000000000000, 0.000000000000000000 ) ) ;
#10377=CARTESIAN_POINT ( 'NONE',  ( 2.274274201627370040, 7.958834565715812381, -7.593217523255793466 ) ) ;
#10381=VECTOR ( 'NONE', #28659, 1000.000000000000000 ) ;
#10393=CARTESIAN_POINT ( 'NONE',  ( 3.249999999999999556, 0.000000000000000000, 0.000000000000000000 ) ) ;
#10402=ORIENTED_EDGE ( 'NONE', *, *, #17436, .T. ) ;
#10403=CARTESIAN_POINT ( 'NONE',  ( 0.7632845268458192667, 3.174628368984171889, -8.152713396062660323 ) ) ;
#10406=LINE ( 'NONE', #7891, #30034 ) ;
#10407=ADVANCED_FACE ( 'NONE', ( #19035 ), #29379, .T. ) ;
#10416=DIRECTION ( 'NONE',  ( 1.000000000000000000, 0.000000000000000000, 0.000000000000000000 ) ) ;
#10420=EDGE_LOOP ( 'NONE', ( #5043, #2563, #7260, #23170 ) ) ;
#10422=ORIENTED_EDGE ( 'NONE', *, *, #23022, .T. ) ;
#10426=VERTEX_POINT ( 'NONE', #981 ) ;
#10441=LINE ( 'NONE', #15432, #7011 ) ;
#10465=EDGE_LOOP ( 'NONE', ( #23470, #2744, #6556, #31070, #17136 ) ) ;
#10467=CARTESIAN_POINT ( 'NONE',  ( 0.2100627325166786463, 10.28094456385920807, 2.172043487456292610 ) ) ;
#10474=CARTESIAN_POINT ( 'NONE',  ( 0.000000000000000000, 0.000000000000000000, 0.000000000000000000 ) ) ;
#10480=CARTESIAN_POINT ( 'NONE',  ( -10.00000000000000000, 0.000000000000000000, 0.000000000000000000 ) ) ;
#10493=VERTEX_POINT ( 'NONE', #19184 ) ;
#10510=DIRECTION ( 'NONE',  ( 1.000000000000000000, -0.000000000000000000, -0.000000000000000000 ) ) ;
#10519=CARTESIAN_POINT ( 'NONE',  ( 0.000000000000000000, 8.475820894092974456, 4.057423117305423155 ) ) ;
#10521=CARTESIAN_POINT ( 'NONE',  ( 0.7212197624752669789, 2.263408446298215360, 8.661246924783316814 ) ) ;
#10525=VERTEX_POINT ( 'NONE', #17659 ) ;
#10542=DIRECTION ( 'NONE',  ( -1.000000000000000000, 0.000000000000000000, 0.000000000000000000 ) ) ;
#10543=FACE_OUTER_BOUND ( 'NONE', #21791, .T. ) ;
#10561=DIRECTION ( 'NONE',  ( -1.000000000000000000, 0.000000000000000000, 0.000000000000000000 ) ) ;
#10563=MANIFOLD_SOLID_BREP ( 'Revolve1', #5637 ) ;
#10585=VERTEX_POINT ( 'NONE', #2482 ) ;
#10594=CARTESIAN_POINT ( 'NONE',  ( 0.000000000000000000, 0.000000000000000000, 0.000000000000000000 ) ) ;
#10598=CARTESIAN_POINT ( 'NONE',  ( 0.000000000000000000, -9.241976615262169403, 1.699438267350338982 ) ) ;
#10608=ORIENTED_EDGE ( 'NONE', *, *, #28224, .F. ) ;
#10620=ORIENTED_EDGE ( 'NONE', *, *, #13337, .T. ) ;
#10637=DIRECTION ( 'NONE',  ( -1.000000000000000000, 0.000000000000000000, 0.000000000000000000 ) ) ;
#10654=EDGE_CURVE ( 'NONE', #19087, #25039, #27897, .T. ) ;
#10656=CARTESIAN_POINT ( 'NONE',  ( 3.063284526839887167, 0.000000000000000000, 0.000000000000000000 ) ) ;
#10664=ORIENTED_EDGE ( 'NONE', *, *, #26540, .F. ) ;
#10671=ADVANCED_FACE ( 'NONE', ( #8444 ), #31519, .F. ) ;
#10672=DIRECTION ( 'NONE',  ( 0.000000000000000000, 0.000000000000000000, 1.000000000000000000 ) ) ;
#10677=CARTESIAN_POINT ( 'NONE',  ( 3.249999999999999556, -0.4999240074895051067, 8.734705317681624948 ) ) ;
#10682=AXIS2_PLACEMENT_3D ( 'NONE', #17022, #4343, #14523 ) ;
#10687=ORIENTED_EDGE ( 'NONE', *, *, #16827, .T. ) ;
#10698=LINE ( 'NONE', #7537, #5971 ) ;
#10712=ADVANCED_FACE ( 'NONE', ( #13928 ), #16131, .T. ) ;
#10717=DIRECTION ( 'NONE',  ( 0.000000000000000000, 0.000000000000000000, 1.000000000000000000 ) ) ;
#10723=VERTEX_POINT ( 'NONE', #18820 ) ;
#10728=VECTOR ( 'NONE', #21238, 1000.000000000000000 ) ;
#10732=ORIENTED_EDGE ( 'NONE', *, *, #9210, .T. ) ;
#10741=VERTEX_POINT ( 'NONE', #26358 ) ;
#10745=EDGE_CURVE ( 'NONE', #12480, #1608, #4948, .T. ) ;
#10747=ORIENTED_EDGE ( 'NONE', *, *, #22622, .F. ) ;
#10754=AXIS2_PLACEMENT_3D ( 'NONE', #7239, #1913, #2060 ) ;
#10764=AXIS2_PLACEMENT_3D ( 'NONE', #17796, #15611, #5101 ) ;
#10778=EDGE_LOOP ( 'NONE', ( #24100, #12559, #32141, #2413, #15378 ) ) ;
#10780=EDGE_CURVE ( 'NONE', #1359, #10135, #7612, .T. ) ;
#10792=ORIENTED_EDGE ( 'NONE', *, *, #30254, .F. ) ;
#10807=DIRECTION ( 'NONE',  ( -1.000000000000000000, 0.000000000000000000, 0.000000000000000000 ) ) ;
#10813=ORIENTED_EDGE ( 'NONE', *, *, #5362, .F. ) ;
#10815=AXIS2_PLACEMENT_3D ( 'NONE', #14245, #28993, #13903 ) ;
#10819=CARTESIAN_POINT ( 'NONE',  ( -7.000050800000000351, 0.000000000000000000, 0.000000000000000000 ) ) ;
#10825=AXIS2_PLACEMENT_3D ( 'NONE', #17375, #6992, #27409 ) ;
#10835=CIRCLE ( 'NONE', #27928, 10.94895958125474245 ) ;
#10840=CARTESIAN_POINT ( 'NONE',  ( 0.6791197464446645515, 9.138998021039178354, -0.5477823182331189589 ) ) ;
#10844=FACE_OUTER_BOUND ( 'NONE', #5128, .T. ) ;
#10853=CARTESIAN_POINT ( 'NONE',  ( 0.000000000000000000, 5.227991826304090317, 9.620177616658001085 ) ) ;
#10855=FACE_OUTER_BOUND ( 'NONE', #22694, .T. ) ;
#10874=B_SPLINE_CURVE_WITH_KNOTS ( 'NONE', 3,
 ( #28502, #25831, #5605, #20969, #13409, #5751, #3248, #23628 ),
 .UNSPECIFIED., .F., .F.,
 ( 4, 2, 2, 4 ),
 ( 2.494123547463239299E-07, 0.001262099805913989873, 0.001893025002693609444, 0.002523950199473228798 ),
 .UNSPECIFIED. ) ;
#10876=ORIENTED_EDGE ( 'NONE', *, *, #29391, .T. ) ;
#10878=B_SPLINE_CURVE_WITH_KNOTS ( 'NONE', 3,
 ( #25524, #4640, #27544, #30068, #30383, #12494, #22525, #17495 ),
 .UNSPECIFIED., .F., .F.,
 ( 4, 2, 2, 4 ),
 ( 5.099451029794817991E-07, 0.001229189590460703658, 0.001843529413139567913, 0.002457869235818432169 ),
 .UNSPECIFIED. ) ;
#10888=AXIS2_PLACEMENT_3D ( 'NONE', #20925, #28456, #17930 ) ;
#10892=CARTESIAN_POINT ( 'NONE',  ( 0.000000000000000000, -5.227991826304158707, 9.620177616657965558 ) ) ;
#10895=DIRECTION ( 'NONE',  ( 1.000000000000000000, -0.000000000000000000, -0.000000000000000000 ) ) ;
#10910=LINE ( 'NONE', #21262, #27868 ) ;
#10962=ORIENTED_EDGE ( 'NONE', *, *, #22893, .T. ) ;
#10964=ORIENTED_EDGE ( 'NONE', *, *, #21300, .F. ) ;
#10971=CARTESIAN_POINT ( 'NONE',  ( 0.6728000687415590653, 8.860258565202267178, -2.287261066729833647 ) ) ;
#10973=B_SPLINE_CURVE_WITH_KNOTS ( 'NONE', 3,
 ( #20002, #25150, #2597, #12947, #2270, #15123, #7605, #7272 ),
 .UNSPECIFIED., .F., .F.,
 ( 4, 2, 2, 4 ),
 ( 2.304311362624057754E-07, 0.001064504214901549435, 0.001596641106784193239, 0.002128777998666837260 ),
 .UNSPECIFIED. ) ;
#10974=EDGE_LOOP ( 'NONE', ( #18628, #10747, #23960, #17992 ) ) ;
#10975=DIRECTION ( 'NONE',  ( 0.000000000000000000, 0.000000000000000000, -1.000000000000000000 ) ) ;
#10981=CYLINDRICAL_SURFACE ( 'NONE', #27847, 4.000000000000001776 ) ;
#10986=EDGE_LOOP ( 'NONE', ( #20637, #32226, #4384, #2712, #25978 ) ) ;
#11011=DIRECTION ( 'NONE',  ( 1.000000000000000000, 0.000000000000000000, -0.000000000000000000 ) ) ;
#11013=ORIENTED_EDGE ( 'NONE', *, *, #28395, .T. ) ;
#11027=FACE_OUTER_BOUND ( 'NONE', #1075, .T. ) ;
#11033=DIRECTION ( 'NONE',  ( 0.000000000000000000, 0.000000000000000000, 1.000000000000000000 ) ) ;
#11036=EDGE_LOOP ( 'NONE', ( #243, #23613 ) ) ;
#11037=ORIENTED_EDGE ( 'NONE', *, *, #16432, .F. ) ;
#11058=EDGE_CURVE ( 'NONE', #10525, #7245, #2171, .T. ) ;
#11068=CARTESIAN_POINT ( 'NONE',  ( 2.274274201625318348, -5.222868219166783454, -9.680994141368850947 ) ) ;
#11071=DIRECTION ( 'NONE',  ( -1.000000000000000000, 0.000000000000000000, 0.000000000000000000 ) ) ;
#11082=DIRECTION ( 'NONE',  ( -1.000000000000000000, 0.000000000000000000, 0.000000000000000000 ) ) ;
#11092=ORIENTED_EDGE ( 'NONE', *, *, #31638, .T. ) ;
#11096=CARTESIAN_POINT ( 'NONE',  ( 2.864530875629069051, 9.539603485476133571, 0.6595692664037854369 ) ) ;
#11101=ORIENTED_EDGE ( 'NONE', *, *, #12601, .F. ) ;
#11114=CARTESIAN_POINT ( 'NONE',  ( 0.1574692253521047247, 2.132217800984971934, -10.40622129948815910 ) ) ;
#11119=CARTESIAN_POINT ( 'NONE',  ( 2.970200481228956413, 4.917777846811763887, -7.729547851462088559 ) ) ;
#11126=EDGE_CURVE ( 'NONE', #15594, #7501, #18868, .T. ) ;
#11128=CYLINDRICAL_SURFACE ( 'NONE', #17704, 8.749000000000002331 ) ;
#11129=CARTESIAN_POINT ( 'NONE',  ( 0.7212198416532932255, -6.922088825881659524, -5.676697589997751869 ) ) ;
#11135=DIRECTION ( 'NONE',  ( 1.000000000000000000, -0.000000000000000000, -0.000000000000000000 ) ) ;
#11161=DIRECTION ( 'NONE',  ( 0.000000000000000000, 0.000000000000000000, -1.000000000000000000 ) ) ;
#11162=CARTESIAN_POINT ( 'NONE',  ( 0.5640492184727913250, -3.576105523038064504, 8.844377740319870895 ) ) ;
#11184=CARTESIAN_POINT ( 'NONE',  ( 0.000000000000000000, 8.264486777890107660, -4.472189673936814991 ) ) ;
#11185=EDGE_CURVE ( 'NONE', #28142, #3782, #13697, .T. ) ;
#11194=ORIENTED_EDGE ( 'NONE', *, *, #26632, .F. ) ;
#11199=EDGE_CURVE ( 'NONE', #14830, #15097, #14473, .T. ) ;
#11201=ORIENTED_EDGE ( 'NONE', *, *, #12704, .T. ) ;
#11223=DIRECTION ( 'NONE',  ( 1.000000000000000000, 0.000000000000000000, 0.000000000000000000 ) ) ;
#11224=ORIENTED_EDGE ( 'NONE', *, *, #12017, .F. ) ;
#11225=CARTESIAN_POINT ( 'NONE',  ( -10.00000000000000000, 0.000000000000000000, 0.000000000000000000 ) ) ;
#11227=ORIENTED_EDGE ( 'NONE', *, *, #17335, .F. ) ;
#11240=EDGE_CURVE ( 'NONE', #5778, #7501, #11386, .T. ) ;
#11247=CARTESIAN_POINT ( 'NONE',  ( 2.864531019710239601, 3.575186956654106574, -8.868883597856958900 ) ) ;
#11250=CARTESIAN_POINT ( 'NONE',  ( 0.000000000000000000, -4.709950686174546597, -9.884132761439110126 ) ) ;
#11252=CARTESIAN_POINT ( 'NONE',  ( 0.6791197464446651066, 0.5477823182330875396, 9.138998021039181907 ) ) ;
#11257=VERTEX_POINT ( 'NONE', #9972 ) ;
#11261=AXIS2_PLACEMENT_3D ( 'NONE', #2159, #30263, #25554 ) ;
#11274=ORIENTED_EDGE ( 'NONE', *, *, #8283, .T. ) ;
#11277=B_SPLINE_CURVE_WITH_KNOTS ( 'NONE', 3,
 ( #32202, #29686, #29179, #13933, #6765, #11119, #16305, #21656 ),
 .UNSPECIFIED., .F., .F.,
 ( 4, 2, 2, 4 ),
 ( 2.152606690539618764E-07, 0.001262065476468824396, 0.001892990584368709666, 0.002523915692268595152 ),
 .UNSPECIFIED. ) ;
#11283=DIRECTION ( 'NONE',  ( 1.000000000000000000, 0.000000000000000000, 0.000000000000000000 ) ) ;
#11287=AXIS2_PLACEMENT_3D ( 'NONE', #18906, #5842, #26090 ) ;
#11294=CARTESIAN_POINT ( 'NONE',  ( -3.671333707197877479E-13, 1.999317321091317545, -10.76487093102143433 ) ) ;
#11295=DIRECTION ( 'NONE',  ( -1.000000000000000000, 0.000000000000000000, 0.000000000000000000 ) ) ;
#11300=FACE_OUTER_BOUND ( 'NONE', #20115, .T. ) ;
#11308=DIRECTION ( 'NONE',  ( -1.000000000000000000, 0.000000000000000000, 0.000000000000000000 ) ) ;
#11321=CIRCLE ( 'NONE', #2267, 4.000000000000001776 ) ;
#11324=CARTESIAN_POINT ( 'NONE',  ( 2.589203020517547138, 5.222514179739501827, 8.895471158038665394 ) ) ;
#11327=LINE ( 'NONE', #18864, #15156 ) ;
#11338=CIRCLE ( 'NONE', #23117, 4.000000000000001776 ) ;
#11346=CIRCLE ( 'NONE', #22570, 4.000000000000001776 ) ;
#11347=CARTESIAN_POINT ( 'NONE',  ( -7.000050800000001239, 0.000000000000000000, 0.000000000000000000 ) ) ;
#11355=ORIENTED_EDGE ( 'NONE', *, *, #33060, .F. ) ;
#11360=ORIENTED_EDGE ( 'NONE', *, *, #11405, .T. ) ;
#11364=AXIS2_PLACEMENT_3D ( 'NONE', #7351, #2873, #18204 ) ;
#11365=CIRCLE ( 'NONE', #7621, 4.000000000000001776 ) ;
#11385=ORIENTED_EDGE ( 'NONE', *, *, #16435, .F. ) ;
#11386=CIRCLE ( 'NONE', #15660, 11.00000000000000000 ) ;
#11394=CARTESIAN_POINT ( 'NONE',  ( 0.5704039292223109792, -6.124150562935243514, -7.316743080999502880 ) ) ;
#11405=EDGE_CURVE ( 'NONE', #7918, #8629, #17344, .T. ) ;
#11407=CIRCLE ( 'NONE', #8728, 10.94895958125474245 ) ;
#11411=ORIENTED_EDGE ( 'NONE', *, *, #19461, .F. ) ;
#11412=ORIENTED_EDGE ( 'NONE', *, *, #10018, .F. ) ;
#11414=AXIS2_PLACEMENT_3D ( 'NONE', #28327, #12769, #2779 ) ;
#11415=EDGE_CURVE ( 'NONE', #6905, #14707, #30621, .T. ) ;
#11429=DIRECTION ( 'NONE',  ( -1.000000000000000000, 0.000000000000000000, 0.000000000000000000 ) ) ;
#11432=AXIS2_PLACEMENT_3D ( 'NONE', #17168, #22034, #29729 ) ;
#11433=EDGE_LOOP ( 'NONE', ( #22359, #6518, #31325, #7659, #11725 ) ) ;
#11435=DIRECTION ( 'NONE',  ( -1.000000000000000000, 0.000000000000000000, -0.000000000000000000 ) ) ;
#11446=ORIENTED_EDGE ( 'NONE', *, *, #19665, .T. ) ;
#11451=CARTESIAN_POINT ( 'NONE',  ( 3.249999999999999556, 7.360373001730986964, -4.729683950898791345 ) ) ;
#11460=CARTESIAN_POINT ( 'NONE',  ( -1.361091220733346370E-15, -7.944914065997057406, -7.533794289458144000 ) ) ;
#11481=ORIENTED_EDGE ( 'NONE', *, *, #16384, .T. ) ;
#11482=CYLINDRICAL_SURFACE ( 'NONE', #10300, 8.749000000000002331 ) ;
#11492=ORIENTED_EDGE ( 'NONE', *, *, #16384, .F. ) ;
#11499=DIRECTION ( 'NONE',  ( -1.000000000000000000, -0.000000000000000000, 0.000000000000000000 ) ) ;
#11500=CYLINDRICAL_SURFACE ( 'NONE', #18819, 11.00000000000000000 ) ;
#11504=DIRECTION ( 'NONE',  ( 0.000000000000000000, 0.000000000000000000, -1.000000000000000000 ) ) ;
#11511=EDGE_CURVE ( 'NONE', #15150, #780, #3899, .T. ) ;
#11514=EDGE_CURVE ( 'NONE', #2486, #2084, #32439, .T. ) ;
#11525=CARTESIAN_POINT ( 'NONE',  ( 0.000000000000000000, -10.85582367538895276, 1.425064293572299023 ) ) ;
#11539=ORIENTED_EDGE ( 'NONE', *, *, #28831, .T. ) ;
#11542=DIRECTION ( 'NONE',  ( -1.000000000000000000, 0.000000000000000000, -0.000000000000000000 ) ) ;
#11549=CARTESIAN_POINT ( 'NONE',  ( 0.3749740905865315277, -6.632019415960365372, -7.612528756000566332 ) ) ;
#11556=CARTESIAN_POINT ( 'NONE',  ( 3.249999999999999556, 2.223716399045570835, 8.461683424509324425 ) ) ;
#11570=FACE_OUTER_BOUND ( 'NONE', #21771, .T. ) ;
#11576=CARTESIAN_POINT ( 'NONE',  ( 0.000000000000000000, 0.000000000000000000, 0.000000000000000000 ) ) ;
#11590=EDGE_CURVE ( 'NONE', #2834, #22995, #10310, .T. ) ;
#11598=DIRECTION ( 'NONE',  ( -1.000000000000000000, 0.000000000000000000, 0.000000000000000000 ) ) ;
#11607=ORIENTED_EDGE ( 'NONE', *, *, #21346, .F. ) ;
#11612=CARTESIAN_POINT ( 'NONE',  ( 3.249999999999999556, -4.729683950898817102, -7.360373001730970977 ) ) ;
#11614=CARTESIAN_POINT ( 'NONE',  ( 3.249999999999999556, 8.264486777890107660, -4.472189673936814991 ) ) ;
#11617=EDGE_CURVE ( 'NONE', #2486, #32250, #10313, .T. ) ;
#11621=DIRECTION ( 'NONE',  ( 0.000000000000000000, 0.000000000000000000, 1.000000000000000000 ) ) ;
#11651=CARTESIAN_POINT ( 'NONE',  ( 1.624999999999999778, -4.762163868918207754, -9.915734732513271865 ) ) ;
#11657=CARTESIAN_POINT ( 'NONE',  ( -3.449949199999996274, 7.347880794884120722E-16, 6.000000000000000888 ) ) ;
#11666=CARTESIAN_POINT ( 'NONE',  ( 2.976845824368064442, 7.725179967474443465, -4.933977349953490688 ) ) ;
#11668=ORIENTED_EDGE ( 'NONE', *, *, #6491, .F. ) ;
#11679=ORIENTED_EDGE ( 'NONE', *, *, #14073, .F. ) ;
#11694=ORIENTED_EDGE ( 'NONE', *, *, #7407, .F. ) ;
#11705=EDGE_LOOP ( 'NONE', ( #29014, #28684, #8303, #29533 ) ) ;
#11715=ORIENTED_EDGE ( 'NONE', *, *, #28362, .F. ) ;
#11719=ORIENTED_EDGE ( 'NONE', *, *, #24763, .F. ) ;
#11723=DIRECTION ( 'NONE',  ( 0.000000000000000000, 0.000000000000000000, -1.000000000000000000 ) ) ;
#11724=DIRECTION ( 'NONE',  ( -1.000000000000000000, 0.000000000000000000, 0.000000000000000000 ) ) ;
#11725=ORIENTED_EDGE ( 'NONE', *, *, #353, .F. ) ;
#11728=CARTESIAN_POINT ( 'NONE',  ( 0.000000000000000000, 0.000000000000000000, 0.000000000000000000 ) ) ;
#11731=VERTEX_POINT ( 'NONE', #27002 ) ;
#11738=CARTESIAN_POINT ( 'NONE',  ( 0.5032041927225600064, -6.298925283836295463, 7.418882907483850708 ) ) ;
#11747=VECTOR ( 'NONE', #7329, 1000.000000000000000 ) ;
#11748=DIRECTION ( 'NONE',  ( 0.000000000000000000, 2.042810365310287719E-14, 1.000000000000000000 ) ) ;
#11749=VERTEX_POINT ( 'NONE', #8787 ) ;
#11751=EDGE_LOOP ( 'NONE', ( #10964, #27764, #8070, #2354, #28537 ) ) ;
#11756=CARTESIAN_POINT ( 'NONE',  ( 0.000000000000000000, 0.000000000000000000, 0.000000000000000000 ) ) ;
#11767=ORIENTED_EDGE ( 'NONE', *, *, #7715, .T. ) ;
#11770=DIRECTION ( 'NONE',  ( 0.000000000000000000, 0.000000000000000000, 1.000000000000000000 ) ) ;
#11774=EDGE_CURVE ( 'NONE', #28142, #22329, #21974, .T. ) ;
#11783=EDGE_CURVE ( 'NONE', #27107, #25565, #11277, .T. ) ;
#11786=VERTEX_POINT ( 'NONE', #3615 ) ;
#11800=DIRECTION ( 'NONE',  ( 1.000000000000000000, -0.000000000000000000, -0.000000000000000000 ) ) ;
#11809=VECTOR ( 'NONE', #5254, 1000.000000000000000 ) ;
#11812=ORIENTED_EDGE ( 'NONE', *, *, #27003, .F. ) ;
#11830=CIRCLE ( 'NONE', #26253, 4.000000000000001776 ) ;
#11832=VERTEX_POINT ( 'NONE', #4602 ) ;
#11833=AXIS2_PLACEMENT_3D ( 'NONE', #27336, #19815, #1776 ) ;
#11841=ORIENTED_EDGE ( 'NONE', *, *, #2235, .F. ) ;
#11843=ADVANCED_FACE ( 'NONE', ( #22810 ), #20302, .T. ) ;
#11844=AXIS2_PLACEMENT_3D ( 'NONE', #15766, #23435, #17592 ) ;
#11851=CARTESIAN_POINT ( 'NONE',  ( -7.000050800000000351, 0.000000000000000000, 0.000000000000000000 ) ) ;
#11852=VECTOR ( 'NONE', #9374, 1000.000000000000000 ) ;
#11854=ORIENTED_EDGE ( 'NONE', *, *, #16432, .T. ) ;
#11858=DIRECTION ( 'NONE',  ( 1.000000000000000000, 0.000000000000000000, 0.000000000000000000 ) ) ;
#11862=CIRCLE ( 'NONE', #18814, 11.00000000000000000 ) ;
#11864=CYLINDRICAL_SURFACE ( 'NONE', #32056, 4.000000000000001776 ) ;
#11887=AXIS2_PLACEMENT_3D ( 'NONE', #12085, #32652, #24791 ) ;
#11892=ORIENTED_EDGE ( 'NONE', *, *, #18269, .T. ) ;
#11897=AXIS2_PLACEMENT_3D ( 'NONE', #7540, #27955, #5060 ) ;
#11916=AXIS2_PLACEMENT_3D ( 'NONE', #26716, #3524, #13187 ) ;
#11925=AXIS2_PLACEMENT_3D ( 'NONE', #29436, #8534, #16735 ) ;
#11930=DIRECTION ( 'NONE',  ( -1.000000000000000000, -0.000000000000000000, -0.000000000000000000 ) ) ;
#11935=CARTESIAN_POINT ( 'NONE',  ( 3.020080256212049896, -5.680439424464590381, -6.926136578642559272 ) ) ;
#11942=CARTESIAN_POINT ( 'NONE',  ( 2.437082531750065950, -7.214115859539295350, 7.858345965138763489 ) ) ;
#11944=EDGE_LOOP ( 'NONE', ( #24247, #13533, #11411, #12998 ) ) ;
#11949=CARTESIAN_POINT ( 'NONE',  ( 2.970200481232436740, -4.917777846806421493, 7.729547851449619422 ) ) ;
#11961=DIRECTION ( 'NONE',  ( 1.000000000000000000, -0.000000000000000000, -0.000000000000000000 ) ) ;
#11970=DIRECTION ( 'NONE',  ( -1.000000000000000000, 0.000000000000000000, 0.000000000000000000 ) ) ;
#11982=CARTESIAN_POINT ( 'NONE',  ( 3.249999999999999556, 0.000000000000000000, 0.000000000000000000 ) ) ;
#11986=CARTESIAN_POINT ( 'NONE',  ( 3.063284526839887167, 0.000000000000000000, 0.000000000000000000 ) ) ;
#11987=ORIENTED_EDGE ( 'NONE', *, *, #31684, .T. ) ;
#12004=DIRECTION ( 'NONE',  ( 1.000000000000000000, -0.000000000000000000, -0.000000000000000000 ) ) ;
#12017=EDGE_CURVE ( 'NONE', #22797, #17929, #6468, .T. ) ;
#12019=CARTESIAN_POINT ( 'NONE',  ( 2.589203020517547582, 8.895471158038725790, -5.222514179739403239 ) ) ;
#12031=ORIENTED_EDGE ( 'NONE', *, *, #10654, .F. ) ;
#12036=DIRECTION ( 'NONE',  ( -1.000000000000000000, 0.000000000000000000, 0.000000000000000000 ) ) ;
#12037=ORIENTED_EDGE ( 'NONE', *, *, #19635, .T. ) ;
#12039=DIRECTION ( 'NONE',  ( 1.000000000000000000, 0.000000000000000000, 0.000000000000000000 ) ) ;
#12047=EDGE_CURVE ( 'NONE', #22885, #29923, #10874, .T. ) ;
#12056=EDGE_CURVE ( 'NONE', #16695, #6314, #11407, .T. ) ;
#12057=CARTESIAN_POINT ( 'NONE',  ( 0.000000000000000000, 10.82112760146738850, -1.975651141462128280 ) ) ;
#12059=B_SPLINE_CURVE_WITH_KNOTS ( 'NONE', 3,
 ( #25096, #17270, #24942, #27115, #4570, #14744, #2055, #2214 ),
 .UNSPECIFIED., .F., .F.,
 ( 4, 2, 2, 4 ),
 ( 2.213836054482316663E-07, 0.001261154818855362647, 0.001891621536480320902, 0.002522088254105278940 ),
 .UNSPECIFIED. ) ;
#12071=CARTESIAN_POINT ( 'NONE',  ( 2.736976356551361622, -8.480777311736980906, 5.155436092272288384 ) ) ;
#12078=CARTESIAN_POINT ( 'NONE',  ( 2.274274201625327230, 10.82112760146739028, -1.975651141462127391 ) ) ;
#12082=DIRECTION ( 'NONE',  ( -1.000000000000000000, -0.000000000000000000, -0.000000000000000000 ) ) ;
#12085=CARTESIAN_POINT ( 'NONE',  ( 3.249999999999999556, 8.264486777890107660, 4.472189673936814991 ) ) ;
#12090=CYLINDRICAL_SURFACE ( 'NONE', #19330, 11.00000000000000000 ) ;
#12097=EDGE_LOOP ( 'NONE', ( #20982, #197, #17081, #1860 ) ) ;
#12102=DIRECTION ( 'NONE',  ( 0.000000000000000000, 0.000000000000000000, 1.000000000000000000 ) ) ;
#12131=CARTESIAN_POINT ( 'NONE',  ( 2.864531314636033610, 7.330015575757897750, 6.140839842381188518 ) ) ;
#12133=CARTESIAN_POINT ( 'NONE',  ( 2.990360172271274486, 7.668143846948784592, 4.902036888218493260 ) ) ;
#12135=CARTESIAN_POINT ( 'NONE',  ( 0.000000000000000000, 0.000000000000000000, 0.000000000000000000 ) ) ;
#12165=CARTESIAN_POINT ( 'NONE',  ( 3.249999999999999556, 1.239665997526887109, 9.314797388894895391 ) ) ;
#12187=LINE ( 'NONE', #1864, #8123 ) ;
#12189=EDGE_LOOP ( 'NONE', ( #10792, #831, #11767, #29132 ) ) ;
#12191=ORIENTED_EDGE ( 'NONE', *, *, #23302, .F. ) ;
#12201=CARTESIAN_POINT ( 'NONE',  ( 0.5032041927271341253, 7.418882907476129773, 6.298925283824120314 ) ) ;
#12207=DIRECTION ( 'NONE',  ( 0.000000000000000000, 0.000000000000000000, 1.000000000000000000 ) ) ;
#12210=VERTEX_POINT ( 'NONE', #15067 ) ;
#12216=EDGE_CURVE ( 'NONE', #26576, #2834, #19636, .T. ) ;
#12227=CARTESIAN_POINT ( 'NONE',  ( 2.274274201625319236, -9.680994141368833183, 5.222868219166820758 ) ) ;
#12234=VERTEX_POINT ( 'NONE', #12227 ) ;
#12236=DIRECTION ( 'NONE',  ( 0.000000000000000000, 0.000000000000000000, 1.000000000000000000 ) ) ;
#12245=EDGE_CURVE ( 'NONE', #29709, #11749, #7696, .T. ) ;
#12247=EDGE_LOOP ( 'NONE', ( #28065, #21917, #1732, #6578 ) ) ;
#12273=CARTESIAN_POINT ( 'NONE',  ( 0.000000000000000000, 7.533794289458167981, -7.944914065997031649 ) ) ;
#12277=VERTEX_POINT ( 'NONE', #32488 ) ;
#12288=ORIENTED_EDGE ( 'NONE', *, *, #2552, .T. ) ;
#12294=VERTEX_POINT ( 'NONE', #6732 ) ;
#12302=AXIS2_PLACEMENT_3D ( 'NONE', #16233, #26270, #13854 ) ;
#12305=AXIS2_PLACEMENT_3D ( 'NONE', #13542, #30954, #1009 ) ;
#12319=CARTESIAN_POINT ( 'NONE',  ( 0.000000000000000000, 7.347880794884120722E-16, 6.000000000000000888 ) ) ;
#12330=B_SPLINE_CURVE_WITH_KNOTS ( 'NONE', 3,
 ( #18395, #23549, #493, #2527, #20736, #30788 ),
 .UNSPECIFIED., .F., .F.,
 ( 4, 2, 4 ),
 ( 0.0008064882591616613769, 0.001664279756741902493, 0.002522071254322143935 ),
 .UNSPECIFIED. ) ;
#12334=EDGE_CURVE ( 'NONE', #18943, #6749, #12059, .T. ) ;
#12340=CARTESIAN_POINT ( 'NONE',  ( 1.624999999999999778, -7.593217523260639368, 7.958834565716742304 ) ) ;
#12358=CARTESIAN_POINT ( 'NONE',  ( 0.000000000000000000, 4.057423117305393845, 8.475820894092990443 ) ) ;
#12374=CIRCLE ( 'NONE', #6475, 8.749000000000002331 ) ;
#12375=CARTESIAN_POINT ( 'NONE',  ( 2.357330058169019527, 7.401770933800327690, -7.915524238820659697 ) ) ;
#12378=VECTOR ( 'NONE', #20928, 1000.000000000000000 ) ;
#12388=AXIS2_PLACEMENT_3D ( 'NONE', #28177, #30725, #8289 ) ;
#12390=CARTESIAN_POINT ( 'NONE',  ( 0.1606233164486141063, 5.257199111574340833, 9.238724727304049367 ) ) ;
#12394=DIRECTION ( 'NONE',  ( 0.000000000000000000, 0.000000000000000000, 1.000000000000000000 ) ) ;
#12410=VERTEX_POINT ( 'NONE', #18245 ) ;
#12413=CIRCLE ( 'NONE', #16681, 10.94895958125474245 ) ;
#12415=EDGE_CURVE ( 'NONE', #10741, #19641, #10364, .T. ) ;
#12425=EDGE_LOOP ( 'NONE', ( #3634, #30532, #15776, #19736 ) ) ;
#12428=CARTESIAN_POINT ( 'NONE',  ( 0.3045634402744727964, -4.096074720329294649, -9.425384029459461743 ) ) ;
#12429=EDGE_LOOP ( 'NONE', ( #30757, #524, #33002, #17447 ) ) ;
#12431=PRODUCT ( 'Part3_SlicingGear', 'Part3_SlicingGear', '', ( #19706 ) ) ;
#12437=CIRCLE ( 'NONE', #11364, 8.749000000000002331 ) ;
#12446=CARTESIAN_POINT ( 'NONE',  ( 0.000000000000000000, 0.000000000000000000, 0.000000000000000000 ) ) ;
#12452=FACE_OUTER_BOUND ( 'NONE', #23239, .T. ) ;
#12459=ADVANCED_FACE ( 'NONE', ( #3063 ), #31145, .T. ) ;
#12461=VERTEX_POINT ( 'NONE', #25603 ) ;
#12465=CARTESIAN_POINT ( 'NONE',  ( 0.3749742847179773353, 3.955024136977333793, 9.289351359934620689 ) ) ;
#12466=CARTESIAN_POINT ( 'NONE',  ( 0.000000000000000000, 9.241976615262160522, -1.699438267350404930 ) ) ;
#12469=DIRECTION ( 'NONE',  ( 0.000000000000000000, 0.000000000000000000, 1.000000000000000000 ) ) ;
#12470=DIRECTION ( 'NONE',  ( 1.000000000000000000, 0.000000000000000000, 0.000000000000000000 ) ) ;
#12473=ORIENTED_EDGE ( 'NONE', *, *, #15001, .F. ) ;
#12480=VERTEX_POINT ( 'NONE', #10403 ) ;
#12490=DIRECTION ( 'NONE',  ( 0.000000000000000000, 0.000000000000000000, 1.000000000000000000 ) ) ;
#12494=CARTESIAN_POINT ( 'NONE',  ( 0.6728000631949255794, 0.5626559339000506421, -9.133409206458198426 ) ) ;
#12506=ORIENTED_EDGE ( 'NONE', *, *, #21300, .T. ) ;
#12511=CYLINDRICAL_SURFACE ( 'NONE', #16727, 11.00000000000000000 ) ;
#12521=CARTESIAN_POINT ( 'NONE',  ( 0.5032040568826979809, 8.283195248915220077, -5.109302080990099526 ) ) ;
#12525=DIRECTION ( 'NONE',  ( 0.000000000000000000, 0.000000000000000000, 1.000000000000000000 ) ) ;
#12529=ORIENTED_EDGE ( 'NONE', *, *, #886, .T. ) ;
#12538=CARTESIAN_POINT ( 'NONE',  ( 2.274274201627372705, 7.593217523255878731, 7.958834565715730669 ) ) ;
#12539=CARTESIAN_POINT ( 'NONE',  ( 2.857987896746965184, -9.278099925236423573, -2.305585824582613519 ) ) ;
#12549=ORIENTED_EDGE ( 'NONE', *, *, #13272, .T. ) ;
#12550=CARTESIAN_POINT ( 'NONE',  ( 3.063284526839887167, 8.461683424509313767, 2.223716399045601921 ) ) ;
#12559=ORIENTED_EDGE ( 'NONE', *, *, #23112, .T. ) ;
#12567=CARTESIAN_POINT ( 'NONE',  ( 0.000000000000000000, 0.000000000000000000, 0.000000000000000000 ) ) ;
#12571=EDGE_CURVE ( 'NONE', #9130, #18033, #26392, .T. ) ;
#12589=EDGE_LOOP ( 'NONE', ( #5087, #24653, #3820, #7411 ) ) ;
#12591=EDGE_LOOP ( 'NONE', ( #64, #26048, #29631, #27577, #17408 ) ) ;
#12592=CARTESIAN_POINT ( 'NONE',  ( 0.3749742847181603556, -3.955024136976903470, -9.289351359934268970 ) ) ;
#12600=CARTESIAN_POINT ( 'NONE',  ( -7.000050800000001239, 0.000000000000000000, 3.499999999999999556 ) ) ;
#12601=EDGE_CURVE ( 'NONE', #16746, #8190, #16209, .T. ) ;
#12622=CARTESIAN_POINT ( 'NONE',  ( 3.063284526839887167, 0.000000000000000000, 0.000000000000000000 ) ) ;
#12630=DIRECTION ( 'NONE',  ( -1.000000000000000000, -0.000000000000000000, 0.000000000000000000 ) ) ;
#12634=ORIENTED_EDGE ( 'NONE', *, *, #353, .T. ) ;
#12639=CARTESIAN_POINT ( 'NONE',  ( 4.546085788309846232E-16, -9.884132761439026638, -4.709950686174718903 ) ) ;
#12656=ORIENTED_EDGE ( 'NONE', *, *, #17169, .F. ) ;
#12664=CARTESIAN_POINT ( 'NONE',  ( 3.063284526839887167, -3.174628368996133432, 8.152713396088751452 ) ) ;
#12665=DIRECTION ( 'NONE',  ( -1.000000000000000000, 0.000000000000000000, -0.000000000000000000 ) ) ;
#12670=ADVANCED_FACE ( 'NONE', ( #1823 ), #26700, .F. ) ;
#12672=CARTESIAN_POINT ( 'NONE',  ( 0.7632845268429988561, 7.360373001717848140, -4.729683950891435451 ) ) ;
#12683=CARTESIAN_POINT ( 'NONE',  ( 3.250000000000001332, 0.000000000000000000, -7.000000000000000888 ) ) ;
#12686=ORIENTED_EDGE ( 'NONE', *, *, #23933, .T. ) ;
#12687=CARTESIAN_POINT ( 'NONE',  ( 0.3076689118679166723, 4.089891983576842804, -9.439351442243262724 ) ) ;
#12692=EDGE_CURVE ( 'NONE', #32326, #3441, #6093, .T. ) ;
#12698=CARTESIAN_POINT ( 'NONE',  ( 0.7632845268398871230, 0.000000000000000000, 0.000000000000000000 ) ) ;
#12703=ORIENTED_EDGE ( 'NONE', *, *, #21484, .T. ) ;
#12704=EDGE_CURVE ( 'NONE', #30416, #17249, #21024, .T. ) ;
#12707=CARTESIAN_POINT ( 'NONE',  ( 0.000000000000000000, -10.82112760146734587, -1.975651141462354987 ) ) ;
#12711=ORIENTED_EDGE ( 'NONE', *, *, #13816, .F. ) ;
#12725=CARTESIAN_POINT ( 'NONE',  ( 2.494102553062040428, 10.32114304930246540, 2.161619314007376058 ) ) ;
#12728=DIRECTION ( 'NONE',  ( 0.000000000000000000, 0.5877852522924684742, 0.8090169943749507819 ) ) ;
#12744=CARTESIAN_POINT ( 'NONE',  ( 2.357329895872532610, 1.335530315079654917, -10.75444571268653249 ) ) ;
#12750=CARTESIAN_POINT ( 'NONE',  ( 0.000000000000000000, -4.472189673936843413, 8.264486777890091673 ) ) ;
#12756=CARTESIAN_POINT ( 'NONE',  ( 0.000000000000000000, 0.000000000000000000, 0.000000000000000000 ) ) ;
#12759=CARTESIAN_POINT ( 'NONE',  ( -3.687509558818933845E-13, 7.944914065997426889, -7.533794289458821680 ) ) ;
#12769=DIRECTION ( 'NONE',  ( -1.000000000000000000, -0.000000000000000000, 0.000000000000000000 ) ) ;
#12771=VERTEX_POINT ( 'NONE', #4493 ) ;
#12773=CARTESIAN_POINT ( 'NONE',  ( 2.589202944057211742, 7.715757980413557426, 6.846250362091539365 ) ) ;
#12775=VERTEX_POINT ( 'NONE', #17848 ) ;
#12782=AXIS2_PLACEMENT_3D ( 'NONE', #6606, #4754, #30191 ) ;
#12785=CARTESIAN_POINT ( 'NONE',  ( 0.5032040285305338090, -9.002252291025264697, -3.698073368203398825 ) ) ;
#12802=ORIENTED_EDGE ( 'NONE', *, *, #23011, .T. ) ;
#12807=CIRCLE ( 'NONE', #5869, 7.000000000000000888 ) ;
#12813=CARTESIAN_POINT ( 'NONE',  ( 0.6424020794401417156, -8.982780240576513364, 2.300561732649537561 ) ) ;
#12820=CIRCLE ( 'NONE', #12302, 10.94895958125474245 ) ;
#12821=DIRECTION ( 'NONE',  ( -1.000000000000000000, -0.000000000000000000, -0.000000000000000000 ) ) ;
#12823=FACE_OUTER_BOUND ( 'NONE', #26602, .T. ) ;
#12826=AXIS2_PLACEMENT_3D ( 'NONE', #19676, #29869, #21009 ) ;
#12834=ORIENTED_EDGE ( 'NONE', *, *, #9062, .T. ) ;
#12843=CARTESIAN_POINT ( 'NONE',  ( 0.08034253656881387706, 5.242601083769395487, -9.429377841196931342 ) ) ;
#12857=CARTESIAN_POINT ( 'NONE',  ( 0.6903785682175527239, -7.668066208469608291, 4.901993410350687697 ) ) ;
#12864=ORIENTED_EDGE ( 'NONE', *, *, #6356, .T. ) ;
#12881=DIRECTION ( 'NONE',  ( -1.000000000000000000, 0.000000000000000000, 0.000000000000000000 ) ) ;
#12912=AXIS2_PLACEMENT_3D ( 'NONE', #5409, #20783, #30986 ) ;
#12934=CARTESIAN_POINT ( 'NONE',  ( 0.2099939045493650069, -10.28101406640744209, 2.171920878037989056 ) ) ;
#12947=CARTESIAN_POINT ( 'NONE',  ( 0.4370649308509315101, 8.480516373469937363, 5.155378858006763210 ) ) ;
#12960=DIRECTION ( 'NONE',  ( -1.000000000000000000, -0.000000000000000000, 0.000000000000000000 ) ) ;
#12962=AXIS2_PLACEMENT_3D ( 'NONE', #20979, #5266, #25650 ) ;
#12966=AXIS2_PLACEMENT_3D ( 'NONE', #9467, #22348, #9629 ) ;
#12983=AXIS2_PLACEMENT_3D ( 'NONE', #25367, #9464, #12490 ) ;
#12995=DIRECTION ( 'NONE',  ( 1.000000000000000000, 0.000000000000000000, 0.000000000000000000 ) ) ;
#12998=ORIENTED_EDGE ( 'NONE', *, *, #22927, .T. ) ;
#13011=CARTESIAN_POINT ( 'NONE',  ( 2.857987933995208785, -0.6743480930025086417, -9.536462466387789050 ) ) ;
#13017=CARTESIAN_POINT ( 'NONE',  ( 0.3749743454410884302, -9.839947797887033332, -2.260462012960365197 ) ) ;
#13023=CARTESIAN_POINT ( 'NONE',  ( 2.592584512312225975, 0.9926283730735776523, 10.27797909968510126 ) ) ;
#13032=ADVANCED_FACE ( 'NONE', ( #31528 ), #13147, .T. ) ;
#13039=CARTESIAN_POINT ( 'NONE',  ( 3.063284526846072442, -8.461683424479964799, -2.223716399039827429 ) ) ;
#13047=VERTEX_POINT ( 'NONE', #28546 ) ;
#13048=DIRECTION ( 'NONE',  ( 0.000000000000000000, 0.000000000000000000, 1.000000000000000000 ) ) ;
#13053=ADVANCED_FACE ( 'NONE', ( #31715 ), #14432, .T. ) ;
#13061=DIRECTION ( 'NONE',  ( 0.000000000000000000, 0.000000000000000000, -1.000000000000000000 ) ) ;
#13064=LINE ( 'NONE', #367, #32143 ) ;
#13089=DIRECTION ( 'NONE',  ( 0.000000000000000000, 0.000000000000000000, -1.000000000000000000 ) ) ;
#13109=DIRECTION ( 'NONE',  ( 0.000000000000000000, 0.000000000000000000, 1.000000000000000000 ) ) ;
#13131=ORIENTED_EDGE ( 'NONE', *, *, #22622, .T. ) ;
#13134=ORIENTED_EDGE ( 'NONE', *, *, #26052, .T. ) ;
#13147=CYLINDRICAL_SURFACE ( 'NONE', #785, 11.00000000000000000 ) ;
#13151=DIRECTION ( 'NONE',  ( -1.000000000000000000, 0.000000000000000000, -0.000000000000000000 ) ) ;
#13154=EDGE_LOOP ( 'NONE', ( #2185, #4222, #27605, #30121 ) ) ;
#13163=CYLINDRICAL_SURFACE ( 'NONE', #23037, 8.749000000000002331 ) ;
#13171=ORIENTED_EDGE ( 'NONE', *, *, #14208, .F. ) ;
#13173=DIRECTION ( 'NONE',  ( 0.000000000000000000, 0.000000000000000000, -1.000000000000000000 ) ) ;
#13187=DIRECTION ( 'NONE',  ( 0.000000000000000000, 0.000000000000000000, 1.000000000000000000 ) ) ;
#13190=DIRECTION ( 'NONE',  ( -1.000000000000000000, 0.000000000000000000, 0.000000000000000000 ) ) ;
#13231=DIRECTION ( 'NONE',  ( 0.000000000000000000, 0.000000000000000000, -1.000000000000000000 ) ) ;
#13242=CARTESIAN_POINT ( 'NONE',  ( 3.249999999999999556, 9.314797388894893615, 5.239665997526921082 ) ) ;
#13244=ORIENTED_EDGE ( 'NONE', *, *, #3809, .F. ) ;
#13259=DIRECTION ( 'NONE',  ( -1.000000000000000000, 0.000000000000000000, 0.000000000000000000 ) ) ;
#13264=EDGE_CURVE ( 'NONE', #979, #32109, #32557, .T. ) ;
#13266=ORIENTED_EDGE ( 'NONE', *, *, #17256, .F. ) ;
#13272=EDGE_CURVE ( 'NONE', #31785, #7245, #4449, .T. ) ;
#13273=ORIENTED_EDGE ( 'NONE', *, *, #2224, .T. ) ;
#13289=ORIENTED_EDGE ( 'NONE', *, *, #11405, .F. ) ;
#13311=CARTESIAN_POINT ( 'NONE',  ( 0.7212197813471248331, 8.337493976377276184, 3.259817272365101104 ) ) ;
#13316=DIRECTION ( 'NONE',  ( 1.000000000000000000, -0.000000000000000000, 0.000000000000000000 ) ) ;
#13320=CIRCLE ( 'NONE', #5861, 10.94895958125474245 ) ;
#13325=CARTESIAN_POINT ( 'NONE',  ( -10.00000000000000000, 0.000000000000000000, 0.000000000000000000 ) ) ;
#13335=CARTESIAN_POINT ( 'NONE',  ( 0.3076688774149766159, 2.239519426675734337, 10.04057401064416233 ) ) ;
#13337=EDGE_CURVE ( 'NONE', #18655, #5149, #273, .T. ) ;
#13361=ORIENTED_EDGE ( 'NONE', *, *, #20031, .T. ) ;
#13366=DIRECTION ( 'NONE',  ( 0.000000000000000000, 0.000000000000000000, -1.000000000000000000 ) ) ;
#13369=DIRECTION ( 'NONE',  ( 0.000000000000000000, -1.865174681370262988E-14, 1.000000000000000000 ) ) ;
#13370=AXIS2_PLACEMENT_3D ( 'NONE', #12135, #24491, #22008 ) ;
#13379=ORIENTED_EDGE ( 'NONE', *, *, #15336, .T. ) ;
#13384=CARTESIAN_POINT ( 'NONE',  ( 3.020080181661099594, 8.342499971033895179, -3.262125172873930001 ) ) ;
#13390=CARTESIAN_POINT ( 'NONE',  ( 2.274274201625327230, 0.000000000000000000, 0.000000000000000000 ) ) ;
#13395=ORIENTED_EDGE ( 'NONE', *, *, #28198, .F. ) ;
#13403=ORIENTED_EDGE ( 'NONE', *, *, #6327, .F. ) ;
#13409=CARTESIAN_POINT ( 'NONE',  ( 2.857987970437214198, 3.588272043371452114, 8.861329655870052946 ) ) ;
#13411=DIRECTION ( 'NONE',  ( 1.000000000000000000, -0.000000000000000000, -0.000000000000000000 ) ) ;
#13446=EDGE_LOOP ( 'NONE', ( #9032, #9380, #8600, #3571 ) ) ;
#13449=ORIENTED_EDGE ( 'NONE', *, *, #12047, .T. ) ;
#13459=FACE_OUTER_BOUND ( 'NONE', #2429, .T. ) ;
#13464=EDGE_CURVE ( 'NONE', #4033, #2323, #1239, .T. ) ;
#13467=FACE_OUTER_BOUND ( 'NONE', #21928, .T. ) ;
#13472=ADVANCED_FACE ( 'NONE', ( #21452 ), #1884, .F. ) ;
#13496=ORIENTED_EDGE ( 'NONE', *, *, #16890, .F. ) ;
#13516=CARTESIAN_POINT ( 'NONE',  ( 0.5032039771612126788, 2.299586922890515694, 9.456648240374278203 ) ) ;
#13526=AXIS2_PLACEMENT_3D ( 'NONE', #19194, #16356, #31764 ) ;
#13533=ORIENTED_EDGE ( 'NONE', *, *, #20041, .F. ) ;
#13534=DIRECTION ( 'NONE',  ( 0.000000000000000000, 0.000000000000000000, 1.000000000000000000 ) ) ;
#13542=CARTESIAN_POINT ( 'NONE',  ( 0.000000000000000000, -8.264486777890139635, 4.472189673936756371 ) ) ;
#13560=DIRECTION ( 'NONE',  ( -1.000000000000000000, 0.000000000000000000, 0.000000000000000000 ) ) ;
#13593=DIRECTION ( 'NONE',  ( 1.000000000000000000, -0.000000000000000000, -0.000000000000000000 ) ) ;
#13596=ORIENTED_EDGE ( 'NONE', *, *, #4534, .F. ) ;
#13610=FACE_OUTER_BOUND ( 'NONE', #25706, .T. ) ;
#13613=ORIENTED_EDGE ( 'NONE', *, *, #7159, .F. ) ;
#13615=CARTESIAN_POINT ( 'NONE',  ( 2.866494652514124830, 9.241976615262203154, 2.300561732649596181 ) ) ;
#13622=DIRECTION ( 'NONE',  ( 1.000000000000000000, -0.000000000000000000, -0.000000000000000000 ) ) ;
#13628=CARTESIAN_POINT ( 'NONE',  ( 3.063284526845909017, -8.734705317652711187, 0.4999240074859884198 ) ) ;
#13633=CARTESIAN_POINT ( 'NONE',  ( -3.688478485700421711E-13, 5.227991826304162259, -9.620177616658798669 ) ) ;
#13660=CARTESIAN_POINT ( 'NONE',  ( 0.3045634671934228099, 10.22982953726899780, -0.9829946734957932808 ) ) ;
#13662=CARTESIAN_POINT ( 'NONE',  ( 3.249999999999999556, 0.000000000000000000, -6.999999999999998224 ) ) ;
#13689=DIRECTION ( 'NONE',  ( -1.000000000000000000, -0.000000000000000000, -0.000000000000000000 ) ) ;
#13697=B_SPLINE_CURVE_WITH_KNOTS ( 'NONE', 3,
 ( #13805, #3649, #16838, #19175, #29367, #4137, #22022, #24198 ),
 .UNSPECIFIED., .F., .F.,
 ( 4, 2, 2, 4 ),
 ( 2.304311362615608600E-07, 0.001261163669367360842, 0.001891630288482910351, 0.002522096907598460076 ),
 .UNSPECIFIED. ) ;
#13708=ADVANCED_FACE ( 'NONE', ( #19915 ), #27430, .T. ) ;
#13714=CARTESIAN_POINT ( 'NONE',  ( 2.970200414851740245, -2.288523046050797038, 8.870914041964226726 ) ) ;
#13722=CARTESIAN_POINT ( 'NONE',  ( 2.970200448035948959, 8.521880193026294847, -3.362738345043123633 ) ) ;
#13733=DIRECTION ( 'NONE',  ( 0.000000000000000000, 0.000000000000000000, 1.000000000000000000 ) ) ;
#13738=CYLINDRICAL_SURFACE ( 'NONE', #4903, 11.00000000000000000 ) ;
#13743=DIRECTION ( 'NONE',  ( 1.000000000000000000, -0.000000000000000000, -0.000000000000000000 ) ) ;
#13745=ORIENTED_EDGE ( 'NONE', *, *, #26538, .T. ) ;
#13758=ORIENTED_EDGE ( 'NONE', *, *, #4240, .F. ) ;
#13767=ORIENTED_EDGE ( 'NONE', *, *, #27535, .F. ) ;
#13799=FACE_OUTER_BOUND ( 'NONE', #7801, .T. ) ;
#13805=CARTESIAN_POINT ( 'NONE',  ( 3.063284526839887167, -4.729683950898817102, -7.360373001730970977 ) ) ;
#13811=DIRECTION ( 'NONE',  ( -1.000000000000000000, 0.000000000000000000, 0.000000000000000000 ) ) ;
#13816=EDGE_CURVE ( 'NONE', #25039, #3168, #23839, .T. ) ;
#13821=B_SPLINE_CURVE_WITH_KNOTS ( 'NONE', 3,
 ( #15294, #30207, #20161, #12465, #283, #2100, #9791, #20321 ),
 .UNSPECIFIED., .F., .F.,
 ( 4, 2, 2, 4 ),
 ( 2.213836054398032120E-07, 0.001227982086136578848, 0.001841862437402149106, 0.002455742788667719147 ),
 .UNSPECIFIED. ) ;
#13833=CARTESIAN_POINT ( 'NONE',  ( 3.063284526839887167, 0.000000000000000000, -8.749000000000004107 ) ) ;
#13835=CIRCLE ( 'NONE', #14921, 4.000000000000000888 ) ;
#13847=DIRECTION ( 'NONE',  ( 1.000000000000000000, 0.000000000000000000, 0.000000000000000000 ) ) ;
#13851=B_SPLINE_CURVE_WITH_KNOTS ( 'NONE', 3,
 ( #2468, #5287, #20827, #12785, #28536, #4969, #28344, #30373 ),
 .UNSPECIFIED., .F., .F.,
 ( 4, 2, 2, 4 ),
 ( 5.099451029780936180E-07, 0.001229189756360174034, 0.001843529661988772611, 0.002457869567617371187 ),
 .UNSPECIFIED. ) ;
#13854=DIRECTION ( 'NONE',  ( 0.000000000000000000, 0.000000000000000000, -1.000000000000000000 ) ) ;
#13855=ORIENTED_EDGE ( 'NONE', *, *, #24252, .T. ) ;
#13858=EDGE_CURVE ( 'NONE', #25356, #6749, #27683, .T. ) ;
#13863=CYLINDRICAL_SURFACE ( 'NONE', #26345, 4.000000000000001776 ) ;
#13864=CIRCLE ( 'NONE', #4803, 8.999999999999998224 ) ;
#13865=B_SPLINE_CURVE_WITH_KNOTS ( 'NONE', 3,
 ( #17691, #20067, #13023, #23229, #166, #22881, #33083, #20719 ),
 .UNSPECIFIED., .F., .F.,
 ( 4, 2, 2, 4 ),
 ( 2.851296420411806090E-07, 0.001262135616826462903, 0.001893060860418671653, 0.002523986104010880402 ),
 .UNSPECIFIED. ) ;
#13872=DIRECTION ( 'NONE',  ( 1.000000000000000000, -0.000000000000000000, -0.000000000000000000 ) ) ;
#13879=CYLINDRICAL_SURFACE ( 'NONE', #26297, 11.00000000000000000 ) ;
#13896=EDGE_CURVE ( 'NONE', #28781, #2837, #1969, .T. ) ;
#13898=CARTESIAN_POINT ( 'NONE',  ( 3.063284526846069777, -2.223716399039799452, 8.461683424479977234 ) ) ;
#13903=DIRECTION ( 'NONE',  ( 0.000000000000000000, 0.000000000000000000, 1.000000000000000000 ) ) ;
#13905=CIRCLE ( 'NONE', #14433, 10.99999999999999822 ) ;
#13917=EDGE_LOOP ( 'NONE', ( #28599, #5356, #31617, #32168 ) ) ;
#13920=ORIENTED_EDGE ( 'NONE', *, *, #17491, .F. ) ;
#13928=FACE_OUTER_BOUND ( 'NONE', #31113, .T. ) ;
#13932=DIRECTION ( 'NONE',  ( -1.000000000000000000, 0.000000000000000000, -0.000000000000000000 ) ) ;
#13933=CARTESIAN_POINT ( 'NONE',  ( 2.795120501770171018, 5.116149273379854812, -8.308193303472245717 ) ) ;
#13937=CIRCLE ( 'NONE', #4357, 10.94895958125474245 ) ;
#13938=ADVANCED_FACE ( 'NONE', ( #6795 ), #22340, .T. ) ;
#13944=AXIS2_PLACEMENT_3D ( 'NONE', #29554, #6151, #18860 ) ;
#13955=DIRECTION ( 'NONE',  ( 0.000000000000000000, 0.000000000000000000, 1.000000000000000000 ) ) ;
#13961=ORIENTED_EDGE ( 'NONE', *, *, #16319, .T. ) ;
#13972=CARTESIAN_POINT ( 'NONE',  ( 2.437082530871053532, 5.244446742619491175, 9.289394354155787070 ) ) ;
#13975=EDGE_CURVE ( 'NONE', #17287, #6932, #3265, .T. ) ;
#13988=CARTESIAN_POINT ( 'NONE',  ( 2.661997913519430714, -2.255009087902858589, -9.876677602395409039 ) ) ;
#13991=CIRCLE ( 'NONE', #21486, 4.000000000000001776 ) ;
#13999=CYLINDRICAL_SURFACE ( 'NONE', #25255, 4.000000000000001776 ) ;
#14007=VERTEX_POINT ( 'NONE', #10118 ) ;
#14014=CIRCLE ( 'NONE', #19362, 8.749000000000002331 ) ;
#14016=CIRCLE ( 'NONE', #30071, 4.000000000000001776 ) ;
#14017=VECTOR ( 'NONE', #23729, 1000.000000000000000 ) ;
#14029=CARTESIAN_POINT ( 'NONE',  ( 0.000000000000000000, 0.000000000000000000, 0.000000000000000000 ) ) ;
#14034=FACE_OUTER_BOUND ( 'NONE', #17430, .T. ) ;
#14035=CARTESIAN_POINT ( 'NONE',  ( 3.249999999999999556, 0.000000000000000000, 0.000000000000000000 ) ) ;
#14036=EDGE_LOOP ( 'NONE', ( #25377, #7249, #13379, #12711, #19291 ) ) ;
#14040=AXIS2_PLACEMENT_3D ( 'NONE', #19009, #32844, #13955 ) ;
#14049=CARTESIAN_POINT ( 'NONE',  ( 3.249999999999999556, 9.314797388894893615, 1.239665997526919972 ) ) ;
#14050=AXIS2_PLACEMENT_3D ( 'NONE', #30943, #684, #28601 ) ;
#14066=ORIENTED_EDGE ( 'NONE', *, *, #613, .F. ) ;
#14067=DIRECTION ( 'NONE',  ( -1.000000000000000000, 0.000000000000000000, 0.000000000000000000 ) ) ;
#14072=VECTOR ( 'NONE', #20987, 1000.000000000000000 ) ;
#14073=EDGE_CURVE ( 'NONE', #17287, #30501, #29825, .T. ) ;
#14075=DIRECTION ( 'NONE',  ( 1.000000000000000000, 0.000000000000000000, 0.000000000000000000 ) ) ;
#14077=ORIENTED_EDGE ( 'NONE', *, *, #21661, .F. ) ;
#14081=B_SPLINE_CURVE_WITH_KNOTS ( 'NONE', 3,
 ( #3317, #23032, #153, #25897, #13011, #10338, #7984, #20553 ),
 .UNSPECIFIED., .F., .F.,
 ( 4, 2, 2, 4 ),
 ( 2.851296507433586163E-07, 0.001262135616845464631, 0.001893060860442827460, 0.002523986104040190290 ),
 .UNSPECIFIED. ) ;
#14088=FACE_OUTER_BOUND ( 'NONE', #18323, .T. ) ;
#14115=CARTESIAN_POINT ( 'NONE',  ( 2.274274201625327230, -9.680994141368730155, -5.222868219166962866 ) ) ;
#14116=CARTESIAN_POINT ( 'NONE',  ( -3.671333707197877479E-13, 1.999317321091317545, -10.76487093102143433 ) ) ;
#14130=LINE ( 'NONE', #6272, #26762 ) ;
#14144=ORIENTED_EDGE ( 'NONE', *, *, #14073, .T. ) ;
#14163=DIRECTION ( 'NONE',  ( 1.000000000000000000, -0.000000000000000000, -0.000000000000000000 ) ) ;
#14166=DIRECTION ( 'NONE',  ( -1.000000000000000000, 0.000000000000000000, -0.000000000000000000 ) ) ;
#14167=CARTESIAN_POINT ( 'NONE',  ( 3.249999999999999556, 0.000000000000000000, 0.000000000000000000 ) ) ;
#14168=ORIENTED_EDGE ( 'NONE', *, *, #25213, .F. ) ;
#14183=PLANE ( 'NONE',  #10151 ) ;
#14184=ORIENTED_EDGE ( 'NONE', *, *, #31416, .T. ) ;
#14192=B_SPLINE_CURVE_WITH_KNOTS ( 'NONE', 3,
 ( #7853, #15525, #17708, #5033, #2677, #15211, #12843, #2870 ),
 .UNSPECIFIED., .F., .F.,
 ( 4, 2, 2, 4 ),
 ( 2.304311362615608600E-07, 0.001227991214883613832, 0.001841871606757292763, 0.002455751998630971693 ),
 .UNSPECIFIED. ) ;
#14197=DIRECTION ( 'NONE',  ( 0.000000000000000000, 0.000000000000000000, -1.000000000000000000 ) ) ;
#14208=EDGE_CURVE ( 'NONE', #448, #14007, #9070, .T. ) ;
#14213=CARTESIAN_POINT ( 'NONE',  ( 2.274274201625327230, 5.222868219166857173, 9.680994141368788775 ) ) ;
#14227=CARTESIAN_POINT ( 'NONE',  ( 2.425585535379221280, -9.314797388879910045, 5.239665997526856245 ) ) ;
#14239=ADVANCED_FACE ( 'NONE', ( #17881 ), #5171, .T. ) ;
#14244=ORIENTED_EDGE ( 'NONE', *, *, #17256, .T. ) ;
#14245=CARTESIAN_POINT ( 'NONE',  ( 0.7632845268398871230, 0.000000000000000000, 0.000000000000000000 ) ) ;
#14247=CARTESIAN_POINT ( 'NONE',  ( 0.000000000000000000, 0.000000000000000000, 0.000000000000000000 ) ) ;
#14251=CARTESIAN_POINT ( 'NONE',  ( -10.00000000000000000, 0.000000000000000000, 0.000000000000000000 ) ) ;
#14252=CARTESIAN_POINT ( 'NONE',  ( 2.437082427505627091, 9.703015696712945726, 4.432669656489494514 ) ) ;
#14281=CARTESIAN_POINT ( 'NONE',  ( 3.063284526839887167, -2.223716399045513992, -8.461683424509338636 ) ) ;
#14286=CARTESIAN_POINT ( 'NONE',  ( 0.000000000000000000, 0.000000000000000000, 0.000000000000000000 ) ) ;
#14294=ORIENTED_EDGE ( 'NONE', *, *, #31668, .T. ) ;
#14300=CARTESIAN_POINT ( 'NONE',  ( 3.063284526839887167, -0.4999240074895051067, 8.734705317681624948 ) ) ;
#14307=ORIENTED_EDGE ( 'NONE', *, *, #24268, .T. ) ;
#14312=CARTESIAN_POINT ( 'NONE',  ( 0.5032039692148283505, 9.704418393831403478, 0.7352278974741125461 ) ) ;
#14313=EDGE_CURVE ( 'NONE', #10741, #3275, #13865, .T. ) ;
#14314=DIRECTION ( 'NONE',  ( -1.000000000000000000, -0.000000000000000000, -0.000000000000000000 ) ) ;
#14317=DIRECTION ( 'NONE',  ( 1.000000000000000000, 0.000000000000000000, 0.000000000000000000 ) ) ;
#14326=ORIENTED_EDGE ( 'NONE', *, *, #29744, .F. ) ;
#14334=VERTEX_POINT ( 'NONE', #10352 ) ;
#14335=PLANE ( 'NONE',  #29523 ) ;
#14343=CARTESIAN_POINT ( 'NONE',  ( 2.864530875629061057, -9.539603485476147782, -0.6595692664038580455 ) ) ;
#14346=ADVANCED_FACE ( 'NONE', ( #5019 ), #30771, .T. ) ;
#14351=ADVANCED_FACE ( 'NONE', ( #25724 ), #5512, .T. ) ;
#14354=CARTESIAN_POINT ( 'NONE',  ( 2.857987970441411729, -3.588272043362970898, -8.861329655858744658 ) ) ;
#14373=ORIENTED_EDGE ( 'NONE', *, *, #1623, .T. ) ;
#14384=ORIENTED_EDGE ( 'NONE', *, *, #5111, .T. ) ;
#14386=VECTOR ( 'NONE', #12960, 1000.000000000000000 ) ;
#14388=B_SPLINE_CURVE_WITH_KNOTS ( 'NONE', 3,
 ( #24288, #3732, #11247, #16418, #21938, #21451, #6233, #31828 ),
 .UNSPECIFIED., .F., .F.,
 ( 4, 2, 2, 4 ),
 ( 2.213836054374538867E-07, 0.001261154818855340096, 0.001891621536480290978, 0.002522088254105242077 ),
 .UNSPECIFIED. ) ;
#14392=CARTESIAN_POINT ( 'NONE',  ( 0.1606233661161337867, -7.161985370900606718, 7.854816391753094429 ) ) ;
#14396=CARTESIAN_POINT ( 'NONE',  ( -10.00000000000000000, 0.000000000000000000, 0.000000000000000000 ) ) ;
#14400=CIRCLE ( 'NONE', #31529, 6.000000000000000888 ) ;
#14412=ORIENTED_EDGE ( 'NONE', *, *, #30395, .F. ) ;
#14416=ORIENTED_EDGE ( 'NONE', *, *, #27126, .F. ) ;
#14419=ADVANCED_FACE ( 'NONE', ( #20870 ), #18211, .T. ) ;
#14423=CARTESIAN_POINT ( 'NONE',  ( 0.000000000000000000, 4.472189673936902032, -8.264486777890061475 ) ) ;
#14425=EDGE_CURVE ( 'NONE', #17751, #1971, #6303, .T. ) ;
#14426=CYLINDRICAL_SURFACE ( 'NONE', #537, 6.999999999999998224 ) ;
#14429=CIRCLE ( 'NONE', #52, 11.00000000000000000 ) ;
#14432=CYLINDRICAL_SURFACE ( 'NONE', #32291, 8.749000000000002331 ) ;
#14433=AXIS2_PLACEMENT_3D ( 'NONE', #21310, #8924, #6602 ) ;
#14446=FACE_OUTER_BOUND ( 'NONE', #883, .T. ) ;
#14448=ORIENTED_EDGE ( 'NONE', *, *, #14855, .T. ) ;
#14449=DIRECTION ( 'NONE',  ( -1.000000000000000000, -0.000000000000000000, -0.000000000000000000 ) ) ;
#14451=B_SPLINE_CURVE_WITH_KNOTS ( 'NONE', 3,
 ( #27917, #2519, #12687, #22891, #10173, #15359, #7197, #17892 ),
 .UNSPECIFIED., .F., .F.,
 ( 4, 2, 2, 4 ),
 ( 5.099451029773404998E-07, 0.001229189756374618209, 0.001843529662010439307, 0.002457869567646260404 ),
 .UNSPECIFIED. ) ;
#14452=ORIENTED_EDGE ( 'NONE', *, *, #6755, .T. ) ;
#14463=VECTOR ( 'NONE', #2949, 1000.000000000000000 ) ;
#14469=AXIS2_PLACEMENT_3D ( 'NONE', #24097, #14075, #11723 ) ;
#14473=LINE ( 'NONE', #27187, #18308 ) ;
#14482=CARTESIAN_POINT ( 'NONE',  ( 2.440333653313243367, -9.715096239900898212, 4.424884217110374607 ) ) ;
#14485=DIRECTION ( 'NONE',  ( -1.000000000000000000, 0.000000000000000000, 0.000000000000000000 ) ) ;
#14491=AXIS2_PLACEMENT_3D ( 'NONE', #616, #10807, #18835 ) ;
#14492=AXIS2_PLACEMENT_3D ( 'NONE', #910, #31982, #3913 ) ;
#14519=CIRCLE ( 'NONE', #8658, 9.000000000000001776 ) ;
#14523=DIRECTION ( 'NONE',  ( 0.000000000000000000, 0.000000000000000000, 1.000000000000000000 ) ) ;
#14529=CARTESIAN_POINT ( 'NONE',  ( 2.976845687893340919, -9.149921655307462487, -0.5490754078163497809 ) ) ;
#14530=DIRECTION ( 'NONE',  ( 1.000000000000000000, -0.000000000000000000, -0.000000000000000000 ) ) ;
#14531=AXIS2_PLACEMENT_3D ( 'NONE', #7710, #17905, #7360 ) ;
#14559=AXIS2_PLACEMENT_3D ( 'NONE', #24841, #12470, #7283 ) ;
#14566=DIRECTION ( 'NONE',  ( 0.000000000000000000, 0.000000000000000000, 1.000000000000000000 ) ) ;
#14571=CARTESIAN_POINT ( 'NONE',  ( 2.678494152628110303, -8.648785596948973975, 5.187417801898995151 ) ) ;
#14574=EDGE_LOOP ( 'NONE', ( #19990, #23908, #21783, #14452, #11607 ) ) ;
#14583=ORIENTED_EDGE ( 'NONE', *, *, #20393, .T. ) ;
#14586=CIRCLE ( 'NONE', #200, 6.999999999999998224 ) ;
#14593=ORIENTED_EDGE ( 'NONE', *, *, #23857, .F. ) ;
#14608=DIRECTION ( 'NONE',  ( 0.000000000000000000, 0.000000000000000000, 1.000000000000000000 ) ) ;
#14617=ORIENTED_EDGE ( 'NONE', *, *, #10745, .F. ) ;
#14622=AXIS2_PLACEMENT_3D ( 'NONE', #30663, #10052, #20266 ) ;
#14625=CARTESIAN_POINT ( 'NONE',  ( -1.433134780067091442E-16, -9.620177616658022401, 5.227991826304056566 ) ) ;
#14626=CARTESIAN_POINT ( 'NONE',  ( 0.3749740905863481744, 7.612528756000837227, -6.632019415960804132 ) ) ;
#14640=CARTESIAN_POINT ( 'NONE',  ( 0.000000000000000000, 0.000000000000000000, 0.000000000000000000 ) ) ;
#14651=CARTESIAN_POINT ( 'NONE',  ( 3.249999999999999556, 8.152713396088763886, 3.174628368996105010 ) ) ;
#14654=CARTESIAN_POINT ( 'NONE',  ( 1.624999999999999778, -9.915734732513186600, -4.762163868918378284 ) ) ;
#14676=EDGE_LOOP ( 'NONE', ( #30243, #27358, #27608, #32971, #16665 ) ) ;
#14684=LINE ( 'NONE', #19702, #19375 ) ;
#14693=EDGE_LOOP ( 'NONE', ( #13244, #25629, #17446, #24275 ) ) ;
#14705=ORIENTED_EDGE ( 'NONE', *, *, #18607, .F. ) ;
#14707=VERTEX_POINT ( 'NONE', #6457 ) ;
#14722=CARTESIAN_POINT ( 'NONE',  ( 3.063284526842892319, -5.538577986798981279, -6.772677083981775148 ) ) ;
#14733=EDGE_CURVE ( 'NONE', #4619, #22777, #7591, .T. ) ;
#14743=VERTEX_POINT ( 'NONE', #15784 ) ;
#14744=CARTESIAN_POINT ( 'NONE',  ( 2.437082427505614657, -9.703015696712927962, -4.432669656489585108 ) ) ;
#14747=EDGE_CURVE ( 'NONE', #15147, #4279, #25177, .T. ) ;
#14750=CARTESIAN_POINT ( 'NONE',  ( 0.000000000000000000, 5.222868219166857173, 9.680994141368786998 ) ) ;
#14758=DIRECTION ( 'NONE',  ( 0.000000000000000000, 0.000000000000000000, -1.000000000000000000 ) ) ;
#14762=ORIENTED_EDGE ( 'NONE', *, *, #17033, .T. ) ;
#14763=VERTEX_POINT ( 'NONE', #23624 ) ;
#14766=LINE ( 'NONE', #27490, #28280 ) ;
#14796=CARTESIAN_POINT ( 'NONE',  ( 0.000000000000000000, 0.000000000000000000, 0.000000000000000000 ) ) ;
#14824=EDGE_LOOP ( 'NONE', ( #5830, #31761, #32571, #14904 ) ) ;
#14830=VERTEX_POINT ( 'NONE', #20487 ) ;
#14831=DIRECTION ( 'NONE',  ( 1.000000000000000000, -0.000000000000000000, -0.000000000000000000 ) ) ;
#14841=CARTESIAN_POINT ( 'NONE',  ( 1.624999999999999778, -10.82112760146737962, 1.975651141462197113 ) ) ;
#14851=EDGE_CURVE ( 'NONE', #19087, #596, #20965, .T. ) ;
#14855=EDGE_CURVE ( 'NONE', #30676, #24271, #31184, .T. ) ;
#14857=CARTESIAN_POINT ( 'NONE',  ( 0.000000000000000000, -4.762163868918342757, 9.915734732513202587 ) ) ;
#14866=DIRECTION ( 'NONE',  ( 0.000000000000000000, 0.000000000000000000, 1.000000000000000000 ) ) ;
#14869=ORIENTED_EDGE ( 'NONE', *, *, #15469, .T. ) ;
#14874=DIRECTION ( 'NONE',  ( 0.000000000000000000, 0.000000000000000000, -1.000000000000000000 ) ) ;
#14878=CARTESIAN_POINT ( 'NONE',  ( 0.000000000000000000, 0.000000000000000000, 0.000000000000000000 ) ) ;
#14885=ORIENTED_EDGE ( 'NONE', *, *, #29391, .F. ) ;
#14887=FACE_OUTER_BOUND ( 'NONE', #23662, .T. ) ;
#14893=ADVANCED_FACE ( 'NONE', ( #11570 ), #13738, .T. ) ;
#14898=CARTESIAN_POINT ( 'NONE',  ( 0.000000000000000000, -1.999317321091575561, 10.76487093102064030 ) ) ;
#14904=ORIENTED_EDGE ( 'NONE', *, *, #29524, .F. ) ;
#14913=CARTESIAN_POINT ( 'NONE',  ( 0.5704036742843068275, -3.563415854978262409, -8.851103337321053033 ) ) ;
#14916=CARTESIAN_POINT ( 'NONE',  ( 0.000000000000000000, 0.000000000000000000, 0.000000000000000000 ) ) ;
#14921=AXIS2_PLACEMENT_3D ( 'NONE', #10519, #18048, #28237 ) ;
#14922=VERTEX_POINT ( 'NONE', #24103 ) ;
#14934=CARTESIAN_POINT ( 'NONE',  ( 0.08034255810681184551, 7.899847910286125874, -7.347818361010319599 ) ) ;
#14945=CIRCLE ( 'NONE', #7481, 10.99999999999999822 ) ;
#14974=DIRECTION ( 'NONE',  ( 0.000000000000000000, 0.000000000000000000, -1.000000000000000000 ) ) ;
#14993=AXIS2_PLACEMENT_3D ( 'NONE', #5472, #25873, #7815 ) ;
#15001=EDGE_CURVE ( 'NONE', #22521, #15923, #13937, .T. ) ;
#15017=CARTESIAN_POINT ( 'NONE',  ( 0.000000000000000000, 0.000000000000000000, -6.000000000000000888 ) ) ;
#15023=DIRECTION ( 'NONE',  ( 0.000000000000000000, 0.000000000000000000, -1.000000000000000000 ) ) ;
#15025=CARTESIAN_POINT ( 'NONE',  ( 2.592584712405588299, -10.08167743096628222, -2.232024585011588069 ) ) ;
#15026=CIRCLE ( 'NONE', #10216, 4.000000000000001776 ) ;
#15031=CARTESIAN_POINT ( 'NONE',  ( 3.249999999999999556, -1.239665997526818053, -9.314797388894906049 ) ) ;
#15032=EDGE_CURVE ( 'NONE', #15923, #19457, #21429, .T. ) ;
#15033=CARTESIAN_POINT ( 'NONE',  ( 3.063284526839887167, 0.000000000000000000, 0.000000000000000000 ) ) ;
#15050=EDGE_CURVE ( 'NONE', #19429, #7258, #9178, .T. ) ;
#15058=CARTESIAN_POINT ( 'NONE',  ( 0.7632845268430009655, 4.729683950891516275, 7.360373001717795738 ) ) ;
#15062=ADVANCED_FACE ( 'NONE', ( #17568 ), #22120, .T. ) ;
#15065=DIRECTION ( 'NONE',  ( -1.000000000000000000, 0.000000000000000000, 0.000000000000000000 ) ) ;
#15067=CARTESIAN_POINT ( 'NONE',  ( 0.000000000000000000, -7.593217523260520352, -7.958834565716849774 ) ) ;
#15072=AXIS2_PLACEMENT_3D ( 'NONE', #14167, #19690, #24365 ) ;
#15080=ADVANCED_FACE ( 'NONE', ( #9392 ), #32333, .F. ) ;
#15088=FACE_OUTER_BOUND ( 'NONE', #12189, .T. ) ;
#15092=CARTESIAN_POINT ( 'NONE',  ( 3.249999999999999556, -9.241976615262146311, 2.300561732649529567 ) ) ;
#15097=VERTEX_POINT ( 'NONE', #17265 ) ;
#15103=ORIENTED_EDGE ( 'NONE', *, *, #28362, .T. ) ;
#15108=ORIENTED_EDGE ( 'NONE', *, *, #4534, .T. ) ;
#15118=CARTESIAN_POINT ( 'NONE',  ( 0.1255855353732055757, -9.314797388894898944, 5.239665997526856245 ) ) ;
#15123=CARTESIAN_POINT ( 'NONE',  ( 0.2562068301981437757, 8.982429233983488359, 5.229384870727559864 ) ) ;
#15126=AXIS2_PLACEMENT_3D ( 'NONE', #22940, #10416, #13089 ) ;
#15128=LINE ( 'NONE', #1780, #2819 ) ;
#15147=VERTEX_POINT ( 'NONE', #29646 ) ;
#15150=VERTEX_POINT ( 'NONE', #10892 ) ;
#15156=VECTOR ( 'NONE', #13316, 1000.000000000000000 ) ;
#15157=DIRECTION ( 'NONE',  ( 0.000000000000000000, 0.000000000000000000, -1.000000000000000000 ) ) ;
#15162=ADVANCED_FACE ( 'NONE', ( #14034 ), #16379, .T. ) ;
#15185=B_SPLINE_CURVE_WITH_KNOTS ( 'NONE', 3,
 ( #5044, #30439, #10191, #32960, #12857, #15538 ),
 .UNSPECIFIED., .F., .F.,
 ( 4, 2, 4 ),
 ( 0.0003283404404905848075, 0.001393105083344284116, 0.002457869726197983370 ),
 .UNSPECIFIED. ) ;
#15204=CARTESIAN_POINT ( 'NONE',  ( 2.274274201625313907, -9.915734732513202587, -4.762163868918404930 ) ) ;
#15211=CARTESIAN_POINT ( 'NONE',  ( 0.1574692315732393044, 5.243558859478304690, -9.238013023060988260 ) ) ;
#15217=LINE ( 'NONE', #10677, #4985 ) ;
#15223=CARTESIAN_POINT ( 'NONE',  ( 1.624999999999999778, -9.915734732513254102, 4.762163868918234400 ) ) ;
#15238=DIRECTION ( 'NONE',  ( 0.000000000000000000, 0.000000000000000000, 1.000000000000000000 ) ) ;
#15251=ORIENTED_EDGE ( 'NONE', *, *, #8201, .F. ) ;
#15256=PLANE ( 'NONE',  #15126 ) ;
#15268=ADVANCED_FACE ( 'NONE', ( #2166 ), #4933, .T. ) ;
#15279=CARTESIAN_POINT ( 'NONE',  ( 0.1081011292492479320, -10.52678838719862142, 2.097343412299245369 ) ) ;
#15291=DIRECTION ( 'NONE',  ( 0.000000000000000000, 0.000000000000000000, -1.000000000000000000 ) ) ;
#15292=ORIENTED_EDGE ( 'NONE', *, *, #13896, .T. ) ;
#15294=CARTESIAN_POINT ( 'NONE',  ( 0.7632845268398871230, 3.174628368996073924, 8.152713396088772768 ) ) ;
#15300=FACE_OUTER_BOUND ( 'NONE', #5700, .T. ) ;
#15302=CARTESIAN_POINT ( 'NONE',  ( 1.624999999999999778, 4.762163868918416476, -9.915734732513170613 ) ) ;
#15306=EDGE_LOOP ( 'NONE', ( #18079, #12703, #9185, #20978 ) ) ;
#15312=EDGE_CURVE ( 'NONE', #1130, #24626, #27837, .T. ) ;
#15323=CARTESIAN_POINT ( 'NONE',  ( 0.5032039692105046980, -0.7352278974791391919, 9.704418393844074231 ) ) ;
#15335=DIRECTION ( 'NONE',  ( 0.000000000000000000, 1.598721155460225418E-14, 1.000000000000000000 ) ) ;
#15336=EDGE_CURVE ( 'NONE', #10493, #3168, #12187, .T. ) ;
#15359=CARTESIAN_POINT ( 'NONE',  ( 0.6728001046013614150, 3.357496170308760242, -8.512517952453828585 ) ) ;
#15365=CARTESIAN_POINT ( 'NONE',  ( 2.976845726615125809, 2.305279507610603851, 8.871766062375160189 ) ) ;
#15369=VERTEX_POINT ( 'NONE', #19904 ) ;
#15371=EDGE_CURVE ( 'NONE', #31221, #3483, #21461, .T. ) ;
#15378=ORIENTED_EDGE ( 'NONE', *, *, #29744, .T. ) ;
#15417=B_SPLINE_CURVE_WITH_KNOTS ( 'NONE', 3,
 ( #21590, #31798, #20931, #8239, #14354, #24911, #32613, #4187 ),
 .UNSPECIFIED., .F., .F.,
 ( 4, 2, 2, 4 ),
 ( 2.494123658409239446E-07, 0.001262099805927724113, 0.001893025002708666410, 0.002523950199489608925 ),
 .UNSPECIFIED. ) ;
#15432=CARTESIAN_POINT ( 'NONE',  ( 1.624999999999999778, -7.958834565716820464, 7.593217523260554103 ) ) ;
#15435=B_SPLINE_CURVE_WITH_KNOTS ( 'NONE', 3,
 ( #16784, #27299, #21784, #19471, #4083, #11942, #31992, #1253 ),
 .UNSPECIFIED., .F., .F.,
 ( 4, 2, 2, 4 ),
 ( 2.737843117599802759E-07, 0.001261207499628692018, 0.001891674357287159150, 0.002522141214945626715 ),
 .UNSPECIFIED. ) ;
#15461=CARTESIAN_POINT ( 'NONE',  ( 2.274274201625327230, 1.464956435139694868, -10.90201369670497122 ) ) ;
#15465=CARTESIAN_POINT ( 'NONE',  ( -10.00000000000000000, 0.000000000000000000, 0.000000000000000000 ) ) ;
#15468=CYLINDRICAL_SURFACE ( 'NONE', #4784, 8.749000000000002331 ) ;
#15469=EDGE_CURVE ( 'NONE', #10288, #7687, #5178, .T. ) ;
#15482=CIRCLE ( 'NONE', #30441, 10.94895958125474245 ) ;
#15491=ORIENTED_EDGE ( 'NONE', *, *, #5851, .F. ) ;
#15504=DIRECTION ( 'NONE',  ( 0.000000000000000000, 0.000000000000000000, 1.000000000000000000 ) ) ;
#15505=DIRECTION ( 'NONE',  ( 0.000000000000000000, 0.000000000000000000, 1.000000000000000000 ) ) ;
#15511=CARTESIAN_POINT ( 'NONE',  ( 2.357330058169011977, -7.915524238820694336, -7.401770933800325913 ) ) ;
#15515=ORIENTED_EDGE ( 'NONE', *, *, #10780, .T. ) ;
#15520=ORIENTED_EDGE ( 'NONE', *, *, #7159, .T. ) ;
#15525=CARTESIAN_POINT ( 'NONE',  ( 0.6791198416089742063, 4.928602827912397011, -7.715582677071021855 ) ) ;
#15532=CARTESIAN_POINT ( 'NONE',  ( 0.6728000687415542913, 2.287261066729925574, 8.860258565202251191 ) ) ;
#15538=CARTESIAN_POINT ( 'NONE',  ( 0.7632845268398871230, -7.360373001730951437, 4.729683950898845524 ) ) ;
#15549=AXIS2_PLACEMENT_3D ( 'NONE', #25997, #10275, #5263 ) ;
#15551=CARTESIAN_POINT ( 'NONE',  ( -18.30155664144426453, 0.000000000000000000, -3.895301350492843540 ) ) ;
#15564=CIRCLE ( 'NONE', #18764, 10.99999999999999822 ) ;
#15582=ORIENTED_EDGE ( 'NONE', *, *, #14747, .F. ) ;
#15594=VERTEX_POINT ( 'NONE', #833 ) ;
#15602=ORIENTED_EDGE ( 'NONE', *, *, #6548, .T. ) ;
#15607=AXIS2_PLACEMENT_3D ( 'NONE', #15763, #3076, #13231 ) ;
#15610=AXIS2_PLACEMENT_3D ( 'NONE', #1247, #11435, #21630 ) ;
#15611=DIRECTION ( 'NONE',  ( 1.000000000000000000, 0.000000000000000000, 0.000000000000000000 ) ) ;
#15619=CARTESIAN_POINT ( 'NONE',  ( 0.9499999999999995115, 0.000000000000000000, 0.000000000000000000 ) ) ;
#15625=DIRECTION ( 'NONE',  ( 1.000000000000000000, -0.000000000000000000, -0.000000000000000000 ) ) ;
#15634=VECTOR ( 'NONE', #17546, 1000.000000000000000 ) ;
#15640=( NAMED_UNIT ( * ) SI_UNIT ( $, .STERADIAN. ) SOLID_ANGLE_UNIT ( ) );
#15660=AXIS2_PLACEMENT_3D ( 'NONE', #8822, #19027, #29213 ) ;
#15682=CARTESIAN_POINT ( 'NONE',  ( 3.249999999999999556, 9.314797388894893615, 1.239665997526919972 ) ) ;
#15690=ADVANCED_FACE ( 'NONE', ( #6304 ), #11500, .T. ) ;
#15698=EDGE_CURVE ( 'NONE', #30416, #3718, #18205, .T. ) ;
#15717=CARTESIAN_POINT ( 'NONE',  ( 0.7632845268398879002, -8.152713396088778097, 3.174628368996039729 ) ) ;
#15741=ORIENTED_EDGE ( 'NONE', *, *, #23544, .F. ) ;
#15749=CARTESIAN_POINT ( 'NONE',  ( 3.063284526839887167, -3.174628368996133432, 8.152713396088751452 ) ) ;
#15763=CARTESIAN_POINT ( 'NONE',  ( 0.000000000000000000, 1.239665997526887109, 9.314797388894895391 ) ) ;
#15766=CARTESIAN_POINT ( 'NONE',  ( -5.750050799999999462, 0.000000000000000000, 0.000000000000000000 ) ) ;
#15768=EDGE_LOOP ( 'NONE', ( #14617, #18944, #27098, #20523 ) ) ;
#15776=ORIENTED_EDGE ( 'NONE', *, *, #19136, .T. ) ;
#15781=VERTEX_POINT ( 'NONE', #19856 ) ;
#15784=CARTESIAN_POINT ( 'NONE',  ( 0.000000000000000000, -7.593217523260636703, 7.958834565716742304 ) ) ;
#15792=CARTESIAN_POINT ( 'NONE',  ( -7.000050800000001239, 0.000000000000000000, 0.000000000000000000 ) ) ;
#15794=DIRECTION ( 'NONE',  ( 0.000000000000000000, 0.000000000000000000, -1.000000000000000000 ) ) ;
#15797=ORIENTED_EDGE ( 'NONE', *, *, #31668, .F. ) ;
#15800=ORIENTED_EDGE ( 'NONE', *, *, #31917, .F. ) ;
#15844=DIRECTION ( 'NONE',  ( 0.000000000000000000, 0.000000000000000000, 1.000000000000000000 ) ) ;
#15850=DIRECTION ( 'NONE',  ( 1.000000000000000000, -0.000000000000000000, -0.000000000000000000 ) ) ;
#15855=LINE ( 'NONE', #834, #6984 ) ;
#15866=CARTESIAN_POINT ( 'NONE',  ( 2.970200481232438516, -7.729547851449594553, -4.917777846806449915 ) ) ;
#15873=CARTESIAN_POINT ( 'NONE',  ( 0.7632845268398871230, 0.000000000000000000, 8.749000000000002331 ) ) ;
#15874=ORIENTED_EDGE ( 'NONE', *, *, #13337, .F. ) ;
#15875=FACE_OUTER_BOUND ( 'NONE', #29960, .T. ) ;
#15878=ORIENTED_EDGE ( 'NONE', *, *, #24682, .T. ) ;
#15890=APPLICATION_CONTEXT ( 'configuration controlled 3d designs of mechanical parts and assemblies' ) ;
#15894=ORIENTED_EDGE ( 'NONE', *, *, #27058, .F. ) ;
#15897=CARTESIAN_POINT ( 'NONE',  ( 2.692650308882783783, 9.794433827820187233, 2.271349672997489577 ) ) ;
#15905=EDGE_LOOP ( 'NONE', ( #30499, #17783, #919, #11694 ) ) ;
#15908=CARTESIAN_POINT ( 'NONE',  ( 2.857987970437215086, 8.861329655870090249, -3.588272043371362408 ) ) ;
#15914=LINE ( 'NONE', #733, #5467 ) ;
#15923=VERTEX_POINT ( 'NONE', #27691 ) ;
#15940=VERTEX_POINT ( 'NONE', #11294 ) ;
#15949=CARTESIAN_POINT ( 'NONE',  ( 0.000000000000000000, 9.314797388894909602, -1.239665997526784746 ) ) ;
#15954=ORIENTED_EDGE ( 'NONE', *, *, #23890, .F. ) ;
#15968=CARTESIAN_POINT ( 'NONE',  ( 3.063284526839887167, 0.000000000000000000, 0.000000000000000000 ) ) ;
#15995=TOROIDAL_SURFACE ( 'NONE', #30969, 6.923700951379997193, 9.000000000000000000 ) ;
#16005=ORIENTED_EDGE ( 'NONE', *, *, #13975, .T. ) ;
#16008=CARTESIAN_POINT ( 'NONE',  ( 0.7632845268398871230, 8.152713396088806519, -3.174628368995990879 ) ) ;
#16011=CARTESIAN_POINT ( 'NONE',  ( 0.6728000631899151429, -9.133409206477399067, -0.5626559339043897268 ) ) ;
#16031=DIRECTION ( 'NONE',  ( -1.000000000000000000, -0.000000000000000000, -0.000000000000000000 ) ) ;
#16055=B_SPLINE_CURVE_WITH_KNOTS ( 'NONE', 3,
 ( #15749, #28619, #8524, #3694, #24062, #18728, #28932, #28454 ),
 .UNSPECIFIED., .F., .F.,
 ( 4, 2, 2, 4 ),
 ( 2.213836054437087486E-07, 0.001261154818855359178, 0.001891621536480315915, 0.002522088254105272868 ),
 .UNSPECIFIED. ) ;
#16056=DIRECTION ( 'NONE',  ( 1.000000000000000000, 0.000000000000000000, 0.000000000000000000 ) ) ;
#16077=B_SPLINE_CURVE_WITH_KNOTS ( 'NONE', 3,
 ( #19604, #30462, #2398, #1905, #9723, #10049, #30159, #12078 ),
 .UNSPECIFIED., .F., .F.,
 ( 4, 2, 2, 4 ),
 ( 2.049880227661072435E-07, 0.001261138121172438592, 0.001891604687747274784, 0.002522071254322110975 ),
 .UNSPECIFIED. ) ;
#16082=ADVANCED_FACE ( 'NONE', ( #27004 ), #29843, .T. ) ;
#16095=ORIENTED_EDGE ( 'NONE', *, *, #30633, .T. ) ;
#16099=VECTOR ( 'NONE', #23571, 1000.000000000000000 ) ;
#16108=CARTESIAN_POINT ( 'NONE',  ( 0.7632845268398879002, -8.152713396088778097, 3.174628368996039729 ) ) ;
#16131=CYLINDRICAL_SURFACE ( 'NONE', #5505, 4.000000000000001776 ) ;
#16133=CIRCLE ( 'NONE', #14531, 3.499999999999999556 ) ;
#16135=CARTESIAN_POINT ( 'NONE',  ( 0.7212197624752703096, 8.661246924783327472, -2.263408446298125654 ) ) ;
#16146=DIRECTION ( 'NONE',  ( -1.000000000000000000, 0.000000000000000000, -0.000000000000000000 ) ) ;
#16162=AXIS2_PLACEMENT_3D ( 'NONE', #14878, #25080, #14566 ) ;
#16174=VERTEX_POINT ( 'NONE', #2592 ) ;
#16179=CARTESIAN_POINT ( 'NONE',  ( 2.976845970491565296, -7.079702685456837230, -5.822399416825385643 ) ) ;
#16189=ORIENTED_EDGE ( 'NONE', *, *, #3702, .T. ) ;
#16204=DIRECTION ( 'NONE',  ( 0.000000000000000000, 0.000000000000000000, 1.000000000000000000 ) ) ;
#16207=CIRCLE ( 'NONE', #23171, 8.749000000000002331 ) ;
#16208=CIRCLE ( 'NONE', #19334, 8.749000000000002331 ) ;
#16209=B_SPLINE_CURVE_WITH_KNOTS ( 'NONE', 3,
 ( #5067, #14482, #19182, #1478, #21849, #29882, #706, #4145 ),
 .UNSPECIFIED., .F., .F.,
 ( 4, 2, 2, 4 ),
 ( 2.494123658409239446E-07, 0.001262099805927711102, 0.001893025002708644509, 0.002523950199489578133 ),
 .UNSPECIFIED. ) ;
#16218=ORIENTED_EDGE ( 'NONE', *, *, #25213, .T. ) ;
#16224=CARTESIAN_POINT ( 'NONE',  ( 0.6791198416090081791, -4.928602827912263784, 7.715582677070920603 ) ) ;
#16233=CARTESIAN_POINT ( 'NONE',  ( 0.000000000000000000, 0.000000000000000000, 0.000000000000000000 ) ) ;
#16234=VERTEX_POINT ( 'NONE', #28156 ) ;
#16235=EDGE_CURVE ( 'NONE', #26576, #1557, #10441, .T. ) ;
#16255=DIRECTION ( 'NONE',  ( -1.000000000000000000, 0.000000000000000000, 0.000000000000000000 ) ) ;
#16266=DIRECTION ( 'NONE',  ( 0.000000000000000000, 0.000000000000000000, 1.000000000000000000 ) ) ;
#16275=VERTEX_POINT ( 'NONE', #18116 ) ;
#16278=CARTESIAN_POINT ( 'NONE',  ( 2.357329895872533054, 10.75444571268654848, 1.335530315079542563 ) ) ;
#16298=CARTESIAN_POINT ( 'NONE',  ( 3.249999999999999556, 0.4999240074894433228, 8.734705317681628500 ) ) ;
#16303=FACE_OUTER_BOUND ( 'NONE', #30690, .T. ) ;
#16305=CARTESIAN_POINT ( 'NONE',  ( 3.020080204141757374, 4.831795131260099296, -7.542713057980071412 ) ) ;
#16314=CARTESIAN_POINT ( 'NONE',  ( 0.7632845268398871230, -6.772677083992345359, -5.538577986808975062 ) ) ;
#16315=CARTESIAN_POINT ( 'NONE',  ( 0.000000000000000000, -1.975651141462316351, 10.82112760146735297 ) ) ;
#16319=EDGE_CURVE ( 'NONE', #12410, #979, #909, .T. ) ;
#16323=CYLINDRICAL_SURFACE ( 'NONE', #14040, 8.749000000000002331 ) ;
#16332=CARTESIAN_POINT ( 'NONE',  ( 2.864530875629062390, -0.6595692664038241837, 9.539603485476151334 ) ) ;
#16333=CARTESIAN_POINT ( 'NONE',  ( 2.274274201625327230, 5.222868219166857173, 9.680994141368788775 ) ) ;
#16336=CARTESIAN_POINT ( 'NONE',  ( 0.5704039292222262691, 6.124150562935539277, 7.316743080999650317 ) ) ;
#16337=EDGE_CURVE ( 'NONE', #18033, #20676, #10206, .T. ) ;
#16339=CARTESIAN_POINT ( 'NONE',  ( 1.624999999999999778, 9.680994141368847394, -5.222868219166750592 ) ) ;
#16348=CARTESIAN_POINT ( 'NONE',  ( 0.7212197813410882175, -3.259817272377325992, 8.337493976400230267 ) ) ;
#16353=ADVANCED_FACE ( 'NONE', ( #2955 ), #29427, .T. ) ;
#16356=DIRECTION ( 'NONE',  ( 1.000000000000000000, -0.000000000000000000, -0.000000000000000000 ) ) ;
#16367=ORIENTED_EDGE ( 'NONE', *, *, #20703, .F. ) ;
#16369=ORIENTED_EDGE ( 'NONE', *, *, #18370, .T. ) ;
#16378=DIRECTION ( 'NONE',  ( -1.000000000000000000, 0.000000000000000000, 0.000000000000000000 ) ) ;
#16379=CYLINDRICAL_SURFACE ( 'NONE', #27881, 4.000000000000001776 ) ;
#16384=EDGE_CURVE ( 'NONE', #17287, #32109, #7534, .T. ) ;
#16388=CARTESIAN_POINT ( 'NONE',  ( 0.000000000000000000, 0.000000000000000000, 0.000000000000000000 ) ) ;
#16402=DIRECTION ( 'NONE',  ( 0.000000000000000000, 0.000000000000000000, 1.000000000000000000 ) ) ;
#16418=CARTESIAN_POINT ( 'NONE',  ( 2.661997781067684699, 3.981025027156612772, -9.315861390595046032 ) ) ;
#16432=EDGE_CURVE ( 'NONE', #18655, #7759, #7836, .T. ) ;
#16435=EDGE_CURVE ( 'NONE', #18983, #27498, #31579, .T. ) ;
#16441=DIRECTION ( 'NONE',  ( -1.000000000000000000, 0.000000000000000000, 0.000000000000000000 ) ) ;
#16443=CARTESIAN_POINT ( 'NONE',  ( 0.000000000000000000, -5.222868219166785231, -9.680994141368824302 ) ) ;
#16447=DIRECTION ( 'NONE',  ( 0.000000000000000000, 0.000000000000000000, 1.000000000000000000 ) ) ;
#16456=DIRECTION ( 'NONE',  ( -1.000000000000000000, 0.000000000000000000, 0.000000000000000000 ) ) ;
#16459=ADVANCED_FACE ( 'NONE', ( #17225 ), #24906, .T. ) ;
#16467=CARTESIAN_POINT ( 'NONE',  ( 3.063284526839887167, 0.000000000000000000, 0.000000000000000000 ) ) ;
#16471=B_SPLINE_CURVE_WITH_KNOTS ( 'NONE', 3,
 ( #31752, #29220, #6305, #13988, #24205, #26699, #20187, #2311 ),
 .UNSPECIFIED., .F., .F.,
 ( 4, 2, 2, 4 ),
 ( 2.049880227769566238E-07, 0.001261138121172460493, 0.001891604687747302106, 0.002522071254322143935 ),
 .UNSPECIFIED. ) ;
#16476=ORIENTED_EDGE ( 'NONE', *, *, #11058, .F. ) ;
#16510=EDGE_CURVE ( 'NONE', #12775, #31261, #2762, .T. ) ;
#16511=ORIENTED_EDGE ( 'NONE', *, *, #29137, .T. ) ;
#16520=ORIENTED_EDGE ( 'NONE', *, *, #10654, .T. ) ;
#16553=CARTESIAN_POINT ( 'NONE',  ( 2.795120570939530591, 9.022485053488420448, -3.714272345039503431 ) ) ;
#16554=DIRECTION ( 'NONE',  ( 1.000000000000000000, 0.000000000000000000, 0.000000000000000000 ) ) ;
#16562=CIRCLE ( 'NONE', #8085, 8.749000000000002331 ) ;
#16567=DIRECTION ( 'NONE',  ( -1.000000000000000000, 0.000000000000000000, 0.000000000000000000 ) ) ;
#16580=DIRECTION ( 'NONE',  ( 1.000000000000000000, -0.000000000000000000, -0.000000000000000000 ) ) ;
#16585=CARTESIAN_POINT ( 'NONE',  ( 0.5640493910588681992, -6.134141009809383149, 7.306425354229878266 ) ) ;
#16603=ORIENTED_EDGE ( 'NONE', *, *, #24477, .F. ) ;
#16607=ORIENTED_EDGE ( 'NONE', *, *, #27973, .F. ) ;
#16608=CARTESIAN_POINT ( 'NONE',  ( 3.249999999999999556, -5.538577986808947529, 6.772677083992368452 ) ) ;
#16609=ORIENTED_EDGE ( 'NONE', *, *, #24501, .T. ) ;
#16630=VECTOR ( 'NONE', #13872, 1000.000000000000000 ) ;
#16654=AXIS2_PLACEMENT_3D ( 'NONE', #11756, #27308, #19479 ) ;
#16658=CARTESIAN_POINT ( 'NONE',  ( 3.063284526839890276, 4.729683950898869504, 7.360373001730925679 ) ) ;
#16665=ORIENTED_EDGE ( 'NONE', *, *, #17368, .F. ) ;
#16673=VECTOR ( 'NONE', #19001, 1000.000000000000000 ) ;
#16674=AXIS2_PLACEMENT_3D ( 'NONE', #21943, #23950, #29658 ) ;
#16681=AXIS2_PLACEMENT_3D ( 'NONE', #6142, #26204, #7979 ) ;
#16688=EDGE_CURVE ( 'NONE', #22217, #29709, #8582, .T. ) ;
#16691=CARTESIAN_POINT ( 'NONE',  ( 0.1606233164476231767, -5.257199111574093031, -9.238724727306442119 ) ) ;
#16695=VERTEX_POINT ( 'NONE', #10853 ) ;
#16700=VECTOR ( 'NONE', #27202, 1000.000000000000000 ) ;
#16718=CYLINDRICAL_SURFACE ( 'NONE', #32248, 8.749000000000002331 ) ;
#16719=ADVANCED_FACE ( 'NONE', ( #8342 ), #23874, .F. ) ;
#16722=ORIENTED_EDGE ( 'NONE', *, *, #811, .T. ) ;
#16726=DIRECTION ( 'NONE',  ( 0.000000000000000000, 0.000000000000000000, -1.000000000000000000 ) ) ;
#16727=AXIS2_PLACEMENT_3D ( 'NONE', #22716, #7470, #1114 ) ;
#16730=AXIS2_PLACEMENT_3D ( 'NONE', #9990, #4812, #7471 ) ;
#16735=DIRECTION ( 'NONE',  ( 0.000000000000000000, 0.000000000000000000, -1.000000000000000000 ) ) ;
#16746=VERTEX_POINT ( 'NONE', #29380 ) ;
#16748=CARTESIAN_POINT ( 'NONE',  ( 10.25005080000000035, 0.000000000000000000, 0.000000000000000000 ) ) ;
#16751=FACE_OUTER_BOUND ( 'NONE', #14824, .T. ) ;
#16758=CARTESIAN_POINT ( 'NONE',  ( 0.000000000000000000, 0.000000000000000000, 0.000000000000000000 ) ) ;
#16768=ORIENTED_EDGE ( 'NONE', *, *, #4041, .T. ) ;
#16777=CARTESIAN_POINT ( 'NONE',  ( 0.7632845268398871230, 0.4999240074894433228, 8.734705317681628500 ) ) ;
#16780=ORIENTED_EDGE ( 'NONE', *, *, #18607, .T. ) ;
#16783=B_SPLINE_CURVE_WITH_KNOTS ( 'NONE', 3,
 ( #2646, #12813, #25212, #17513 ),
 .UNSPECIFIED., .F., .F.,
 ( 4, 4 ),
 ( 0.001654338126360077339, 0.002457869280243896344 ),
 .UNSPECIFIED. ) ;
#16784=CARTESIAN_POINT ( 'NONE',  ( 3.063284526839887167, -5.538577986808947529, 6.772677083992368452 ) ) ;
#16802=CARTESIAN_POINT ( 'NONE',  ( 3.063284526839887167, 0.000000000000000000, 0.000000000000000000 ) ) ;
#16810=CARTESIAN_POINT ( 'NONE',  ( 0.1255855353822278031, 9.314797388872380068, 5.239665997526921970 ) ) ;
#16827=EDGE_CURVE ( 'NONE', #25565, #26497, #19689, .T. ) ;
#16838=CARTESIAN_POINT ( 'NONE',  ( 2.864531114197722328, -5.073635298885090350, -8.105385692883677606 ) ) ;
#16842=CARTESIAN_POINT ( 'NONE',  ( 3.063284526839888944, 8.152713396088756781, 3.174628368996099681 ) ) ;
#16845=CARTESIAN_POINT ( 'NONE',  ( 0.3076688720859437898, 10.24120291390723558, 0.9727984658935059370 ) ) ;
#16858=CARTESIAN_POINT ( 'NONE',  ( 5.084999606894402593E-16, -5.227991826304019263, -9.620177616658041941 ) ) ;
#16860=DIRECTION ( 'NONE',  ( -1.000000000000000000, -0.000000000000000000, 0.000000000000000000 ) ) ;
#16869=VERTEX_POINT ( 'NONE', #4311 ) ;
#16880=EDGE_LOOP ( 'NONE', ( #19344, #11719 ) ) ;
#16883=CARTESIAN_POINT ( 'NONE',  ( 2.592584925145449137, 6.844296717726236601, 7.731606906650903888 ) ) ;
#16889=CARTESIAN_POINT ( 'NONE',  ( 2.440333710190773164, -2.130583817698453508, 10.46055952248795329 ) ) ;
#16890=EDGE_CURVE ( 'NONE', #31286, #6749, #8116, .T. ) ;
#16893=VERTEX_POINT ( 'NONE', #7308 ) ;
#16899=DIRECTION ( 'NONE',  ( 0.000000000000000000, 1.224646799147352961E-16, 1.000000000000000000 ) ) ;
#16901=CARTESIAN_POINT ( 'NONE',  ( 3.063284526839887167, 0.000000000000000000, 0.000000000000000000 ) ) ;
#16902=ADVANCED_FACE ( 'NONE', ( #24699 ), #22204, .T. ) ;
#16905=VERTEX_POINT ( 'NONE', #11657 ) ;
#16906=CARTESIAN_POINT ( 'NONE',  ( 2.970200390942824065, -9.143933199822406266, 0.5647484629967252090 ) ) ;
#16916=DIRECTION ( 'NONE',  ( -1.000000000000000000, 0.000000000000000000, 0.000000000000000000 ) ) ;
#16927=CARTESIAN_POINT ( 'NONE',  ( 0.3749742512057840371, -8.659825570211374668, -5.190538276685897401 ) ) ;
#16929=CARTESIAN_POINT ( 'NONE',  ( 0.000000000000000000, 4.762163868918270815, 9.915734732513236338 ) ) ;
#16960=CARTESIAN_POINT ( 'NONE',  ( 3.063284526839887167, 8.461683424509313767, 2.223716399045601921 ) ) ;
#16973=DIRECTION ( 'NONE',  ( -1.000000000000000000, 0.000000000000000000, 0.000000000000000000 ) ) ;
#16982=DIRECTION ( 'NONE',  ( 1.000000000000000000, 0.000000000000000000, 0.000000000000000000 ) ) ;
#16984=ORIENTED_EDGE ( 'NONE', *, *, #22244, .T. ) ;
#16992=CARTESIAN_POINT ( 'NONE',  ( 0.000000000000000000, 0.000000000000000000, 0.000000000000000000 ) ) ;
#17002=ADVANCED_FACE ( 'NONE', ( #22856 ), #2996, .F. ) ;
#17007=FACE_OUTER_BOUND ( 'NONE', #17591, .T. ) ;
#17022=CARTESIAN_POINT ( 'NONE',  ( 3.249999999999999556, 0.000000000000000000, 0.000000000000000000 ) ) ;
#17033=EDGE_CURVE ( 'NONE', #28679, #15781, #17776, .T. ) ;
#17038=DIRECTION ( 'NONE',  ( 1.000000000000000000, -0.000000000000000000, -0.000000000000000000 ) ) ;
#17040=DIRECTION ( 'NONE',  ( 0.000000000000000000, 0.000000000000000000, -1.000000000000000000 ) ) ;
#17043=ORIENTED_EDGE ( 'NONE', *, *, #13272, .F. ) ;
#17044=VECTOR ( 'NONE', #2456, 1000.000000000000000 ) ;
#17053=B_SPLINE_CURVE_WITH_KNOTS ( 'NONE', 3,
 ( #18651, #18836, #312, #18506 ),
 .UNSPECIFIED., .F., .F.,
 ( 4, 4 ),
 ( 2.152606690576576400E-07, 0.0003940451885343313073 ),
 .UNSPECIFIED. ) ;
#17069=CARTESIAN_POINT ( 'NONE',  ( 3.063284526842894540, -6.772677083981750279, 5.538577986799005259 ) ) ;
#17070=CIRCLE ( 'NONE', #552, 10.99999999999999822 ) ;
#17076=CARTESIAN_POINT ( 'NONE',  ( 1.624999999999999778, -5.222868219166785231, -9.680994141368826078 ) ) ;
#17081=ORIENTED_EDGE ( 'NONE', *, *, #30961, .T. ) ;
#17088=ADVANCED_FACE ( 'NONE', ( #3139 ), #10981, .T. ) ;
#17095=VECTOR ( 'NONE', #32638, 1000.000000000000000 ) ;
#17110=CARTESIAN_POINT ( 'NONE',  ( 3.063284526839887167, 2.223716399045691183, -8.461683424509292450 ) ) ;
#17122=AXIS2_PLACEMENT_3D ( 'NONE', #11614, #21810, #6920 ) ;
#17125=CARTESIAN_POINT ( 'NONE',  ( 0.7632845268448539278, 8.734705317657757817, 0.4999240074866477257 ) ) ;
#17126=DIRECTION ( 'NONE',  ( 0.000000000000000000, 0.000000000000000000, 1.000000000000000000 ) ) ;
#17129=ADVANCED_FACE ( 'NONE', ( #11300 ), #11128, .T. ) ;
#17131=ORIENTED_EDGE ( 'NONE', *, *, #6928, .T. ) ;
#17136=ORIENTED_EDGE ( 'NONE', *, *, #7715, .F. ) ;
#17149=CIRCLE ( 'NONE', #30544, 10.94895958125474245 ) ;
#17151=FACE_OUTER_BOUND ( 'NONE', #775, .T. ) ;
#17161=AXIS2_PLACEMENT_3D ( 'NONE', #27806, #27994, #23300 ) ;
#17168=CARTESIAN_POINT ( 'NONE',  ( 0.000000000000000000, 0.000000000000000000, 0.000000000000000000 ) ) ;
#17169=EDGE_CURVE ( 'NONE', #596, #32538, #17179, .T. ) ;
#17175=ORIENTED_EDGE ( 'NONE', *, *, #23302, .T. ) ;
#17179=CIRCLE ( 'NONE', #14491, 8.749000000000002331 ) ;
#17197=DIRECTION ( 'NONE',  ( 1.000000000000000000, 0.000000000000000000, 0.000000000000000000 ) ) ;
#17198=AXIS2_PLACEMENT_3D ( 'NONE', #1329, #14314, #11161 ) ;
#17200=CARTESIAN_POINT ( 'NONE',  ( 3.249999999999999556, 8.734705317681626724, -0.4999240074894737984 ) ) ;
#17202=CIRCLE ( 'NONE', #30570, 15.00000000000000355 ) ;
#17205=DIRECTION ( 'NONE',  ( 0.000000000000000000, 0.000000000000000000, -1.000000000000000000 ) ) ;
#17213=ORIENTED_EDGE ( 'NONE', *, *, #32889, .T. ) ;
#17225=FACE_OUTER_BOUND ( 'NONE', #12589, .T. ) ;
#17245=CARTESIAN_POINT ( 'NONE',  ( 2.437082531750072167, 7.214115859539331765, -7.858345965138702205 ) ) ;
#17249=VERTEX_POINT ( 'NONE', #17125 ) ;
#17250=CARTESIAN_POINT ( 'NONE',  ( 0.000000000000000000, 0.000000000000000000, 0.000000000000000000 ) ) ;
#17252=ORIENTED_EDGE ( 'NONE', *, *, #31170, .T. ) ;
#17255=CARTESIAN_POINT ( 'NONE',  ( 2.556102741905670328, -8.982703267213965503, 5.229406529225562039 ) ) ;
#17256=EDGE_CURVE ( 'NONE', #15940, #2042, #26257, .T. ) ;
#17261=DIRECTION ( 'NONE',  ( 1.000000000000000000, 0.000000000000000000, 0.000000000000000000 ) ) ;
#17263=EDGE_CURVE ( 'NONE', #29923, #16893, #30025, .T. ) ;
#17265=CARTESIAN_POINT ( 'NONE',  ( 0.000000000000000000, 10.82112760146736186, 1.975651141462277272 ) ) ;
#17269=ORIENTED_EDGE ( 'NONE', *, *, #25349, .T. ) ;
#17270=CARTESIAN_POINT ( 'NONE',  ( 2.976845773540287787, -8.532418605434708425, -3.349682859779589350 ) ) ;
#17287=VERTEX_POINT ( 'NONE', #12273 ) ;
#17288=CARTESIAN_POINT ( 'NONE',  ( -7.000050800000000351, 0.000000000000000000, -6.000000000000000888 ) ) ;
#17325=ORIENTED_EDGE ( 'NONE', *, *, #13975, .F. ) ;
#17335=EDGE_CURVE ( 'NONE', #1359, #15940, #4376, .T. ) ;
#17339=CARTESIAN_POINT ( 'NONE',  ( 1.624999999999999778, -4.762163868918343645, 9.915734732513202587 ) ) ;
#17342=CARTESIAN_POINT ( 'NONE',  ( 0.000000000000000000, 10.76487093102067583, -1.999317321091388377 ) ) ;
#17344=LINE ( 'NONE', #4791, #191 ) ;
#17347=DIRECTION ( 'NONE',  ( -1.000000000000000000, -0.000000000000000000, -0.000000000000000000 ) ) ;
#17355=CARTESIAN_POINT ( 'NONE',  ( 3.249999999999999556, 6.478011392632891052, 6.807171995660606711 ) ) ;
#17368=EDGE_CURVE ( 'NONE', #32762, #31355, #24494, .T. ) ;
#17369=ORIENTED_EDGE ( 'NONE', *, *, #24268, .F. ) ;
#17375=CARTESIAN_POINT ( 'NONE',  ( 2.274274201625327230, 0.000000000000000000, 0.000000000000000000 ) ) ;
#17386=CARTESIAN_POINT ( 'NONE',  ( 2.437082316315974939, -10.59788678609685952, -1.217322776604839785 ) ) ;
#17408=ORIENTED_EDGE ( 'NONE', *, *, #17786, .F. ) ;
#17409=CYLINDRICAL_SURFACE ( 'NONE', #2346, 11.00000000000000000 ) ;
#17414=ORIENTED_EDGE ( 'NONE', *, *, #15032, .T. ) ;
#17421=DIRECTION ( 'NONE',  ( -1.000000000000000000, -0.000000000000000000, 0.000000000000000000 ) ) ;
#17430=EDGE_LOOP ( 'NONE', ( #23247, #13361, #4860, #3894, #815 ) ) ;
#17432=DIRECTION ( 'NONE',  ( -1.000000000000000000, -0.000000000000000000, -0.000000000000000000 ) ) ;
#17436=EDGE_CURVE ( 'NONE', #18851, #32762, #10973, .T. ) ;
#17440=EDGE_LOOP ( 'NONE', ( #4351, #2046, #21765, #20426 ) ) ;
#17446=ORIENTED_EDGE ( 'NONE', *, *, #9360, .T. ) ;
#17447=ORIENTED_EDGE ( 'NONE', *, *, #10196, .F. ) ;
#17450=CARTESIAN_POINT ( 'NONE',  ( 0.3045634635876924845, -2.226307684702756529, 10.03290811084030842 ) ) ;
#17453=LINE ( 'NONE', #32198, #10114 ) ;
#17463=CARTESIAN_POINT ( 'NONE',  ( 0.6728000687364281696, -2.287261066731684611, -8.860258565222334681 ) ) ;
#17490=ORIENTED_EDGE ( 'NONE', *, *, #18641, .F. ) ;
#17491=EDGE_CURVE ( 'NONE', #19087, #26011, #14519, .T. ) ;
#17495=CARTESIAN_POINT ( 'NONE',  ( 0.7632845268448663623, 0.4999240074867329353, -8.734705317657697421 ) ) ;
#17501=ORIENTED_EDGE ( 'NONE', *, *, #6821, .T. ) ;
#17513=CARTESIAN_POINT ( 'NONE',  ( 0.7632845268398871230, -8.461683424509331530, 2.223716399045538861 ) ) ;
#17520=CARTESIAN_POINT ( 'NONE',  ( -7.000050800000000351, 0.000000000000000000, 0.000000000000000000 ) ) ;
#17523=DIRECTION ( 'NONE',  ( 1.000000000000000000, -0.000000000000000000, -0.000000000000000000 ) ) ;
#17537=ORIENTED_EDGE ( 'NONE', *, *, #21148, .F. ) ;
#17539=CARTESIAN_POINT ( 'NONE',  ( 2.795120465740001059, -9.482538569678542473, -2.298374178342494467 ) ) ;
#17546=DIRECTION ( 'NONE',  ( -1.000000000000000000, 0.000000000000000000, 0.000000000000000000 ) ) ;
#17554=EDGE_CURVE ( 'NONE', #4033, #15369, #3244, .T. ) ;
#17561=CARTESIAN_POINT ( 'NONE',  ( 0.7632845268451443621, 5.538577986791731078, -6.772677083973650092 ) ) ;
#17565=ORIENTED_EDGE ( 'NONE', *, *, #14313, .T. ) ;
#17568=FACE_OUTER_BOUND ( 'NONE', #7821, .T. ) ;
#17576=FACE_OUTER_BOUND ( 'NONE', #31509, .T. ) ;
#17586=VECTOR ( 'NONE', #21931, 1000.000000000000000 ) ;
#17591=EDGE_LOOP ( 'NONE', ( #27674, #9477, #10962, #29386, #13131 ) ) ;
#17592=DIRECTION ( 'NONE',  ( 0.000000000000000000, 0.000000000000000000, -1.000000000000000000 ) ) ;
#17601=CYLINDRICAL_SURFACE ( 'NONE', #17161, 4.000000000000001776 ) ;
#17602=CIRCLE ( 'NONE', #4243, 11.00000000000000000 ) ;
#17609=DIRECTION ( 'NONE',  ( 0.000000000000000000, 0.000000000000000000, -1.000000000000000000 ) ) ;
#17613=EDGE_CURVE ( 'NONE', #31435, #6261, #19895, .T. ) ;
#17626=CIRCLE ( 'NONE', #7483, 4.000000000000001776 ) ;
#17627=DIRECTION ( 'NONE',  ( 1.000000000000000000, -0.000000000000000000, -0.000000000000000000 ) ) ;
#17637=VERTEX_POINT ( 'NONE', #28317 ) ;
#17653=VERTEX_POINT ( 'NONE', #11250 ) ;
#17659=CARTESIAN_POINT ( 'NONE',  ( 3.063284526839887167, -6.772677083992345359, -5.538577986808975062 ) ) ;
#17663=B_SPLINE_CURVE_WITH_KNOTS ( 'NONE', 3,
 ( #3190, #21391, #28603, #858, #26730, #8687, #24045, #11525 ),
 .UNSPECIFIED., .F., .F.,
 ( 4, 2, 2, 4 ),
 ( 2.024520226829450289E-07, 0.001227962984610849210, 0.001841843250904934542, 0.002455723517199020090 ),
 .UNSPECIFIED. ) ;
#17666=ORIENTED_EDGE ( 'NONE', *, *, #11199, .F. ) ;
#17671=CIRCLE ( 'NONE', #22999, 15.00000000000000355 ) ;
#17679=CARTESIAN_POINT ( 'NONE',  ( -7.000050800000000351, 0.000000000000000000, 0.000000000000000000 ) ) ;
#17687=CARTESIAN_POINT ( 'NONE',  ( 0.3076689308780821142, 8.857103639574720688, -5.232617538234502597 ) ) ;
#17691=CARTESIAN_POINT ( 'NONE',  ( 2.274274201621893976, 1.464956435144894931, 10.90201369671109610 ) ) ;
#17695=ORIENTED_EDGE ( 'NONE', *, *, #11617, .F. ) ;
#17697=DIRECTION ( 'NONE',  ( -1.000000000000000000, 0.000000000000000000, -0.000000000000000000 ) ) ;
#17701=ORIENTED_EDGE ( 'NONE', *, *, #7048, .F. ) ;
#17704=AXIS2_PLACEMENT_3D ( 'NONE', #8310, #18650, #6273 ) ;
#17708=CARTESIAN_POINT ( 'NONE',  ( 0.5704037183047365733, 5.066169706250169824, -8.085411865508655538 ) ) ;
#17718=EDGE_CURVE ( 'NONE', #26820, #30798, #13991, .T. ) ;
#17726=CARTESIAN_POINT ( 'NONE',  ( 3.063284526839889388, 2.223716399045570391, 8.461683424509315543 ) ) ;
#17735=ORIENTED_EDGE ( 'NONE', *, *, #23648, .T. ) ;
#17746=DIRECTION ( 'NONE',  ( 0.000000000000000000, 0.000000000000000000, 1.000000000000000000 ) ) ;
#17751=VERTEX_POINT ( 'NONE', #9403 ) ;
#17755=DIRECTION ( 'NONE',  ( 0.000000000000000000, 1.224646799147352961E-16, 1.000000000000000000 ) ) ;
#17759=CARTESIAN_POINT ( 'NONE',  ( 3.249999999999999556, 4.057423117305393845, 8.475820894092990443 ) ) ;
#17770=FACE_OUTER_BOUND ( 'NONE', #24134, .T. ) ;
#17776=B_SPLINE_CURVE_WITH_KNOTS ( 'NONE', 3,
 ( #2317, #5476, #4799, #15323, #25880, #7653, #7818, #2483 ),
 .UNSPECIFIED., .F., .F.,
 ( 4, 2, 2, 4 ),
 ( 5.099451029770106864E-07, 0.001229189590448579025, 0.001843529413121382157, 0.002457869235794185071 ),
 .UNSPECIFIED. ) ;
#17777=AXIS2_PLACEMENT_3D ( 'NONE', #18334, #28541, #8129 ) ;
#17779=ORIENTED_EDGE ( 'NONE', *, *, #30846, .F. ) ;
#17782=CARTESIAN_POINT ( 'NONE',  ( 3.249999999999999556, -1.239665997526952612, 9.314797388894886510 ) ) ;
#17783=ORIENTED_EDGE ( 'NONE', *, *, #15371, .T. ) ;
#17784=ORIENTED_EDGE ( 'NONE', *, *, #31452, .F. ) ;
#17785=DIRECTION ( 'NONE',  ( -1.000000000000000000, 0.000000000000000000, 0.000000000000000000 ) ) ;
#17786=EDGE_CURVE ( 'NONE', #5630, #19429, #24143, .T. ) ;
#17787=CIRCLE ( 'NONE', #22589, 4.000000000000001776 ) ;
#17788=EDGE_CURVE ( 'NONE', #5149, #27498, #32716, .T. ) ;
#17796=CARTESIAN_POINT ( 'NONE',  ( 0.000000000000000000, 0.000000000000000000, 0.000000000000000000 ) ) ;
#17798=DIRECTION ( 'NONE',  ( -1.000000000000000000, 0.000000000000000000, 0.000000000000000000 ) ) ;
#17801=FACE_OUTER_BOUND ( 'NONE', #25550, .T. ) ;
#17802=CARTESIAN_POINT ( 'NONE',  ( 0.6791199890552591656, 7.071625480714588186, -5.814932665552434266 ) ) ;
#17840=AXIS2_PLACEMENT_3D ( 'NONE', #14251, #6895, #6743 ) ;
#17848=CARTESIAN_POINT ( 'NONE',  ( 0.000000000000000000, -4.762163868918202425, -9.915734732513268312 ) ) ;
#17864=CARTESIAN_POINT ( 'NONE',  ( 3.249999999999999556, 8.734705317681626724, 0.4999240074894746311 ) ) ;
#17866=EDGE_CURVE ( 'NONE', #15147, #25174, #29162, .T. ) ;
#17867=FACE_OUTER_BOUND ( 'NONE', #21795, .T. ) ;
#17871=EDGE_CURVE ( 'NONE', #13047, #9758, #37, .T. ) ;
#17876=CARTESIAN_POINT ( 'NONE',  ( 0.1574692253523934382, -10.40622129948746633, -2.132217800985146017 ) ) ;
#17877=DIRECTION ( 'NONE',  ( 0.000000000000000000, 0.000000000000000000, 1.000000000000000000 ) ) ;
#17881=FACE_OUTER_BOUND ( 'NONE', #10465, .T. ) ;
#17892=CARTESIAN_POINT ( 'NONE',  ( 0.7632845268458192667, 3.174628368984171889, -8.152713396062660323 ) ) ;
#17898=CARTESIAN_POINT ( 'NONE',  ( 0.3749742847181612437, -9.289351359934261865, 3.955024136976932780 ) ) ;
#17905=DIRECTION ( 'NONE',  ( 1.000000000000000000, 0.000000000000000000, 0.000000000000000000 ) ) ;
#17914=ORIENTED_EDGE ( 'NONE', *, *, #8283, .F. ) ;
#17929=VERTEX_POINT ( 'NONE', #25454 ) ;
#17930=DIRECTION ( 'NONE',  ( 0.000000000000000000, 0.000000000000000000, 1.000000000000000000 ) ) ;
#17945=CARTESIAN_POINT ( 'NONE',  ( 3.008012635915382038, -8.723904125990801006, 2.275870607900217113 ) ) ;
#17964=CARTESIAN_POINT ( 'NONE',  ( 3.249999999999999556, 0.000000000000000000, 8.749000000000002331 ) ) ;
#17967=DIRECTION ( 'NONE',  ( 0.000000000000000000, 0.000000000000000000, -1.000000000000000000 ) ) ;
#17969=CARTESIAN_POINT ( 'NONE',  ( 3.249999999999999556, 8.572527594031471218E-16, 6.999999999999998224 ) ) ;
#17974=DIRECTION ( 'NONE',  ( 1.000000000000000000, 0.000000000000000000, 0.000000000000000000 ) ) ;
#17980=VERTEX_POINT ( 'NONE', #14750 ) ;
#17985=LINE ( 'NONE', #18133, #14386 ) ;
#17992=ORIENTED_EDGE ( 'NONE', *, *, #6089, .T. ) ;
#17996=EDGE_LOOP ( 'NONE', ( #14705, #14885, #24307, #11274 ) ) ;
#18002=FACE_OUTER_BOUND ( 'NONE', #13154, .T. ) ;
#18004=DIRECTION ( 'NONE',  ( 1.000000000000000000, 0.000000000000000000, 0.000000000000000000 ) ) ;
#18033=VERTEX_POINT ( 'NONE', #879 ) ;
#18035=CARTESIAN_POINT ( 'NONE',  ( 3.249999999999999556, -9.314797388894900720, 1.239665997526854468 ) ) ;
#18042=DIRECTION ( 'NONE',  ( -1.000000000000000000, -0.000000000000000000, 0.000000000000000000 ) ) ;
#18048=DIRECTION ( 'NONE',  ( -1.000000000000000000, 0.000000000000000000, -0.000000000000000000 ) ) ;
#18051=CARTESIAN_POINT ( 'NONE',  ( 2.589202987961084279, 2.218054364314597127, 10.07394153291403782 ) ) ;
#18072=CYLINDRICAL_SURFACE ( 'NONE', #7625, 4.000000000000001776 ) ;
#18079=ORIENTED_EDGE ( 'NONE', *, *, #23112, .F. ) ;
#18089=DIRECTION ( 'NONE',  ( -1.000000000000000000, 0.000000000000000000, -0.000000000000000000 ) ) ;
#18091=CARTESIAN_POINT ( 'NONE',  ( 0.000000000000000000, 9.915734732513218574, 4.762163868918305454 ) ) ;
#18100=CARTESIAN_POINT ( 'NONE',  ( 0.000000000000000000, 10.90201369670498366, -1.464956435139577851 ) ) ;
#18104=CARTESIAN_POINT ( 'NONE',  ( 0.000000000000000000, 0.000000000000000000, 0.000000000000000000 ) ) ;
#18116=CARTESIAN_POINT ( 'NONE',  ( 2.274274201625327230, 7.958834565716768061, 7.593217523260608282 ) ) ;
#18121=DIRECTION ( 'NONE',  ( 1.000000000000000000, 0.000000000000000000, 0.000000000000000000 ) ) ;
#18133=CARTESIAN_POINT ( 'NONE',  ( 1.624999999999999778, -7.593217523260524793, -7.958834565716851550 ) ) ;
#18142=ORIENTED_EDGE ( 'NONE', *, *, #4277, .F. ) ;
#18152=CARTESIAN_POINT ( 'NONE',  ( 0.000000000000000000, 9.241976615262133876, 1.699438267350532161 ) ) ;
#18160=CARTESIAN_POINT ( 'NONE',  ( 0.3076690219754985023, -7.713510465969182661, -6.806638167515123961 ) ) ;
#18163=ORIENTED_EDGE ( 'NONE', *, *, #5095, .F. ) ;
#18174=ORIENTED_EDGE ( 'NONE', *, *, #29209, .T. ) ;
#18175=CARTESIAN_POINT ( 'NONE',  ( 0.1606233060840182858, 9.683549581718741806, 4.384181225613559718 ) ) ;
#18180=CIRCLE ( 'NONE', #8555, 10.99999999999999822 ) ;
#18186=EDGE_CURVE ( 'NONE', #24130, #11832, #25987, .T. ) ;
#18187=CARTESIAN_POINT ( 'NONE',  ( 2.274274201625327230, 0.000000000000000000, 0.000000000000000000 ) ) ;
#18188=EDGE_CURVE ( 'NONE', #4178, #19641, #4824, .T. ) ;
#18192=CIRCLE ( 'NONE', #23533, 11.00000000000000000 ) ;
#18198=ORIENTED_EDGE ( 'NONE', *, *, #23429, .F. ) ;
#18204=DIRECTION ( 'NONE',  ( 0.000000000000000000, 0.000000000000000000, 1.000000000000000000 ) ) ;
#18205=CIRCLE ( 'NONE', #30041, 10.94895958125474245 ) ;
#18211=TOROIDAL_SURFACE ( 'NONE', #9120, 3.895301350492843540, 15.00000000000000178 ) ;
#18232=CIRCLE ( 'NONE', #4932, 15.00000000000000355 ) ;
#18242=DIRECTION ( 'NONE',  ( 0.000000000000000000, 0.000000000000000000, 1.000000000000000000 ) ) ;
#18245=CARTESIAN_POINT ( 'NONE',  ( 3.063284526839887167, 6.772677083992467928, -5.538577986808824960 ) ) ;
#18248=CARTESIAN_POINT ( 'NONE',  ( 1.624999999999999778, 7.958834565716877307, -7.593217523260497259 ) ) ;
#18264=VECTOR ( 'NONE', #5, 1000.000000000000000 ) ;
#18269=EDGE_CURVE ( 'NONE', #29792, #13047, #23243, .T. ) ;
#18275=LINE ( 'NONE', #13242, #1074 ) ;
#18287=CIRCLE ( 'NONE', #24660, 8.749000000000002331 ) ;
#18288=CARTESIAN_POINT ( 'NONE',  ( 3.249999999999999556, 0.000000000000000000, 0.000000000000000000 ) ) ;
#18299=B_SPLINE_CURVE_WITH_KNOTS ( 'NONE', 3,
 ( #2534, #29944, #2189, #7031, #22598, #17245, #12375, #5355 ),
 .UNSPECIFIED., .F., .F.,
 ( 4, 2, 2, 4 ),
 ( 2.737843117464003789E-07, 0.001261207499628673586, 0.001891674357287136598, 0.002522141214945600694 ),
 .UNSPECIFIED. ) ;
#18306=EDGE_LOOP ( 'NONE', ( #10813, #7390, #8850, #16369 ) ) ;
#18308=VECTOR ( 'NONE', #21842, 1000.000000000000000 ) ;
#18315=CARTESIAN_POINT ( 'NONE',  ( -10.00000000000000000, 0.000000000000000000, 0.000000000000000000 ) ) ;
#18323=EDGE_LOOP ( 'NONE', ( #14593, #22383, #3009, #20589 ) ) ;
#18324=EDGE_LOOP ( 'NONE', ( #10293, #15878, #27264, #26343 ) ) ;
#18330=CARTESIAN_POINT ( 'NONE',  ( 0.000000000000000000, 7.533794289458167981, -7.944914065997031649 ) ) ;
#18332=DIRECTION ( 'NONE',  ( 1.000000000000000000, 0.000000000000000000, 0.000000000000000000 ) ) ;
#18334=CARTESIAN_POINT ( 'NONE',  ( 0.000000000000000000, -1.239665997526952612, 9.314797388894886510 ) ) ;
#18338=B_SPLINE_CURVE_WITH_KNOTS ( 'NONE', 3,
 ( #6751, #1571, #4238, #9258, #31849, #11949, #8918, #1421 ),
 .UNSPECIFIED., .F., .F.,
 ( 4, 2, 2, 4 ),
 ( 2.152606640980682932E-07, 0.001262065476475210347, 0.001892990584380766211, 0.002523915692286320123 ),
 .UNSPECIFIED. ) ;
#18358=FACE_OUTER_BOUND ( 'NONE', #12429, .T. ) ;
#18359=EDGE_CURVE ( 'NONE', #19301, #15923, #5253, .T. ) ;
#18370=EDGE_CURVE ( 'NONE', #16869, #26634, #30786, .T. ) ;
#18395=CARTESIAN_POINT ( 'NONE',  ( 2.866494652520772846, -9.241976615239517301, 2.300561732649529123 ) ) ;
#18403=B_SPLINE_CURVE_WITH_KNOTS ( 'NONE', 3,
 ( #16777, #11252, #24441, #21780, #1558, #24603, #22133, #6095 ),
 .UNSPECIFIED., .F., .F.,
 ( 4, 2, 2, 4 ),
 ( 2.024520226885745157E-07, 0.001227962984611320404, 0.001841843250905638406, 0.002455723517199956841 ),
 .UNSPECIFIED. ) ;
#18421=CARTESIAN_POINT ( 'NONE',  ( 0.000000000000000000, -5.227991826304158707, 9.620177616657965558 ) ) ;
#18426=CARTESIAN_POINT ( 'NONE',  ( 0.000000000000000000, -7.944914065997164876, 7.533794289458026761 ) ) ;
#18429=ORIENTED_EDGE ( 'NONE', *, *, #29842, .T. ) ;
#18439=ORIENTED_EDGE ( 'NONE', *, *, #1883, .F. ) ;
#18452=CARTESIAN_POINT ( 'NONE',  ( -10.00000000000000000, 0.000000000000000000, 0.000000000000000000 ) ) ;
#18458=B_SPLINE_CURVE_WITH_KNOTS ( 'NONE', 3,
 ( #9577, #27144, #19797, #1760, #17450, #24628, #30003, #22804 ),
 .UNSPECIFIED., .F., .F.,
 ( 4, 2, 2, 4 ),
 ( 2.049880227679818068E-07, 0.001227965543375839899, 0.001841845821052373383, 0.002455726098728907084 ),
 .UNSPECIFIED. ) ;
#18476=B_SPLINE_CURVE_WITH_KNOTS ( 'NONE', 3,
 ( #26508, #26822, #3944, #8598, #21967, #11114, #31702, #14116 ),
 .UNSPECIFIED., .F., .F.,
 ( 4, 2, 2, 4 ),
 ( 2.049880227734711626E-07, 0.001227965543376307840, 0.001841845821053075078, 0.002455726098729842533 ),
 .UNSPECIFIED. ) ;
#18488=EDGE_LOOP ( 'NONE', ( #16722, #32813, #20411, #15251 ) ) ;
#18492=CARTESIAN_POINT ( 'NONE',  ( 0.5640493910637760511, 6.134141009795983202, -7.306425354220267288 ) ) ;
#18494=PLANE ( 'NONE',  #19709 ) ;
#18506=CARTESIAN_POINT ( 'NONE',  ( 2.425585535373192325, 9.314797388894900720, 5.239665997526921970 ) ) ;
#18512=B_SPLINE_CURVE_WITH_KNOTS ( 'NONE', 3,
 ( #32390, #22330, #24844, #9955, #12133, #32542 ),
 .UNSPECIFIED., .F., .F.,
 ( 4, 2, 4 ),
 ( 0.0003940451885343313073, 0.001458980440401463040, 0.002523915692268594718 ),
 .UNSPECIFIED. ) ;
#18528=EDGE_CURVE ( 'NONE', #9818, #12294, #28491, .T. ) ;
#18530=DIRECTION ( 'NONE',  ( 0.000000000000000000, 0.000000000000000000, 1.000000000000000000 ) ) ;
#18536=ORIENTED_EDGE ( 'NONE', *, *, #25697, .F. ) ;
#18540=ADVANCED_FACE ( 'NONE', ( #26940 ), #27250, .T. ) ;
#18547=CARTESIAN_POINT ( 'NONE',  ( 1.661358730909628482E-15, -10.85582367538893322, -1.425064293572451790 ) ) ;
#18550=EDGE_LOOP ( 'NONE', ( #12031, #24261, #8987, #22794 ) ) ;
#18554=CARTESIAN_POINT ( 'NONE',  ( 3.249999999999999556, 4.286263797015736102E-16, -3.499999999999999556 ) ) ;
#18556=CARTESIAN_POINT ( 'NONE',  ( 3.249999999999999556, 0.000000000000000000, 0.000000000000000000 ) ) ;
#18586=EDGE_CURVE ( 'NONE', #31286, #29455, #30133, .T. ) ;
#18603=ORIENTED_EDGE ( 'NONE', *, *, #24835, .F. ) ;
#18607=EDGE_CURVE ( 'NONE', #681, #30241, #31177, .T. ) ;
#18628=ORIENTED_EDGE ( 'NONE', *, *, #24798, .F. ) ;
#18637=CARTESIAN_POINT ( 'NONE',  ( 0.9499999999999995115, 8.572527594031471218E-16, 6.999999999999998224 ) ) ;
#18641=EDGE_CURVE ( 'NONE', #18983, #23564, #27511, .T. ) ;
#18650=DIRECTION ( 'NONE',  ( -1.000000000000000000, -0.000000000000000000, 0.000000000000000000 ) ) ;
#18651=CARTESIAN_POINT ( 'NONE',  ( 2.274274201627289216, 9.680994141364161365, 5.222868219167314585 ) ) ;
#18655=VERTEX_POINT ( 'NONE', #7358 ) ;
#18679=LINE ( 'NONE', #26406, #8016 ) ;
#18683=B_SPLINE_CURVE_WITH_KNOTS ( 'NONE', 3,
 ( #22669, #27335, #4450, #16960 ),
 .UNSPECIFIED., .F., .F.,
 ( 4, 4 ),
 ( 0.001719859957800634609, 0.002523933526961084049 ),
 .UNSPECIFIED. ) ;
#18689=CARTESIAN_POINT ( 'NONE',  ( 0.000000000000000000, 0.000000000000000000, 0.000000000000000000 ) ) ;
#18692=ORIENTED_EDGE ( 'NONE', *, *, #16688, .F. ) ;
#18700=ORIENTED_EDGE ( 'NONE', *, *, #7055, .F. ) ;
#18709=AXIS2_PLACEMENT_3D ( 'NONE', #16992, #21695, #32561 ) ;
#18711=ORIENTED_EDGE ( 'NONE', *, *, #9397, .T. ) ;
#18724=AXIS2_PLACEMENT_3D ( 'NONE', #2551, #12881, #15238 ) ;
#18727=AXIS2_PLACEMENT_3D ( 'NONE', #21800, #4099, #9265 ) ;
#18728=CARTESIAN_POINT ( 'NONE',  ( 2.437082427505617321, -4.432669656489553134, 9.703015696712942173 ) ) ;
#18735=EDGE_CURVE ( 'NONE', #17249, #17751, #25820, .T. ) ;
#18739=AXIS2_PLACEMENT_3D ( 'NONE', #355, #30941, #22906 ) ;
#18740=CARTESIAN_POINT ( 'NONE',  ( 2.857987896746962075, -2.305585824582580656, 9.278099925236432455 ) ) ;
#18747=CIRCLE ( 'NONE', #11287, 4.000000000000001776 ) ;
#18754=VECTOR ( 'NONE', #14163, 1000.000000000000000 ) ;
#18764=AXIS2_PLACEMENT_3D ( 'NONE', #16758, #26616, #31475 ) ;
#18766=VECTOR ( 'NONE', #9414, 1000.000000000000000 ) ;
#18777=EDGE_CURVE ( 'NONE', #25199, #22329, #25549, .T. ) ;
#18781=VECTOR ( 'NONE', #16580, 1000.000000000000000 ) ;
#18796=CARTESIAN_POINT ( 'NONE',  ( 2.661997781067683366, 9.315861390595088665, 3.981025027156513296 ) ) ;
#18802=B_SPLINE_CURVE_WITH_KNOTS ( 'NONE', 3,
 ( #232, #7551, #12725, #15897, #30821, #5222 ),
 .UNSPECIFIED., .F., .F.,
 ( 4, 2, 4 ),
 ( 2.333100327427146720E-07, 0.0008600466339166887254, 0.001719859957800634609 ),
 .UNSPECIFIED. ) ;
#18814=AXIS2_PLACEMENT_3D ( 'NONE', #8141, #18837, #951 ) ;
#18819=AXIS2_PLACEMENT_3D ( 'NONE', #13325, #23537, #24204 ) ;
#18820=CARTESIAN_POINT ( 'NONE',  ( 0.7632845268429988561, 7.360373001717848140, -4.729683950891435451 ) ) ;
#18835=DIRECTION ( 'NONE',  ( 0.000000000000000000, 0.000000000000000000, 1.000000000000000000 ) ) ;
#18836=CARTESIAN_POINT ( 'NONE',  ( 2.326102263860147179, 9.559024163330285262, 5.234081561440546260 ) ) ;
#18837=DIRECTION ( 'NONE',  ( -1.000000000000000000, 0.000000000000000000, 0.000000000000000000 ) ) ;
#18844=AXIS2_PLACEMENT_3D ( 'NONE', #22486, #32701, #9782 ) ;
#18851=VERTEX_POINT ( 'NONE', #3668 ) ;
#18860=DIRECTION ( 'NONE',  ( 0.000000000000000000, 0.000000000000000000, 1.000000000000000000 ) ) ;
#18862=ORIENTED_EDGE ( 'NONE', *, *, #25697, .T. ) ;
#18864=CARTESIAN_POINT ( 'NONE',  ( 1.624999999999999778, 10.82112760146739383, -1.975651141462126947 ) ) ;
#18868=LINE ( 'NONE', #16339, #6039 ) ;
#18873=CARTESIAN_POINT ( 'NONE',  ( 0.000000000000000000, 0.000000000000000000, 0.000000000000000000 ) ) ;
#18897=CIRCLE ( 'NONE', #14050, 10.94895958125474245 ) ;
#18904=ORIENTED_EDGE ( 'NONE', *, *, #22303, .T. ) ;
#18906=CARTESIAN_POINT ( 'NONE',  ( 0.000000000000000000, 6.478011392632891052, 6.807171995660606711 ) ) ;
#18915=FACE_OUTER_BOUND ( 'NONE', #11944, .T. ) ;
#18929=CARTESIAN_POINT ( 'NONE',  ( 0.000000000000000000, -7.533794289457995674, -7.944914065997195074 ) ) ;
#18943=VERTEX_POINT ( 'NONE', #27884 ) ;
#18944=ORIENTED_EDGE ( 'NONE', *, *, #19732, .F. ) ;
#18951=EDGE_CURVE ( 'NONE', #10585, #25735, #27705, .T. ) ;
#18960=EDGE_CURVE ( 'NONE', #4750, #17249, #9838, .T. ) ;
#18965=ADVANCED_FACE ( 'NONE', ( #4508 ), #29900, .T. ) ;
#18968=ORIENTED_EDGE ( 'NONE', *, *, #24798, .T. ) ;
#18970=CARTESIAN_POINT ( 'NONE',  ( 0.000000000000000000, 4.472189673936786569, 8.264486777890123648 ) ) ;
#18983=VERTEX_POINT ( 'NONE', #9485 ) ;
#18986=LINE ( 'NONE', #16298, #8017 ) ;
#18988=DIRECTION ( 'NONE',  ( -1.000000000000000000, 0.000000000000000000, 0.000000000000000000 ) ) ;
#19001=DIRECTION ( 'NONE',  ( 1.000000000000000000, 0.000000000000000000, -0.000000000000000000 ) ) ;
#19009=CARTESIAN_POINT ( 'NONE',  ( 3.249999999999999556, 0.000000000000000000, 0.000000000000000000 ) ) ;
#19027=DIRECTION ( 'NONE',  ( -1.000000000000000000, 0.000000000000000000, 0.000000000000000000 ) ) ;
#19033=CARTESIAN_POINT ( 'NONE',  ( 0.1606232843943592725, 10.56438947504861936, 1.177222770082250847 ) ) ;
#19035=FACE_OUTER_BOUND ( 'NONE', #27952, .T. ) ;
#19062=CARTESIAN_POINT ( 'NONE',  ( 3.249999999999999556, -4.729683950898923683, 7.360373001730901699 ) ) ;
#19063=CYLINDRICAL_SURFACE ( 'NONE', #9600, 11.00000000000000000 ) ;
#19076=DIRECTION ( 'NONE',  ( -1.000000000000000000, 0.000000000000000000, -0.000000000000000000 ) ) ;
#19085=CARTESIAN_POINT ( 'NONE',  ( 0.000000000000000000, 0.000000000000000000, 0.000000000000000000 ) ) ;
#19087=VERTEX_POINT ( 'NONE', #7280 ) ;
#19099=CARTESIAN_POINT ( 'NONE',  ( 3.063284526839887167, 0.000000000000000000, 0.000000000000000000 ) ) ;
#19106=ORIENTED_EDGE ( 'NONE', *, *, #3702, .F. ) ;
#19108=B_SPLINE_CURVE_WITH_KNOTS ( 'NONE', 3,
 ( #26359, #8445, #6119, #31706 ),
 .UNSPECIFIED., .F., .F.,
 ( 4, 4 ),
 ( 2.049880227751406910E-07, 0.0008064882591616886988 ),
 .UNSPECIFIED. ) ;
#19127=ORIENTED_EDGE ( 'NONE', *, *, #461, .F. ) ;
#19136=EDGE_CURVE ( 'NONE', #3718, #15097, #32218, .T. ) ;
#19151=VERTEX_POINT ( 'NONE', #29700 ) ;
#19169=CARTESIAN_POINT ( 'NONE',  ( 2.357329895872517955, -1.335530315079604735, 10.75444571268657512 ) ) ;
#19175=CARTESIAN_POINT ( 'NONE',  ( 2.661997850953043532, -5.196702353893143389, -8.696442646092096496 ) ) ;
#19182=CARTESIAN_POINT ( 'NONE',  ( 2.592584690696360106, -9.468199582994124341, 4.120115534657283973 ) ) ;
#19184=CARTESIAN_POINT ( 'NONE',  ( 0.000000000000000000, -1.464956435139616930, 10.90201369670498011 ) ) ;
#19194=CARTESIAN_POINT ( 'NONE',  ( 3.249999999999999556, 0.000000000000000000, 0.000000000000000000 ) ) ;
#19197=CARTESIAN_POINT ( 'NONE',  ( 0.7632845268398871230, -4.729683950898817102, -7.360373001730970977 ) ) ;
#19218=LINE ( 'NONE', #19062, #16099 ) ;
#19226=EDGE_LOOP ( 'NONE', ( #23919, #29161, #9416, #6184 ) ) ;
#19227=VERTEX_POINT ( 'NONE', #99 ) ;
#19240=CARTESIAN_POINT ( 'NONE',  ( 0.000000000000000000, 0.000000000000000000, 0.000000000000000000 ) ) ;
#19249=DIRECTION ( 'NONE',  ( 0.000000000000000000, 2.486899575160350335E-14, 1.000000000000000000 ) ) ;
#19251=DIRECTION ( 'NONE',  ( 0.000000000000000000, -0.9510565162951566398, 0.3090169943749382364 ) ) ;
#19269=TOROIDAL_SURFACE ( 'NONE', #23010, 3.895301350492843540, 15.00000000000000178 ) ;
#19270=B_SPLINE_CURVE_WITH_KNOTS ( 'NONE', 3,
 ( #29634, #22417, #24420, #32629, #6715, #16906, #27099, #9710 ),
 .UNSPECIFIED., .F., .F.,
 ( 4, 2, 2, 4 ),
 ( 2.851296507450002721E-07, 0.001262135616845466582, 0.001893060860442827027, 0.002523986104040187688 ),
 .UNSPECIFIED. ) ;
#19275=CARTESIAN_POINT ( 'NONE',  ( 0.000000000000000000, -4.472189673936727949, -8.264486777890155622 ) ) ;
#19281=EDGE_CURVE ( 'NONE', #23666, #24626, #30718, .T. ) ;
#19285=AXIS2_PLACEMENT_3D ( 'NONE', #27239, #4181, #22578 ) ;
#19290=CARTESIAN_POINT ( 'NONE',  ( 2.976845773540289564, 8.532418605434726189, 3.349682859779522737 ) ) ;
#19291=ORIENTED_EDGE ( 'NONE', *, *, #25534, .T. ) ;
#19295=ORIENTED_EDGE ( 'NONE', *, *, #13858, .T. ) ;
#19301=VERTEX_POINT ( 'NONE', #16108 ) ;
#19306=CARTESIAN_POINT ( 'NONE',  ( 0.7632845268398871230, 0.000000000000000000, 0.000000000000000000 ) ) ;
#19321=EDGE_CURVE ( 'NONE', #3441, #20330, #28325, .T. ) ;
#19330=AXIS2_PLACEMENT_3D ( 'NONE', #14396, #22286, #12236 ) ;
#19334=AXIS2_PLACEMENT_3D ( 'NONE', #32074, #1154, #24217 ) ;
#19337=AXIS2_PLACEMENT_3D ( 'NONE', #29527, #6772, #29847 ) ;
#19339=AXIS2_PLACEMENT_3D ( 'NONE', #1674, #29761, #27232 ) ;
#19343=CYLINDRICAL_SURFACE ( 'NONE', #3264, 11.00000000000000000 ) ;
#19344=ORIENTED_EDGE ( 'NONE', *, *, #6356, .F. ) ;
#19346=AXIS2_PLACEMENT_3D ( 'NONE', #19926, #9521, #21906 ) ;
#19350=CARTESIAN_POINT ( 'NONE',  ( 2.976845687893342696, -0.5490754078163165852, 9.149921655307466040 ) ) ;
#19361=EDGE_CURVE ( 'NONE', #16234, #10253, #29035, .T. ) ;
#19362=AXIS2_PLACEMENT_3D ( 'NONE', #15033, #25256, #30790 ) ;
#19367=VECTOR ( 'NONE', #20768, 1000.000000000000000 ) ;
#19375=VECTOR ( 'NONE', #16860, 1000.000000000000000 ) ;
#19379=AXIS2_PLACEMENT_3D ( 'NONE', #30292, #4555, #9381 ) ;
#19396=CARTESIAN_POINT ( 'NONE',  ( -5.750050799999999462, 0.000000000000000000, 0.000000000000000000 ) ) ;
#19398=EDGE_LOOP ( 'NONE', ( #27426, #12288, #3227, #20163 ) ) ;
#19407=DIRECTION ( 'NONE',  ( 0.000000000000000000, 0.000000000000000000, -1.000000000000000000 ) ) ;
#19408=DIRECTION ( 'NONE',  ( 1.000000000000000000, -0.000000000000000000, -0.000000000000000000 ) ) ;
#19418=VECTOR ( 'NONE', #3785, 1000.000000000000000 ) ;
#19428=CARTESIAN_POINT ( 'NONE',  ( 3.249999999999999556, -1.699438267350306120, -9.241976615262172956 ) ) ;
#19429=VERTEX_POINT ( 'NONE', #2070 ) ;
#19457=VERTEX_POINT ( 'NONE', #4739 ) ;
#19461=EDGE_CURVE ( 'NONE', #27353, #25919, #16207, .T. ) ;
#19463=CARTESIAN_POINT ( 'NONE',  ( 0.5704037183048228377, -8.085411865508387308, -5.066169706250034821 ) ) ;
#19471=CARTESIAN_POINT ( 'NONE',  ( 2.661997627134198297, -6.664939678585230176, 7.629706518865833509 ) ) ;
#19479=DIRECTION ( 'NONE',  ( 0.000000000000000000, 0.000000000000000000, -1.000000000000000000 ) ) ;
#19487=AXIS2_PLACEMENT_3D ( 'NONE', #32795, #30125, #27241 ) ;
#19501=CARTESIAN_POINT ( 'NONE',  ( 0.7632845268398871230, -2.223716399045513548, -8.461683424509338636 ) ) ;
#19525=DIRECTION ( 'NONE',  ( 1.000000000000000000, -0.000000000000000000, 0.000000000000000000 ) ) ;
#19531=CARTESIAN_POINT ( 'NONE',  ( 1.624999999999999778, 5.222868219166857173, 9.680994141368792327 ) ) ;
#19555=CARTESIAN_POINT ( 'NONE',  ( 0.7632845268398876781, -0.4999240074893807617, -8.734705317681624948 ) ) ;
#19583=CARTESIAN_POINT ( 'NONE',  ( 0.000000000000000000, 1.464956435139539659, 10.90201369670498899 ) ) ;
#19584=EDGE_CURVE ( 'NONE', #5778, #10585, #27081, .T. ) ;
#19587=DIRECTION ( 'NONE',  ( 1.000000000000000000, -0.000000000000000000, -0.000000000000000000 ) ) ;
#19604=CARTESIAN_POINT ( 'NONE',  ( 3.063284526839890720, 8.461683424509336859, -2.223716399045483794 ) ) ;
#19611=DIRECTION ( 'NONE',  ( -0.000000000000000000, 0.000000000000000000, 1.000000000000000000 ) ) ;
#19619=ORIENTED_EDGE ( 'NONE', *, *, #12415, .T. ) ;
#19630=DIRECTION ( 'NONE',  ( 1.000000000000000000, 0.000000000000000000, 0.000000000000000000 ) ) ;
#19635=EDGE_CURVE ( 'NONE', #31221, #16905, #28800, .T. ) ;
#19636=B_SPLINE_CURVE_WITH_KNOTS ( 'NONE', 3,
 ( #19955, #2401, #24788, #21936, #9398, #24596, #22278, #17069 ),
 .UNSPECIFIED., .F., .F.,
 ( 4, 2, 2, 4 ),
 ( 2.197717205396726239E-07, 0.001262070444981970444, 0.001892995781612686430, 0.002523921118243402199 ),
 .UNSPECIFIED. ) ;
#19638=CARTESIAN_POINT ( 'NONE',  ( -3.671580638170519912E-13, 9.620177616658855513, 5.227991826304058343 ) ) ;
#19641=VERTEX_POINT ( 'NONE', #32129 ) ;
#19645=CARTESIAN_POINT ( 'NONE',  ( 3.249999999999999556, 8.475820894093034852, -4.057423117305301474 ) ) ;
#19655=DIRECTION ( 'NONE',  ( -1.000000000000000000, 0.000000000000000000, 0.000000000000000000 ) ) ;
#19661=CYLINDRICAL_SURFACE ( 'NONE', #29556, 4.000000000000001776 ) ;
#19665=EDGE_CURVE ( 'NONE', #29352, #23090, #25612, .T. ) ;
#19676=CARTESIAN_POINT ( 'NONE',  ( 0.000000000000000000, 0.000000000000000000, 0.000000000000000000 ) ) ;
#19681=CARTESIAN_POINT ( 'NONE',  ( 3.063284526839887167, -8.461683424509331530, 2.223716399045538861 ) ) ;
#19689=LINE ( 'NONE', #9638, #28408 ) ;
#19690=DIRECTION ( 'NONE',  ( -1.000000000000000000, 0.000000000000000000, -0.000000000000000000 ) ) ;
#19702=CARTESIAN_POINT ( 'NONE',  ( 1.624999999999999778, -10.82112760146734765, -1.975651141462353655 ) ) ;
#19705=EDGE_CURVE ( 'NONE', #32002, #7398, #24766, .T. ) ;
#19706=MECHANICAL_CONTEXT ( 'NONE', #520, 'mechanical' ) ;
#19708=CARTESIAN_POINT ( 'NONE',  ( 0.000000000000000000, -5.222868219166924675, 9.680994141368749695 ) ) ;
#19709=AXIS2_PLACEMENT_3D ( 'NONE', #31370, #31042, #28688 ) ;
#19713=CARTESIAN_POINT ( 'NONE',  ( 0.7632845268458183785, 8.152713396062706508, 3.174628368984090176 ) ) ;
#19722=CARTESIAN_POINT ( 'NONE',  ( 3.063284526839887167, 0.000000000000000000, 0.000000000000000000 ) ) ;
#19732=EDGE_CURVE ( 'NONE', #26130, #12480, #29784, .T. ) ;
#19736=ORIENTED_EDGE ( 'NONE', *, *, #22219, .T. ) ;
#19742=LINE ( 'NONE', #15223, #70 ) ;
#19747=FACE_OUTER_BOUND ( 'NONE', #19398, .T. ) ;
#19754=ORIENTED_EDGE ( 'NONE', *, *, #12047, .F. ) ;
#19756=CYLINDRICAL_SURFACE ( 'NONE', #32017, 4.000000000000001776 ) ;
#19758=CARTESIAN_POINT ( 'NONE',  ( 0.000000000000000000, 0.000000000000000000, 0.000000000000000000 ) ) ;
#19763=AXIS2_PLACEMENT_3D ( 'NONE', #26128, #5881, #20951 ) ;
#19778=DIRECTION ( 'NONE',  ( 0.000000000000000000, 0.000000000000000000, -1.000000000000000000 ) ) ;
#19785=ORIENTED_EDGE ( 'NONE', *, *, #17554, .T. ) ;
#19792=ORIENTED_EDGE ( 'NONE', *, *, #19136, .F. ) ;
#19797=CARTESIAN_POINT ( 'NONE',  ( 0.5704035945090657478, -2.319683995708254010, 9.255216539914220775 ) ) ;
#19805=AXIS2_PLACEMENT_3D ( 'NONE', #9006, #12039, #19407 ) ;
#19814=ADVANCED_FACE ( 'NONE', ( #12452 ), #2765, .T. ) ;
#19815=DIRECTION ( 'NONE',  ( -1.000000000000000000, -0.000000000000000000, 0.000000000000000000 ) ) ;
#19819=CARTESIAN_POINT ( 'NONE',  ( 4.183205650141505458E-16, -1.999317321091424793, -10.76487093102067050 ) ) ;
#19824=AXIS2_PLACEMENT_3D ( 'NONE', #20242, #2379, #12207 ) ;
#19844=DIRECTION ( 'NONE',  ( 1.000000000000000000, 0.000000000000000000, -0.000000000000000000 ) ) ;
#19854=CYLINDRICAL_SURFACE ( 'NONE', #27936, 11.00000000000000000 ) ;
#19856=CARTESIAN_POINT ( 'NONE',  ( 0.7632845268398871230, -0.4999240074895051067, 8.734705317681624948 ) ) ;
#19865=ORIENTED_EDGE ( 'NONE', *, *, #30881, .T. ) ;
#19882=EDGE_LOOP ( 'NONE', ( #23871, #3370, #13171, #27730, #17779 ) ) ;
#19885=ADVANCED_FACE ( 'NONE', ( #30368 ), #5281, .T. ) ;
#19889=CARTESIAN_POINT ( 'NONE',  ( 0.000000000000000000, 7.593217523260579860, 7.958834565716794707 ) ) ;
#19892=AXIS2_PLACEMENT_3D ( 'NONE', #5951, #16146, #19611 ) ;
#19895=CIRCLE ( 'NONE', #25200, 3.499999999999999556 ) ;
#19904=CARTESIAN_POINT ( 'NONE',  ( 2.425585535379221280, -9.314797388879910045, 5.239665997526856245 ) ) ;
#19906=AXIS2_PLACEMENT_3D ( 'NONE', #25751, #2882, #13048 ) ;
#19914=EDGE_CURVE ( 'NONE', #689, #5903, #7626, .T. ) ;
#19915=FACE_OUTER_BOUND ( 'NONE', #30002, .T. ) ;
#19926=CARTESIAN_POINT ( 'NONE',  ( 2.274274201625327230, 0.000000000000000000, 0.000000000000000000 ) ) ;
#19940=ORIENTED_EDGE ( 'NONE', *, *, #6899, .F. ) ;
#19943=DIRECTION ( 'NONE',  ( 0.000000000000000000, -0.8090169943749532244, 0.5877852522924653655 ) ) ;
#19955=CARTESIAN_POINT ( 'NONE',  ( 2.274274201625327230, -7.958834565716822240, 7.593217523260554103 ) ) ;
#19959=CARTESIAN_POINT ( 'NONE',  ( 0.000000000000000000, 0.000000000000000000, 0.000000000000000000 ) ) ;
#19962=CARTESIAN_POINT ( 'NONE',  ( 0.7632845268398871230, -8.461683424509292450, -2.223716399045660985 ) ) ;
#19975=CARTESIAN_POINT ( 'NONE',  ( 2.274274201625317460, -7.593217523260661572, 7.958834565716747633 ) ) ;
#19976=VERTEX_POINT ( 'NONE', #20820 ) ;
#19979=CARTESIAN_POINT ( 'NONE',  ( 0.000000000000000000, -8.475820894093002877, 4.057423117305364535 ) ) ;
#19990=ORIENTED_EDGE ( 'NONE', *, *, #30881, .F. ) ;
#20002=CARTESIAN_POINT ( 'NONE',  ( 0.7632845268398871230, 7.360373001730917686, 4.729683950898899703 ) ) ;
#20006=CARTESIAN_POINT ( 'NONE',  ( 0.5640491644726027820, -2.305464659958381901, -9.257234168482330716 ) ) ;
#20014=ORIENTED_EDGE ( 'NONE', *, *, #31082, .T. ) ;
#20031=EDGE_CURVE ( 'NONE', #1745, #15594, #29344, .T. ) ;
#20041=EDGE_CURVE ( 'NONE', #25919, #23564, #14766, .T. ) ;
#20049=EDGE_CURVE ( 'NONE', #32897, #6905, #18338, .T. ) ;
#20065=ADVANCED_FACE ( 'NONE', ( #9073 ), #1266, .T. ) ;
#20067=CARTESIAN_POINT ( 'NONE',  ( 2.440333456259505596, 1.206185435486435864, 10.60697035673404187 ) ) ;
#20080=CARTESIAN_POINT ( 'NONE',  ( 2.857988133321602842, 6.150950518050580129, 7.318787950824131805 ) ) ;
#20109=ORIENTED_EDGE ( 'NONE', *, *, #5979, .T. ) ;
#20111=DIRECTION ( 'NONE',  ( -1.000000000000000000, -0.000000000000000000, -0.000000000000000000 ) ) ;
#20115=EDGE_LOOP ( 'NONE', ( #24412, #24423, #13395, #11892 ) ) ;
#20132=DIRECTION ( 'NONE',  ( -1.000000000000000000, 0.000000000000000000, 0.000000000000000000 ) ) ;
#20139=DIRECTION ( 'NONE',  ( -1.000000000000000000, 0.000000000000000000, 0.000000000000000000 ) ) ;
#20141=EDGE_LOOP ( 'NONE', ( #9370, #3241, #3409, #26149, #13266 ) ) ;
#20148=FACE_OUTER_BOUND ( 'NONE', #21750, .T. ) ;
#20149=DIRECTION ( 'NONE',  ( -1.000000000000000000, 0.000000000000000000, -0.000000000000000000 ) ) ;
#20161=CARTESIAN_POINT ( 'NONE',  ( 0.5704036742842227836, 3.563415854978491115, 8.851103337321282183 ) ) ;
#20163=ORIENTED_EDGE ( 'NONE', *, *, #23814, .T. ) ;
#20172=CARTESIAN_POINT ( 'NONE',  ( 0.4892055063894280575, 9.505891060653322455, 2.300561732651089653 ) ) ;
#20183=ORIENTED_EDGE ( 'NONE', *, *, #12571, .F. ) ;
#20187=CARTESIAN_POINT ( 'NONE',  ( 2.357329994281655239, -2.053141773251381252, -10.64078702437733881 ) ) ;
#20205=EDGE_CURVE ( 'NONE', #596, #20676, #13864, .T. ) ;
#20207=ORIENTED_EDGE ( 'NONE', *, *, #19705, .T. ) ;
#20231=ADVANCED_FACE ( 'NONE', ( #10252 ), #5411, .T. ) ;
#20239=CARTESIAN_POINT ( 'NONE',  ( 2.440333863881507526, 7.872241054360261003, -7.210444323284713519 ) ) ;
#20242=CARTESIAN_POINT ( 'NONE',  ( 3.249999999999999556, 0.000000000000000000, 0.000000000000000000 ) ) ;
#20266=DIRECTION ( 'NONE',  ( 0.000000000000000000, 0.000000000000000000, -1.000000000000000000 ) ) ;
#20272=CARTESIAN_POINT ( 'NONE',  ( 0.08034253656914176756, -9.429377841196146193, -5.242601083769383941 ) ) ;
#20280=PLANE ( 'NONE',  #25308 ) ;
#20288=DIRECTION ( 'NONE',  ( 0.000000000000000000, 0.000000000000000000, -1.000000000000000000 ) ) ;
#20290=ORIENTED_EDGE ( 'NONE', *, *, #30760, .T. ) ;
#20301=DIRECTION ( 'NONE',  ( 1.000000000000000000, 0.000000000000000000, 0.000000000000000000 ) ) ;
#20302=CYLINDRICAL_SURFACE ( 'NONE', #3925, 8.749000000000002331 ) ;
#20307=EDGE_CURVE ( 'NONE', #28679, #7524, #15482, .T. ) ;
#20321=CARTESIAN_POINT ( 'NONE',  ( -3.672954038633582391E-13, 4.709950686175357504, 9.884132761439534676 ) ) ;
#20327=DIRECTION ( 'NONE',  ( -1.000000000000000000, 0.000000000000000000, 0.000000000000000000 ) ) ;
#20330=VERTEX_POINT ( 'NONE', #21126 ) ;
#20331=ORIENTED_EDGE ( 'NONE', *, *, #16235, .F. ) ;
#20334=DIRECTION ( 'NONE',  ( 0.000000000000000000, 0.000000000000000000, 1.000000000000000000 ) ) ;
#20345=AXIS2_PLACEMENT_3D ( 'NONE', #18035, #30599, #32777 ) ;
#20354=DIRECTION ( 'NONE',  ( 1.000000000000000000, -0.000000000000000000, -0.000000000000000000 ) ) ;
#20369=VECTOR ( 'NONE', #23152, 1000.000000000000000 ) ;
#20373=SHAPE_DEFINITION_REPRESENTATION ( #22298, #8974 ) ;
#20381=EDGE_LOOP ( 'NONE', ( #16095, #12037, #29789, #2647 ) ) ;
#20387=VERTEX_POINT ( 'NONE', #26468 ) ;
#20393=EDGE_CURVE ( 'NONE', #8056, #32762, #18275, .T. ) ;
#20401=CIRCLE ( 'NONE', #30552, 4.000000000000001776 ) ;
#20402=EDGE_CURVE ( 'NONE', #6314, #24805, #21874, .T. ) ;
#20411=ORIENTED_EDGE ( 'NONE', *, *, #30633, .F. ) ;
#20426=ORIENTED_EDGE ( 'NONE', *, *, #15050, .T. ) ;
#20433=LINE ( 'NONE', #30650, #17095 ) ;
#20445=VECTOR ( 'NONE', #18089, 1000.000000000000000 ) ;
#20453=CARTESIAN_POINT ( 'NONE',  ( 0.1574692315735313208, -9.238013023060274165, -5.243558859478258505 ) ) ;
#20464=CARTESIAN_POINT ( 'NONE',  ( 3.063284526839887167, -8.461683424509331530, 2.223716399045538861 ) ) ;
#20472=CARTESIAN_POINT ( 'NONE',  ( 0.000000000000000000, 5.222868219166995729, -9.680994141368712391 ) ) ;
#20477=ORIENTED_EDGE ( 'NONE', *, *, #19321, .T. ) ;
#20481=CIRCLE ( 'NONE', #10321, 10.99999999999999822 ) ;
#20487=CARTESIAN_POINT ( 'NONE',  ( 2.274274201627632053, 10.82112760146237029, 1.975651141464422000 ) ) ;
#20493=CARTESIAN_POINT ( 'NONE',  ( 1.624999999999999778, 7.593217523260583413, 7.958834565716794707 ) ) ;
#20497=CARTESIAN_POINT ( 'NONE',  ( -5.749676575031998027, 8.479088208361000873E-16, 6.923700951379999857 ) ) ;
#20511=ORIENTED_EDGE ( 'NONE', *, *, #24743, .T. ) ;
#20523=ORIENTED_EDGE ( 'NONE', *, *, #27316, .T. ) ;
#20524=AXIS2_PLACEMENT_3D ( 'NONE', #10474, #30888, #5638 ) ;
#20529=CARTESIAN_POINT ( 'NONE',  ( 3.249999999999999556, -6.772677083992426184, 5.538577986808876474 ) ) ;
#20530=ORIENTED_EDGE ( 'NONE', *, *, #26506, .F. ) ;
#20550=DIRECTION ( 'NONE',  ( -1.000000000000000000, 0.000000000000000000, -0.000000000000000000 ) ) ;
#20553=CARTESIAN_POINT ( 'NONE',  ( 3.063284526845908129, -0.4999240074859571670, -8.734705317652709411 ) ) ;
#20570=CARTESIAN_POINT ( 'NONE',  ( 1.624999999999999778, -10.90201369670499965, 1.464956435139505908 ) ) ;
#20585=CARTESIAN_POINT ( 'NONE',  ( 2.592584925145450470, 7.731606906650982047, -6.844296717726155777 ) ) ;
#20589=ORIENTED_EDGE ( 'NONE', *, *, #15371, .F. ) ;
#20590=ADVANCED_FACE ( 'NONE', ( #2296 ), #7443, .T. ) ;
#20591=FACE_OUTER_BOUND ( 'NONE', #4586, .T. ) ;
#20597=ORIENTED_EDGE ( 'NONE', *, *, #29639, .T. ) ;
#20600=DIRECTION ( 'NONE',  ( 0.000000000000000000, 0.000000000000000000, -1.000000000000000000 ) ) ;
#20606=EDGE_CURVE ( 'NONE', #5744, #32789, #13851, .T. ) ;
#20614=DIRECTION ( 'NONE',  ( 0.000000000000000000, 1.000000000000000000, -1.224646799147353207E-16 ) ) ;
#20625=ORIENTED_EDGE ( 'NONE', *, *, #28094, .F. ) ;
#20635=CARTESIAN_POINT ( 'NONE',  ( 3.063284526839890276, 0.4999240074895630048, -8.734705317681616066 ) ) ;
#20637=ORIENTED_EDGE ( 'NONE', *, *, #29892, .F. ) ;
#20643=DIRECTION ( 'NONE',  ( -1.000000000000000000, -0.000000000000000000, 0.000000000000000000 ) ) ;
#20667=DIRECTION ( 'NONE',  ( 1.000000000000000000, 0.000000000000000000, -0.000000000000000000 ) ) ;
#20670=( LENGTH_UNIT ( ) NAMED_UNIT ( * ) SI_UNIT ( .MILLI., .METRE. ) );
#20676=VERTEX_POINT ( 'NONE', #18637 ) ;
#20686=CARTESIAN_POINT ( 'NONE',  ( 0.5640491644773603097, 9.257234168466334623, -2.305464659958512907 ) ) ;
#20693=DIRECTION ( 'NONE',  ( -1.000000000000000000, -0.000000000000000000, -0.000000000000000000 ) ) ;
#20703=EDGE_CURVE ( 'NONE', #3275, #32538, #18986, .T. ) ;
#20716=DIRECTION ( 'NONE',  ( 0.000000000000000000, 0.000000000000000000, 1.000000000000000000 ) ) ;
#20719=CARTESIAN_POINT ( 'NONE',  ( 3.063284526839887167, 0.4999240074894433228, 8.734705317681628500 ) ) ;
#20735=CARTESIAN_POINT ( 'NONE',  ( 0.5640491644773562019, 2.305464659958607943, 9.257234168466320412 ) ) ;
#20736=CARTESIAN_POINT ( 'NONE',  ( 2.387277105415073208, -10.57576230868571976, 2.081082275505834023 ) ) ;
#20743=ORIENTED_EDGE ( 'NONE', *, *, #9397, .F. ) ;
#20759=CARTESIAN_POINT ( 'NONE',  ( 0.6791199890552934715, -7.071625480714427425, 5.814932665552373869 ) ) ;
#20768=DIRECTION ( 'NONE',  ( -1.000000000000000000, 0.000000000000000000, -0.000000000000000000 ) ) ;
#20780=ORIENTED_EDGE ( 'NONE', *, *, #28224, .T. ) ;
#20782=ORIENTED_EDGE ( 'NONE', *, *, #5258, .T. ) ;
#20783=DIRECTION ( 'NONE',  ( -1.000000000000000000, 0.000000000000000000, 0.000000000000000000 ) ) ;
#20798=DIRECTION ( 'NONE',  ( 1.000000000000000000, 0.000000000000000000, 0.000000000000000000 ) ) ;
#20804=DIRECTION ( 'NONE',  ( 0.000000000000000000, -0.3090169943749551673, 0.9510565162951511997 ) ) ;
#20813=FACE_OUTER_BOUND ( 'NONE', #1841, .T. ) ;
#20815=AXIS2_PLACEMENT_3D ( 'NONE', #2365, #10021, #30277 ) ;
#20820=CARTESIAN_POINT ( 'NONE',  ( 0.7632845268398871230, 5.538577986808899567, 6.772677083992407532 ) ) ;
#20825=AXIS2_PLACEMENT_3D ( 'NONE', #9582, #20301, #10265 ) ;
#20827=CARTESIAN_POINT ( 'NONE',  ( 0.3076689118644526655, -9.439351442248995028, -4.089891983583746615 ) ) ;
#20846=AXIS2_PLACEMENT_3D ( 'NONE', #17782, #20139, #22799 ) ;
#20870=FACE_OUTER_BOUND ( 'NONE', #15905, .T. ) ;
#20874=ORIENTED_EDGE ( 'NONE', *, *, #23022, .F. ) ;
#20876=B_SPLINE_CURVE_WITH_KNOTS ( 'NONE', 3,
 ( #20635, #2938, #30841, #8255, #3084, #400, #12744, #27990 ),
 .UNSPECIFIED., .F., .F.,
 ( 4, 2, 2, 4 ),
 ( 2.024520226828864513E-07, 0.001261135997420233463, 0.001891602770119006583, 0.002522069542817780355 ),
 .UNSPECIFIED. ) ;
#20889=VECTOR ( 'NONE', #30375, 1000.000000000000000 ) ;
#20890=DIRECTION ( 'NONE',  ( 0.000000000000000000, -0.8090169943749403458, -0.5877852522924831291 ) ) ;
#20891=CARTESIAN_POINT ( 'NONE',  ( 0.7632845268398871230, 0.000000000000000000, 0.000000000000000000 ) ) ;
#20895=ORIENTED_EDGE ( 'NONE', *, *, #3904, .F. ) ;
#20907=DIRECTION ( 'NONE',  ( 0.000000000000000000, 0.000000000000000000, 1.000000000000000000 ) ) ;
#20918=CARTESIAN_POINT ( 'NONE',  ( 2.274274201625327230, 0.000000000000000000, 0.000000000000000000 ) ) ;
#20921=CARTESIAN_POINT ( 'NONE',  ( 0.3045633657615048895, -7.698316278340158192, 6.808202580038414276 ) ) ;
#20925=CARTESIAN_POINT ( 'NONE',  ( 2.274274201625327230, 0.000000000000000000, 0.000000000000000000 ) ) ;
#20928=DIRECTION ( 'NONE',  ( -1.000000000000000000, 0.000000000000000000, -0.000000000000000000 ) ) ;
#20931=CARTESIAN_POINT ( 'NONE',  ( 2.592584690696363214, -4.120115534657249334, -9.468199582994131447 ) ) ;
#20940=CARTESIAN_POINT ( 'NONE',  ( 2.942065251340673093, -8.983930386558810710, 2.300561732648069402 ) ) ;
#20943=CIRCLE ( 'NONE', #8640, 10.99999999999999822 ) ;
#20946=ORIENTED_EDGE ( 'NONE', *, *, #24672, .T. ) ;
#20951=DIRECTION ( 'NONE',  ( 0.000000000000000000, 0.9510565162951544194, -0.3090169943749446202 ) ) ;
#20956=EDGE_CURVE ( 'NONE', #1130, #24612, #4925, .T. ) ;
#20958=DIRECTION ( 'NONE',  ( 0.000000000000000000, 0.000000000000000000, -1.000000000000000000 ) ) ;
#20965=LINE ( 'NONE', #17964, #11809 ) ;
#20969=CARTESIAN_POINT ( 'NONE',  ( 2.795120570939532367, 3.714272345039596246, 9.022485053488384921 ) ) ;
#20975=AXIS2_PLACEMENT_3D ( 'NONE', #22547, #14831, #15335 ) ;
#20977=DIRECTION ( 'NONE',  ( -1.000000000000000000, 0.000000000000000000, 0.000000000000000000 ) ) ;
#20978=ORIENTED_EDGE ( 'NONE', *, *, #1543, .T. ) ;
#20979=CARTESIAN_POINT ( 'NONE',  ( 2.274274201625327230, 0.000000000000000000, 0.000000000000000000 ) ) ;
#20982=ORIENTED_EDGE ( 'NONE', *, *, #31592, .F. ) ;
#20987=DIRECTION ( 'NONE',  ( -1.000000000000000000, -0.000000000000000000, 0.000000000000000000 ) ) ;
#20988=CARTESIAN_POINT ( 'NONE',  ( 1.624999999999999778, -10.90201369670497833, -1.464956435139658231 ) ) ;
#20993=AXIS2_PLACEMENT_3D ( 'NONE', #27926, #7705, #28240 ) ;
#21004=ORIENTED_EDGE ( 'NONE', *, *, #30430, .T. ) ;
#21009=DIRECTION ( 'NONE',  ( 0.000000000000000000, 0.000000000000000000, 1.000000000000000000 ) ) ;
#21016=DIRECTION ( 'NONE',  ( 1.000000000000000000, 0.000000000000000000, 0.000000000000000000 ) ) ;
#21024=B_SPLINE_CURVE_WITH_KNOTS ( 'NONE', 3,
 ( #29569, #19033, #16845, #14312, #24362, #9134, #3998, #6807 ),
 .UNSPECIFIED., .F., .F.,
 ( 4, 2, 2, 4 ),
 ( 5.099451029791657500E-07, 0.001229189590460676770, 0.001843529413139525413, 0.002457869235818374055 ),
 .UNSPECIFIED. ) ;
#21058=CARTESIAN_POINT ( 'NONE',  ( 3.249999999999999556, -9.241976615262146311, -1.699438267350472209 ) ) ;
#21059=ORIENTED_EDGE ( 'NONE', *, *, #31104, .T. ) ;
#21078=EDGE_LOOP ( 'NONE', ( #31725, #6825, #29317, #14384 ) ) ;
#21082=ORIENTED_EDGE ( 'NONE', *, *, #5362, .T. ) ;
#21088=EDGE_LOOP ( 'NONE', ( #30169, #10122, #21786, #2867 ) ) ;
#21089=ORIENTED_EDGE ( 'NONE', *, *, #22893, .F. ) ;
#21103=CARTESIAN_POINT ( 'NONE',  ( 3.063284526839887167, 0.000000000000000000, 0.000000000000000000 ) ) ;
#21104=EDGE_CURVE ( 'NONE', #23564, #18851, #8560, .T. ) ;
#21106=CARTESIAN_POINT ( 'NONE',  ( 9.101556641444268791, 4.770368330595423290E-16, 3.895301350492843540 ) ) ;
#21115=B_SPLINE_CURVE_WITH_KNOTS ( 'NONE', 3,
 ( #4955, #2608, #12131, #30363, #12773, #22982, #25348, #30721 ),
 .UNSPECIFIED., .F., .F.,
 ( 4, 2, 2, 4 ),
 ( 2.737843117452289853E-07, 0.001261207499628671418, 0.001891674357287133779, 0.002522141214945596357 ),
 .UNSPECIFIED. ) ;
#21116=CARTESIAN_POINT ( 'NONE',  ( 0.000000000000000000, 0.000000000000000000, 0.000000000000000000 ) ) ;
#21120=LINE ( 'NONE', #29272, #30557 ) ;
#21123=CARTESIAN_POINT ( 'NONE',  ( 0.000000000000000000, 6.807171995660674213, -6.478011392632816445 ) ) ;
#21126=CARTESIAN_POINT ( 'NONE',  ( 2.274274201625327230, 9.915734732513220351, 4.762163868918306342 ) ) ;
#21148=EDGE_CURVE ( 'NONE', #2834, #4033, #24565, .T. ) ;
#21173=CARTESIAN_POINT ( 'NONE',  ( 0.3076688774149766714, 10.04057401064417654, -2.239519426675632197 ) ) ;
#21202=ORIENTED_EDGE ( 'NONE', *, *, #19584, .F. ) ;
#21220=CARTESIAN_POINT ( 'NONE',  ( 0.5704036742843073826, -8.851103337321047704, 3.563415854978290387 ) ) ;
#21238=DIRECTION ( 'NONE',  ( -1.000000000000000000, -0.000000000000000000, 0.000000000000000000 ) ) ;
#21243=ORIENTED_EDGE ( 'NONE', *, *, #20049, .T. ) ;
#21253=EDGE_CURVE ( 'NONE', #19227, #2042, #20433, .T. ) ;
#21254=EDGE_CURVE ( 'NONE', #7219, #12210, #17626, .T. ) ;
#21262=CARTESIAN_POINT ( 'NONE',  ( 1.624999999999999778, 10.90201369670498721, -1.464956435139580515 ) ) ;
#21267=ORIENTED_EDGE ( 'NONE', *, *, #15312, .T. ) ;
#21268=EDGE_CURVE ( 'NONE', #16695, #12771, #1298, .T. ) ;
#21270=DIRECTION ( 'NONE',  ( 0.000000000000000000, 0.000000000000000000, 1.000000000000000000 ) ) ;
#21281=DIRECTION ( 'NONE',  ( 0.000000000000000000, 0.3090169943749412895, 0.9510565162951555296 ) ) ;
#21294=CARTESIAN_POINT ( 'NONE',  ( 2.661997753583468906, 10.09011512947409805, 0.9074203448822234508 ) ) ;
#21300=EDGE_CURVE ( 'NONE', #32970, #15150, #6086, .T. ) ;
#21310=CARTESIAN_POINT ( 'NONE',  ( 0.000000000000000000, 0.000000000000000000, 0.000000000000000000 ) ) ;
#21335=AXIS2_PLACEMENT_3D ( 'NONE', #17679, #4196, #27094 ) ;
#21339=ORIENTED_EDGE ( 'NONE', *, *, #6899, .T. ) ;
#21341=CIRCLE ( 'NONE', #12782, 11.00000000000000000 ) ;
#21346=EDGE_CURVE ( 'NONE', #28496, #31361, #3779, .T. ) ;
#21353=CARTESIAN_POINT ( 'NONE',  ( 0.1574692247319865734, 10.55579611470142609, -1.187839595765044942 ) ) ;
#21365=CIRCLE ( 'NONE', #20825, 4.000000000000001776 ) ;
#21388=ADVANCED_FACE ( 'NONE', ( #10543 ), #8696, .T. ) ;
#21391=CARTESIAN_POINT ( 'NONE',  ( 0.6791197464446975252, -9.138998021039022035, 0.5477823182330348040 ) ) ;
#21399=CARTESIAN_POINT ( 'NONE',  ( 0.3749742512057836485, -5.190538276685865426, 8.659825570211395984 ) ) ;
#21415=LINE ( 'NONE', #8385, #10232 ) ;
#21417=CARTESIAN_POINT ( 'NONE',  ( 3.063284526846069777, -2.223716399039799452, 8.461683424479977234 ) ) ;
#21420=ORIENTED_EDGE ( 'NONE', *, *, #26052, .F. ) ;
#21422=AXIS2_PLACEMENT_3D ( 'NONE', #28161, #18121, #27823 ) ;
#21423=CARTESIAN_POINT ( 'NONE',  ( 2.592584690691854821, 9.468199583002103736, -4.120115534666250134 ) ) ;
#21429=CIRCLE ( 'NONE', #32664, 4.000000000000001776 ) ;
#21431=FACE_OUTER_BOUND ( 'NONE', #6569, .T. ) ;
#21451=CARTESIAN_POINT ( 'NONE',  ( 2.437082427505626203, 4.432669656489596655, -9.703015696712895988 ) ) ;
#21452=FACE_OUTER_BOUND ( 'NONE', #1262, .T. ) ;
#21461=CIRCLE ( 'NONE', #19339, 10.00000000000000355 ) ;
#21467=AXIS2_PLACEMENT_3D ( 'NONE', #894, #11071, #19251 ) ;
#21482=EDGE_LOOP ( 'NONE', ( #10664, #4773, #28168, #30143 ) ) ;
#21484=EDGE_CURVE ( 'NONE', #24130, #16234, #4819, .T. ) ;
#21486=AXIS2_PLACEMENT_3D ( 'NONE', #10598, #20977, #20804 ) ;
#21498=CIRCLE ( 'NONE', #1213, 4.000000000000001776 ) ;
#21511=CARTESIAN_POINT ( 'NONE',  ( 2.425585535373192325, 9.314797388894900720, 5.239665997526921970 ) ) ;
#21522=ADVANCED_FACE ( 'NONE', ( #29602 ), #11864, .T. ) ;
#21526=ADVANCED_FACE ( 'NONE', ( #9175 ), #19063, .T. ) ;
#21539=AXIS2_PLACEMENT_3D ( 'NONE', #12698, #28096, #14866 ) ;
#21562=ADVANCED_FACE ( 'NONE', ( #9502 ), #6837, .T. ) ;
#21570=DIRECTION ( 'NONE',  ( -1.000000000000000000, -0.000000000000000000, -0.000000000000000000 ) ) ;
#21574=CYLINDRICAL_SURFACE ( 'NONE', #7064, 4.000000000000001776 ) ;
#21590=CARTESIAN_POINT ( 'NONE',  ( 2.274274201625327230, -4.762163868918204201, -9.915734732513268312 ) ) ;
#21592=EDGE_CURVE ( 'NONE', #30798, #23666, #17070, .T. ) ;
#21628=DIRECTION ( 'NONE',  ( 1.000000000000000000, -0.000000000000000000, -0.000000000000000000 ) ) ;
#21629=EDGE_CURVE ( 'NONE', #24805, #17980, #14945, .T. ) ;
#21630=DIRECTION ( 'NONE',  ( 0.000000000000000000, 0.000000000000000000, 1.000000000000000000 ) ) ;
#21631=ADVANCED_FACE ( 'NONE', ( #23232 ), #5517, .T. ) ;
#21635=CARTESIAN_POINT ( 'NONE',  ( 3.063284526839888944, 8.152713396088756781, 3.174628368996099681 ) ) ;
#21640=ORIENTED_EDGE ( 'NONE', *, *, #29137, .F. ) ;
#21643=CARTESIAN_POINT ( 'NONE',  ( 3.249999999999999556, -8.264486777890139635, 4.472189673936756371 ) ) ;
#21645=ORIENTED_EDGE ( 'NONE', *, *, #14208, .T. ) ;
#21647=EDGE_CURVE ( 'NONE', #23090, #29226, #18679, .T. ) ;
#21656=CARTESIAN_POINT ( 'NONE',  ( 3.063284526839887167, 4.729683950898978750, -7.360373001730866171 ) ) ;
#21659=DIRECTION ( 'NONE',  ( 0.000000000000000000, 0.000000000000000000, 1.000000000000000000 ) ) ;
#21661=EDGE_CURVE ( 'NONE', #9818, #18033, #3507, .T. ) ;
#21664=LINE ( 'NONE', #17076, #16673 ) ;
#21670=ORIENTED_EDGE ( 'NONE', *, *, #12216, .T. ) ;
#21672=CARTESIAN_POINT ( 'NONE',  ( 3.249999999999999556, 1.699438267350371179, 9.241976615262162298 ) ) ;
#21695=DIRECTION ( 'NONE',  ( 1.000000000000000000, 0.000000000000000000, 0.000000000000000000 ) ) ;
#21711=CARTESIAN_POINT ( 'NONE',  ( 0.6728001243833413580, -4.913284922779170394, -7.719803900032154331 ) ) ;
#21735=ADVANCED_FACE ( 'NONE', ( #10844 ), #28722, .T. ) ;
#21750=EDGE_LOOP ( 'NONE', ( #25939, #11987, #12634, #9616 ) ) ;
#21756=CARTESIAN_POINT ( 'NONE',  ( 3.063284526839887167, 0.000000000000000000, 0.000000000000000000 ) ) ;
#21765=ORIENTED_EDGE ( 'NONE', *, *, #17786, .T. ) ;
#21771=EDGE_LOOP ( 'NONE', ( #23026, #499, #32922, #968 ) ) ;
#21780=CARTESIAN_POINT ( 'NONE',  ( 0.3749743548324803166, 0.8908839545096812751, 10.05686762493600384 ) ) ;
#21783=ORIENTED_EDGE ( 'NONE', *, *, #30760, .F. ) ;
#21784=CARTESIAN_POINT ( 'NONE',  ( 2.864531314636029613, -6.140839842381227598, 7.330015575757884427 ) ) ;
#21786=ORIENTED_EDGE ( 'NONE', *, *, #15336, .F. ) ;
#21791=EDGE_LOOP ( 'NONE', ( #4316, #29288, #24812, #3754 ) ) ;
#21795=EDGE_LOOP ( 'NONE', ( #747, #27071, #27754, #24149, #1808 ) ) ;
#21800=CARTESIAN_POINT ( 'NONE',  ( 0.000000000000000000, 0.000000000000000000, 0.000000000000000000 ) ) ;
#21810=DIRECTION ( 'NONE',  ( -1.000000000000000000, 0.000000000000000000, 0.000000000000000000 ) ) ;
#21836=CARTESIAN_POINT ( 'NONE',  ( -5.749676575031998027, 0.000000000000000000, 0.000000000000000000 ) ) ;
#21842=DIRECTION ( 'NONE',  ( -1.000000000000000000, 0.000000000000000000, 0.000000000000000000 ) ) ;
#21848=DIRECTION ( 'NONE',  ( -1.000000000000000000, 0.000000000000000000, 0.000000000000000000 ) ) ;
#21849=CARTESIAN_POINT ( 'NONE',  ( 2.857987970441405956, -8.861329655858749987, 3.588272043363009534 ) ) ;
#21874=CIRCLE ( 'NONE', #19763, 4.000000000000002665 ) ;
#21875=DIRECTION ( 'NONE',  ( 0.000000000000000000, 0.9510565162951523099, 0.3090169943749516701 ) ) ;
#21876=ORIENTED_EDGE ( 'NONE', *, *, #18777, .F. ) ;
#21877=ORIENTED_EDGE ( 'NONE', *, *, #30395, .T. ) ;
#21906=DIRECTION ( 'NONE',  ( 0.000000000000000000, 0.000000000000000000, 1.000000000000000000 ) ) ;
#21912=LINE ( 'NONE', #1699, #25701 ) ;
#21917=ORIENTED_EDGE ( 'NONE', *, *, #4476, .F. ) ;
#21928=EDGE_LOOP ( 'NONE', ( #27984, #20511 ) ) ;
#21931=DIRECTION ( 'NONE',  ( -1.000000000000000000, 0.000000000000000000, 0.000000000000000000 ) ) ;
#21936=CARTESIAN_POINT ( 'NONE',  ( 2.795120667416425508, -7.433119754668519263, 6.320583870820093431 ) ) ;
#21938=CARTESIAN_POINT ( 'NONE',  ( 2.589202905186834158, 4.126870756446594513, -9.453729690310105127 ) ) ;
#21941=CARTESIAN_POINT ( 'NONE',  ( 0.7212198416532934475, -5.676697589997725224, 6.922088825881682617 ) ) ;
#21943=CARTESIAN_POINT ( 'NONE',  ( 0.000000000000000000, 0.000000000000000000, 0.000000000000000000 ) ) ;
#21952=VERTEX_POINT ( 'NONE', #19681 ) ;
#21955=ORIENTED_EDGE ( 'NONE', *, *, #12704, .F. ) ;
#21957=CIRCLE ( 'NONE', #7550, 8.749000000000002331 ) ;
#21958=EDGE_LOOP ( 'NONE', ( #25494, #23583, #22592, #32187 ) ) ;
#21962=ORIENTED_EDGE ( 'NONE', *, *, #31416, .F. ) ;
#21967=CARTESIAN_POINT ( 'NONE',  ( 0.3045634635874763796, 2.226307684702712120, -10.03290811084087508 ) ) ;
#21974=LINE ( 'NONE', #11612, #29028 ) ;
#21975=VECTOR ( 'NONE', #24436, 1000.000000000000000 ) ;
#21982=AXIS2_PLACEMENT_3D ( 'NONE', #7399, #10071, #2930 ) ;
#21983=AXIS2_PLACEMENT_3D ( 'NONE', #5507, #2846, #20716 ) ;
#21987=CARTESIAN_POINT ( 'NONE',  ( 3.063284526843245370, -8.152713396074034335, 3.174628368989241611 ) ) ;
#22008=DIRECTION ( 'NONE',  ( 0.000000000000000000, 0.000000000000000000, 1.000000000000000000 ) ) ;
#22022=CARTESIAN_POINT ( 'NONE',  ( 2.357330042320751939, -5.240837896778892890, -9.485534025193874896 ) ) ;
#22027=CARTESIAN_POINT ( 'NONE',  ( 2.274274201621893976, 10.90201369671108722, -1.464956435144929570 ) ) ;
#22030=LINE ( 'NONE', #11651, #45 ) ;
#22034=DIRECTION ( 'NONE',  ( 1.000000000000000000, 0.000000000000000000, 0.000000000000000000 ) ) ;
#22052=ORIENTED_EDGE ( 'NONE', *, *, #4662, .T. ) ;
#22062=DIRECTION ( 'NONE',  ( -1.000000000000000000, 0.000000000000000000, 0.000000000000000000 ) ) ;
#22066=EDGE_LOOP ( 'NONE', ( #23352, #23746, #27838, #14077 ) ) ;
#22101=LINE ( 'NONE', #4195, #11852 ) ;
#22120=CYLINDRICAL_SURFACE ( 'NONE', #30549, 8.749000000000002331 ) ;
#22133=CARTESIAN_POINT ( 'NONE',  ( 0.08034252266819506827, 1.301095883299763667, 10.71005054582427185 ) ) ;
#22142=CARTESIAN_POINT ( 'NONE',  ( 3.249999999999999556, -2.223716399045513548, -8.461683424509336859 ) ) ;
#22143=EDGE_LOOP ( 'NONE', ( #7152, #17735, #8841, #1459 ) ) ;
#22157=CARTESIAN_POINT ( 'NONE',  ( 3.020080166733955185, 2.264483761675466056, -8.666653390702911963 ) ) ;
#22169=EDGE_CURVE ( 'NONE', #4162, #24626, #24035, .T. ) ;
#22197=ORIENTED_EDGE ( 'NONE', *, *, #178, .F. ) ;
#22204=CYLINDRICAL_SURFACE ( 'NONE', #26794, 4.000000000000001776 ) ;
#22213=CARTESIAN_POINT ( 'NONE',  ( 2.437082530871053532, 9.289394354155845690, -5.244446742619389035 ) ) ;
#22214=DIRECTION ( 'NONE',  ( -1.000000000000000000, 0.000000000000000000, 0.000000000000000000 ) ) ;
#22215=EDGE_LOOP ( 'NONE', ( #6113, #26203, #4568, #14416 ) ) ;
#22217=VERTEX_POINT ( 'NONE', #2555 ) ;
#22219=EDGE_CURVE ( 'NONE', #15097, #7918, #18180, .T. ) ;
#22223=DIRECTION ( 'NONE',  ( -1.000000000000000000, 0.000000000000000000, 0.000000000000000000 ) ) ;
#22240=ORIENTED_EDGE ( 'NONE', *, *, #2235, .T. ) ;
#22244=EDGE_CURVE ( 'NONE', #2486, #1971, #12820, .T. ) ;
#22253=EDGE_LOOP ( 'NONE', ( #17695, #16984, #787, #23449 ) ) ;
#22262=DIRECTION ( 'NONE',  ( 1.000000000000000000, -0.000000000000000000, -0.000000000000000000 ) ) ;
#22264=ORIENTED_EDGE ( 'NONE', *, *, #21629, .F. ) ;
#22278=CARTESIAN_POINT ( 'NONE',  ( 3.020080256212050784, -6.926136578642532626, 5.680439424464613474 ) ) ;
#22286=DIRECTION ( 'NONE',  ( -1.000000000000000000, -0.000000000000000000, -0.000000000000000000 ) ) ;
#22291=DIRECTION ( 'NONE',  ( 1.000000000000000000, 0.000000000000000000, 0.000000000000000000 ) ) ;
#22293=EDGE_LOOP ( 'NONE', ( #25630, #9950, #6362, #13961 ) ) ;
#22298=PRODUCT_DEFINITION_SHAPE ( 'NONE', 'NONE',  #28213 ) ;
#22303=EDGE_CURVE ( 'NONE', #32838, #2837, #16055, .T. ) ;
#22329=VERTEX_POINT ( 'NONE', #31616 ) ;
#22330=CARTESIAN_POINT ( 'NONE',  ( 2.558140769686992222, 8.984438712799688531, 5.239665997526921970 ) ) ;
#22340=CYLINDRICAL_SURFACE ( 'NONE', #26748, 8.749000000000002331 ) ;
#22343=ORIENTED_EDGE ( 'NONE', *, *, #25349, .F. ) ;
#22348=DIRECTION ( 'NONE',  ( -1.000000000000000000, 0.000000000000000000, 0.000000000000000000 ) ) ;
#22349=PLANE ( 'NONE',  #18709 ) ;
#22359=ORIENTED_EDGE ( 'NONE', *, *, #17871, .F. ) ;
#22365=ORIENTED_EDGE ( 'NONE', *, *, #29176, .T. ) ;
#22377=ORIENTED_EDGE ( 'NONE', *, *, #19914, .F. ) ;
#22383=ORIENTED_EDGE ( 'NONE', *, *, #29524, .T. ) ;
#22401=CARTESIAN_POINT ( 'NONE',  ( 0.7212198416586409477, 6.922088825865693629, 5.676697589981143821 ) ) ;
#22414=CIRCLE ( 'NONE', #26173, 3.499999999999999556 ) ;
#22417=CARTESIAN_POINT ( 'NONE',  ( 2.440333456264102363, -10.60697035672505706, 1.206185435479571133 ) ) ;
#22442=ORIENTED_EDGE ( 'NONE', *, *, #18359, .F. ) ;
#22459=CARTESIAN_POINT ( 'NONE',  ( 3.249999999999999556, -1.699438267350438014, 9.241976615262153416 ) ) ;
#22461=ORIENTED_EDGE ( 'NONE', *, *, #17368, .T. ) ;
#22462=VERTEX_POINT ( 'NONE', #7502 ) ;
#22464=EDGE_CURVE ( 'NONE', #28731, #12480, #14451, .T. ) ;
#22466=CARTESIAN_POINT ( 'NONE',  ( 0.6791198108364584485, 8.522429291907643645, -3.345077512921565521 ) ) ;
#22469=ORIENTED_EDGE ( 'NONE', *, *, #30040, .T. ) ;
#22479=CARTESIAN_POINT ( 'NONE',  ( 0.7632845268398871230, 6.772677083992467928, -5.538577986808824960 ) ) ;
#22486=CARTESIAN_POINT ( 'NONE',  ( 3.063284526839887167, 0.000000000000000000, 0.000000000000000000 ) ) ;
#22488=CARTESIAN_POINT ( 'NONE',  ( 0.5032039771567776709, -2.299586922889600871, -9.456648240388242144 ) ) ;
#22493=VECTOR ( 'NONE', #5776, 1000.000000000000000 ) ;
#22502=CIRCLE ( 'NONE', #30513, 8.749000000000002331 ) ;
#22504=ORIENTED_EDGE ( 'NONE', *, *, #17263, .F. ) ;
#22511=CARTESIAN_POINT ( 'NONE',  ( 0.000000000000000000, 8.475820894093034852, -4.057423117305301474 ) ) ;
#22512=CARTESIAN_POINT ( 'NONE',  ( -10.00000000000000000, 0.000000000000000000, 0.000000000000000000 ) ) ;
#22518=EDGE_CURVE ( 'NONE', #19457, #14763, #4327, .T. ) ;
#22521=VERTEX_POINT ( 'NONE', #29546 ) ;
#22525=CARTESIAN_POINT ( 'NONE',  ( 0.7212197595562634955, 0.5238431420063290878, -8.936767016196004221 ) ) ;
#22536=AXIS2_PLACEMENT_3D ( 'NONE', #7161, #14485, #27547 ) ;
#22546=ORIENTED_EDGE ( 'NONE', *, *, #15469, .F. ) ;
#22547=CARTESIAN_POINT ( 'NONE',  ( 3.063284526839887167, 0.000000000000000000, 0.000000000000000000 ) ) ;
#22548=AXIS2_PLACEMENT_3D ( 'NONE', #22459, #24809, #14608 ) ;
#22553=LINE ( 'NONE', #25220, #11747 ) ;
#22562=AXIS2_PLACEMENT_3D ( 'NONE', #24115, #11930, #29812 ) ;
#22567=ORIENTED_EDGE ( 'NONE', *, *, #28904, .T. ) ;
#22569=FACE_OUTER_BOUND ( 'NONE', #5153, .T. ) ;
#22570=AXIS2_PLACEMENT_3D ( 'NONE', #2047, #17261, #30301 ) ;
#22578=DIRECTION ( 'NONE',  ( 0.000000000000000000, 0.000000000000000000, -1.000000000000000000 ) ) ;
#22581=EDGE_CURVE ( 'NONE', #8190, #21952, #9091, .T. ) ;
#22583=ADVANCED_FACE ( 'NONE', ( #24997 ), #19343, .T. ) ;
#22589=AXIS2_PLACEMENT_3D ( 'NONE', #32454, #32798, #24752 ) ;
#22592=ORIENTED_EDGE ( 'NONE', *, *, #27003, .T. ) ;
#22597=CIRCLE ( 'NONE', #14559, 10.94895958125474245 ) ;
#22598=CARTESIAN_POINT ( 'NONE',  ( 2.589202944057212186, 6.846250362091623742, -7.715757980413485484 ) ) ;
#22601=VERTEX_POINT ( 'NONE', #32545 ) ;
#22602=CARTESIAN_POINT ( 'NONE',  ( 2.274274201625327230, -1.975651141462315907, 10.82112760146735475 ) ) ;
#22615=DIRECTION ( 'NONE',  ( 0.000000000000000000, 0.000000000000000000, -1.000000000000000000 ) ) ;
#22622=EDGE_CURVE ( 'NONE', #3542, #12771, #32232, .T. ) ;
#22638=DIRECTION ( 'NONE',  ( 0.000000000000000000, 0.000000000000000000, 1.000000000000000000 ) ) ;
#22640=DIRECTION ( 'NONE',  ( 1.000000000000000000, -0.000000000000000000, -0.000000000000000000 ) ) ;
#22644=ORIENTED_EDGE ( 'NONE', *, *, #32340, .T. ) ;
#22669=CARTESIAN_POINT ( 'NONE',  ( 2.866494652514124830, 9.241976615262203154, 2.300561732649596181 ) ) ;
#22670=DIRECTION ( 'NONE',  ( -1.000000000000000000, 0.000000000000000000, -0.000000000000000000 ) ) ;
#22674=DIRECTION ( 'NONE',  ( 0.000000000000000000, 0.000000000000000000, -1.000000000000000000 ) ) ;
#22691=VERTEX_POINT ( 'NONE', #15017 ) ;
#22694=EDGE_LOOP ( 'NONE', ( #7879, #7254, #9163, #19792, #13596 ) ) ;
#22696=DIRECTION ( 'NONE',  ( 0.000000000000000000, 0.000000000000000000, 1.000000000000000000 ) ) ;
#22713=ORIENTED_EDGE ( 'NONE', *, *, #14313, .F. ) ;
#22716=CARTESIAN_POINT ( 'NONE',  ( -10.00000000000000000, 0.000000000000000000, 0.000000000000000000 ) ) ;
#22723=CARTESIAN_POINT ( 'NONE',  ( 3.063284526839890720, 5.538577986808988385, -6.772677083992317826 ) ) ;
#22745=CARTESIAN_POINT ( 'NONE',  ( 3.020080166740162664, -8.666653390676570368, -2.264483761671786333 ) ) ;
#22750=CARTESIAN_POINT ( 'NONE',  ( 1.624999999999999778, -5.222868219166924675, 9.680994141368755024 ) ) ;
#22755=CARTESIAN_POINT ( 'NONE',  ( 2.274274201625327230, -10.82112760146734765, -1.975651141462354543 ) ) ;
#22761=ORIENTED_EDGE ( 'NONE', *, *, #21253, .F. ) ;
#22769=DIRECTION ( 'NONE',  ( -1.000000000000000000, 0.000000000000000000, 0.000000000000000000 ) ) ;
#22770=ORIENTED_EDGE ( 'NONE', *, *, #30617, .F. ) ;
#22777=VERTEX_POINT ( 'NONE', #8003 ) ;
#22792=ORIENTED_EDGE ( 'NONE', *, *, #26490, .T. ) ;
#22794=ORIENTED_EDGE ( 'NONE', *, *, #25534, .F. ) ;
#22797=VERTEX_POINT ( 'NONE', #25733 ) ;
#22799=DIRECTION ( 'NONE',  ( 0.000000000000000000, 0.000000000000000000, 1.000000000000000000 ) ) ;
#22804=CARTESIAN_POINT ( 'NONE',  ( 0.000000000000000000, -1.999317321091575561, 10.76487093102064030 ) ) ;
#22809=CARTESIAN_POINT ( 'NONE',  ( 3.250000000000001332, 0.000000000000000000, 0.000000000000000000 ) ) ;
#22810=FACE_OUTER_BOUND ( 'NONE', #30769, .T. ) ;
#22823=B_SPLINE_CURVE_WITH_KNOTS ( 'NONE', 3,
 ( #32931, #5014, #4822, #13017, #30593, #17876, #30767, #5323 ),
 .UNSPECIFIED., .F., .F.,
 ( 4, 2, 2, 4 ),
 ( 2.049880227679525047E-07, 0.001227965543375835562, 0.001841845821052371431, 0.002455726098728907517 ),
 .UNSPECIFIED. ) ;
#22832=CARTESIAN_POINT ( 'NONE',  ( -3.449949199999996274, 0.000000000000000000, 0.000000000000000000 ) ) ;
#22849=EDGE_LOOP ( 'NONE', ( #8680, #3755, #29269, #7091, #30136, #30249, #20780, #3378, #1527, #18968, #24241, #31946, #3890, #23385, #10402, #22461, #28019, #26776, #20014, #32862, #15108, #29701, #11201, #1889, #24319, #8404, #4368, #644, #22907, #32495, #21059, #22469, #2038, #11492, #14144, #11092, #22567, #14066, #31894, #28711, #14373, #11227, #24991, #14294, #26466, #2537 ) ) ;
#22852=DIRECTION ( 'NONE',  ( 1.000000000000000000, 0.000000000000000000, 0.000000000000000000 ) ) ;
#22854=EDGE_CURVE ( 'NONE', #7258, #2968, #15855, .T. ) ;
#22856=FACE_OUTER_BOUND ( 'NONE', #12097, .T. ) ;
#22868=DIRECTION ( 'NONE',  ( -1.000000000000000000, 0.000000000000000000, -0.000000000000000000 ) ) ;
#22880=CARTESIAN_POINT ( 'NONE',  ( 0.000000000000000000, -1.425064293572261276, -10.85582367538895632 ) ) ;
#22881=CARTESIAN_POINT ( 'NONE',  ( 2.970200390936398982, 0.5647484630023784646, 9.143933199846962623 ) ) ;
#22885=VERTEX_POINT ( 'NONE', #4144 ) ;
#22887=CARTESIAN_POINT ( 'NONE',  ( 2.274274201625327230, 0.000000000000000000, 0.000000000000000000 ) ) ;
#22891=CARTESIAN_POINT ( 'NONE',  ( 0.5032040285356987885, 3.698073368193082189, -9.002252291012698748 ) ) ;
#22893=EDGE_CURVE ( 'NONE', #17980, #32298, #32063, .T. ) ;
#22903=CARTESIAN_POINT ( 'NONE',  ( 2.857988133321601509, 7.318787950824199307, -6.150950518050498417 ) ) ;
#22906=DIRECTION ( 'NONE',  ( 0.000000000000000000, 0.000000000000000000, 1.000000000000000000 ) ) ;
#22907=ORIENTED_EDGE ( 'NONE', *, *, #31452, .T. ) ;
#22927=EDGE_CURVE ( 'NONE', #27353, #18851, #29881, .T. ) ;
#22934=VECTOR ( 'NONE', #33036, 1000.000000000000000 ) ;
#22940=CARTESIAN_POINT ( 'NONE',  ( 0.000000000000000000, 0.000000000000000000, 0.000000000000000000 ) ) ;
#22946=CARTESIAN_POINT ( 'NONE',  ( 0.08034253207418005915, -4.547003328334541017, -9.783802610459700233 ) ) ;
#22950=ORIENTED_EDGE ( 'NONE', *, *, #15032, .F. ) ;
#22954=ORIENTED_EDGE ( 'NONE', *, *, #3151, .F. ) ;
#22960=DIRECTION ( 'NONE',  ( 0.000000000000000000, 0.000000000000000000, -1.000000000000000000 ) ) ;
#22967=CARTESIAN_POINT ( 'NONE',  ( 3.249999999999999556, 4.057423117305515525, -8.475820894092930047 ) ) ;
#22982=CARTESIAN_POINT ( 'NONE',  ( 2.437082531750073056, 7.858345965138778588, 7.214115859539244724 ) ) ;
#22993=DIRECTION ( 'NONE',  ( -1.000000000000000000, 0.000000000000000000, -0.000000000000000000 ) ) ;
#22995=VERTEX_POINT ( 'NONE', #26553 ) ;
#22997=PLANE ( 'NONE',  #514 ) ;
#22998=AXIS2_PLACEMENT_3D ( 'NONE', #12567, #20111, #30460 ) ;
#22999=AXIS2_PLACEMENT_3D ( 'NONE', #15551, #2896, #13061 ) ;
#23001=CARTESIAN_POINT ( 'NONE',  ( 0.7632845268449858223, 8.461683424485162419, -2.223716399040675196 ) ) ;
#23010=AXIS2_PLACEMENT_3D ( 'NONE', #5046, #19587, #14874 ) ;
#23011=EDGE_CURVE ( 'NONE', #15781, #596, #2738, .T. ) ;
#23022=EDGE_CURVE ( 'NONE', #8063, #2968, #16471, .T. ) ;
#23026=ORIENTED_EDGE ( 'NONE', *, *, #9148, .F. ) ;
#23028=AXIS2_PLACEMENT_3D ( 'NONE', #415, #28657, #23631 ) ;
#23029=CIRCLE ( 'NONE', #2202, 4.000000000000001776 ) ;
#23032=CARTESIAN_POINT ( 'NONE',  ( 2.440333456264101475, -1.206185435479534496, -10.60697035672505706 ) ) ;
#23037=AXIS2_PLACEMENT_3D ( 'NONE', #5500, #26049, #25542 ) ;
#23043=EDGE_CURVE ( 'NONE', #1359, #2488, #10878, .T. ) ;
#23045=CARTESIAN_POINT ( 'NONE',  ( 3.249999999999999556, -8.264486777890077462, -4.472189673936872722 ) ) ;
#23070=CARTESIAN_POINT ( 'NONE',  ( 0.1574692293613787764, -9.672096048330555362, 4.391622967207778672 ) ) ;
#23074=ORIENTED_EDGE ( 'NONE', *, *, #22581, .F. ) ;
#23083=AXIS2_PLACEMENT_3D ( 'NONE', #26451, #14317, #875 ) ;
#23090=VERTEX_POINT ( 'NONE', #127 ) ;
#23096=CIRCLE ( 'NONE', #31133, 8.749000000000002331 ) ;
#23097=FACE_OUTER_BOUND ( 'NONE', #17996, .T. ) ;
#23103=FACE_OUTER_BOUND ( 'NONE', #18488, .T. ) ;
#23107=DIRECTION ( 'NONE',  ( 0.000000000000000000, 0.000000000000000000, 1.000000000000000000 ) ) ;
#23109=CIRCLE ( 'NONE', #8682, 9.000000000000001776 ) ;
#23112=EDGE_CURVE ( 'NONE', #24130, #11257, #23029, .T. ) ;
#23115=VECTOR ( 'NONE', #9144, 1000.000000000000000 ) ;
#23117=AXIS2_PLACEMENT_3D ( 'NONE', #31011, #17974, #15794 ) ;
#23124=CARTESIAN_POINT ( 'NONE',  ( 1.624999999999999778, -1.464956435139467272, -10.90201369670500497 ) ) ;
#23128=CYLINDRICAL_SURFACE ( 'NONE', #7, 4.000000000000001776 ) ;
#23129=CARTESIAN_POINT ( 'NONE',  ( 0.000000000000000000, -9.680994141368730155, -5.222868219166962866 ) ) ;
#23138=AXIS2_PLACEMENT_3D ( 'NONE', #6318, #495, #20890 ) ;
#23148=CARTESIAN_POINT ( 'NONE',  ( 3.249999999999999556, -8.734705317681623171, -0.4999240074895356933 ) ) ;
#23152=DIRECTION ( 'NONE',  ( -1.000000000000000000, 0.000000000000000000, 0.000000000000000000 ) ) ;
#23156=CARTESIAN_POINT ( 'NONE',  ( 0.4883783024448289933, -9.508715662567844618, 2.300561732649534896 ) ) ;
#23159=DIRECTION ( 'NONE',  ( -1.000000000000000000, 0.000000000000000000, 0.000000000000000000 ) ) ;
#23166=CARTESIAN_POINT ( 'NONE',  ( 0.7632845268398871230, -8.734705317681623171, -0.4999240074895356933 ) ) ;
#23170=ORIENTED_EDGE ( 'NONE', *, *, #21629, .T. ) ;
#23171=AXIS2_PLACEMENT_3D ( 'NONE', #2236, #22640, #11748 ) ;
#23178=SHAPE_REPRESENTATION_RELATIONSHIP ( 'NONE' , 'NONE' ,  #8974, #24295 ) ;
#23188=AXIS2_PLACEMENT_3D ( 'NONE', #29967, #7235, #32830 ) ;
#23194=CYLINDRICAL_SURFACE ( 'NONE', #29351, 4.000000000000001776 ) ;
#23206=CARTESIAN_POINT ( 'NONE',  ( 0.1606233661161347581, -7.854816391753067784, -7.161985370900642245 ) ) ;
#23225=CARTESIAN_POINT ( 'NONE',  ( 0.5640492482744806635, 8.091724846332327914, -5.053269777826572273 ) ) ;
#23229=CARTESIAN_POINT ( 'NONE',  ( 2.795120610031290198, 0.7443816538168119834, 9.728666380680513370 ) ) ;
#23232=FACE_OUTER_BOUND ( 'NONE', #14036, .T. ) ;
#23234=VECTOR ( 'NONE', #11429, 1000.000000000000000 ) ;
#23239=EDGE_LOOP ( 'NONE', ( #25126, #29055, #29173, #6520, #25865 ) ) ;
#23243=LINE ( 'NONE', #26072, #14017 ) ;
#23247=ORIENTED_EDGE ( 'NONE', *, *, #31104, .F. ) ;
#23250=ADVANCED_FACE ( 'NONE', ( #5642 ), #31375, .T. ) ;
#23267=CARTESIAN_POINT ( 'NONE',  ( 0.1574692315735298220, -5.243558859478220313, 9.238013023060297257 ) ) ;
#23268=EDGE_LOOP ( 'NONE', ( #14168, #22546, #2004, #16511, #1448 ) ) ;
#23272=CARTESIAN_POINT ( 'NONE',  ( 3.063284526839887167, 0.4999240074894433228, 8.734705317681628500 ) ) ;
#23284=ORIENTED_EDGE ( 'NONE', *, *, #20606, .T. ) ;
#23289=CARTESIAN_POINT ( 'NONE',  ( 0.000000000000000000, 4.709950686174755319, -9.884132761439010650 ) ) ;
#23296=CARTESIAN_POINT ( 'NONE',  ( 0.000000000000000000, 10.85582367538894211, 1.425064293572374963 ) ) ;
#23300=DIRECTION ( 'NONE',  ( 0.000000000000000000, 0.000000000000000000, 1.000000000000000000 ) ) ;
#23302=EDGE_CURVE ( 'NONE', #24612, #19151, #7012, .T. ) ;
#23315=EDGE_CURVE ( 'NONE', #5917, #19301, #32135, .T. ) ;
#23321=CARTESIAN_POINT ( 'NONE',  ( 3.063284526839891608, 8.734705317681621395, 0.4999240074894719665 ) ) ;
#23334=CARTESIAN_POINT ( 'NONE',  ( 0.1079232672943445104, 10.52718011138291132, 2.097182127099708637 ) ) ;
#23350=CARTESIAN_POINT ( 'NONE',  ( 0.5032041927225605615, -7.418882907483827616, -6.298925283836324773 ) ) ;
#23352=ORIENTED_EDGE ( 'NONE', *, *, #10314, .F. ) ;
#23357=DIRECTION ( 'NONE',  ( 0.000000000000000000, 0.000000000000000000, -1.000000000000000000 ) ) ;
#23364=CARTESIAN_POINT ( 'NONE',  ( 0.5640492184783237883, 8.844377740304926405, 3.576105523026929855 ) ) ;
#23371=PLANE ( 'NONE',  #21983 ) ;
#23372=ORIENTED_EDGE ( 'NONE', *, *, #19461, .T. ) ;
#23385=ORIENTED_EDGE ( 'NONE', *, *, #21104, .T. ) ;
#23387=CARTESIAN_POINT ( 'NONE',  ( 0.3045634402744734071, -9.425384029459451085, 4.096074720329322183 ) ) ;
#23392=ADVANCED_FACE ( 'NONE', ( #17801 ), #2264, .T. ) ;
#23414=CARTESIAN_POINT ( 'NONE',  ( 0.5704039292223133106, -7.316743080999480675, 6.124150562935273712 ) ) ;
#23429=EDGE_CURVE ( 'NONE', #22521, #29650, #6085, .T. ) ;
#23435=DIRECTION ( 'NONE',  ( 1.000000000000000000, -0.000000000000000000, -0.000000000000000000 ) ) ;
#23449=ORIENTED_EDGE ( 'NONE', *, *, #4277, .T. ) ;
#23460=DIRECTION ( 'NONE',  ( 0.000000000000000000, 0.000000000000000000, 1.000000000000000000 ) ) ;
#23470=ORIENTED_EDGE ( 'NONE', *, *, #25928, .F. ) ;
#23474=ORIENTED_EDGE ( 'NONE', *, *, #2840, .T. ) ;
#23475=DIRECTION ( 'NONE',  ( 0.000000000000000000, 0.000000000000000000, 1.000000000000000000 ) ) ;
#23495=CARTESIAN_POINT ( 'NONE',  ( 0.1606232872998201999, 10.41111328664652014, -2.144970499002631037 ) ) ;
#23504=CARTESIAN_POINT ( 'NONE',  ( 0.6728002192015012373, -7.058361986489737561, -5.823680980849895050 ) ) ;
#23513=FACE_OUTER_BOUND ( 'NONE', #14676, .T. ) ;
#23527=AXIS2_PLACEMENT_3D ( 'NONE', #19099, #26781, #1715 ) ;
#23530=CARTESIAN_POINT ( 'NONE',  ( 3.063284526839890276, 7.360373001730978082, -4.729683950898788680 ) ) ;
#23533=AXIS2_PLACEMENT_3D ( 'NONE', #13390, #23609, #21270 ) ;
#23537=DIRECTION ( 'NONE',  ( -1.000000000000000000, -0.000000000000000000, -0.000000000000000000 ) ) ;
#23543=CARTESIAN_POINT ( 'NONE',  ( 1.624999999999999778, 7.958834565716766285, 7.593217523260609170 ) ) ;
#23544=EDGE_CURVE ( 'NONE', #12294, #20676, #5609, .T. ) ;
#23548=CARTESIAN_POINT ( 'NONE',  ( 2.274274201625327230, 1.975651141462238858, 10.82112760146736896 ) ) ;
#23549=CARTESIAN_POINT ( 'NONE',  ( 2.786096336624678926, -9.516507749480087597, 2.300561732651082103 ) ) ;
#23564=VERTEX_POINT ( 'NONE', #29653 ) ;
#23571=DIRECTION ( 'NONE',  ( -1.000000000000000000, 0.000000000000000000, 0.000000000000000000 ) ) ;
#23573=ORIENTED_EDGE ( 'NONE', *, *, #25211, .T. ) ;
#23580=CYLINDRICAL_SURFACE ( 'NONE', #26701, 11.00000000000000000 ) ;
#23583=ORIENTED_EDGE ( 'NONE', *, *, #29109, .T. ) ;
#23585=EDGE_CURVE ( 'NONE', #26130, #5903, #14388, .T. ) ;
#23587=TOROIDAL_SURFACE ( 'NONE', #40, 6.923700951379999857, 9.000000000000001776 ) ;
#23593=CIRCLE ( 'NONE', #15607, 4.000000000000001776 ) ;
#23598=ORIENTED_EDGE ( 'NONE', *, *, #23585, .T. ) ;
#23607=ORIENTED_EDGE ( 'NONE', *, *, #27535, .T. ) ;
#23609=DIRECTION ( 'NONE',  ( -1.000000000000000000, 0.000000000000000000, 0.000000000000000000 ) ) ;
#23613=ORIENTED_EDGE ( 'NONE', *, *, #32400, .F. ) ;
#23619=VERTEX_POINT ( 'NONE', #1403 ) ;
#23624=CARTESIAN_POINT ( 'NONE',  ( 0.000000000000000000, -9.680994141368802985, 5.222868219166823422 ) ) ;
#23628=CARTESIAN_POINT ( 'NONE',  ( 3.063284526839887167, 3.174628368996073924, 8.152713396088772768 ) ) ;
#23631=DIRECTION ( 'NONE',  ( 0.000000000000000000, 0.000000000000000000, 1.000000000000000000 ) ) ;
#23648=EDGE_CURVE ( 'NONE', #2670, #7219, #17149, .T. ) ;
#23654=VECTOR ( 'NONE', #4997, 1000.000000000000000 ) ;
#23662=EDGE_LOOP ( 'NONE', ( #9909, #2036, #2163, #11715, #27251 ) ) ;
#23666=VERTEX_POINT ( 'NONE', #6733 ) ;
#23671=ADVANCED_FACE ( 'NONE', ( #14088 ), #1702, .T. ) ;
#23686=PLANE ( 'NONE',  #19892 ) ;
#23697=VERTEX_POINT ( 'NONE', #13898 ) ;
#23701=ORIENTED_EDGE ( 'NONE', *, *, #19281, .T. ) ;
#23710=EDGE_CURVE ( 'NONE', #16905, #25765, #24110, .T. ) ;
#23724=CARTESIAN_POINT ( 'NONE',  ( 0.1606233060821305736, -4.384181225617423294, 9.683549581721083044 ) ) ;
#23729=DIRECTION ( 'NONE',  ( -1.000000000000000000, -0.000000000000000000, 0.000000000000000000 ) ) ;
#23731=FACE_OUTER_BOUND ( 'NONE', #32354, .T. ) ;
#23746=ORIENTED_EDGE ( 'NONE', *, *, #23544, .T. ) ;
#23753=ORIENTED_EDGE ( 'NONE', *, *, #12692, .T. ) ;
#23767=CARTESIAN_POINT ( 'NONE',  ( 2.795120465739999727, -2.298374178342462049, 9.482538569678554907 ) ) ;
#23770=ORIENTED_EDGE ( 'NONE', *, *, #10314, .T. ) ;
#23772=DIRECTION ( 'NONE',  ( 0.000000000000000000, 0.000000000000000000, 1.000000000000000000 ) ) ;
#23773=CARTESIAN_POINT ( 'NONE',  ( 2.274274201620948510, 9.915734732518576067, -4.762163868927066446 ) ) ;
#23792=DIRECTION ( 'NONE',  ( 1.000000000000000000, 0.000000000000000000, 0.000000000000000000 ) ) ;
#23804=CARTESIAN_POINT ( 'NONE',  ( 2.976845687893344916, 9.149921655307451829, 0.5490754078162828344 ) ) ;
#23810=ORIENTED_EDGE ( 'NONE', *, *, #31935, .T. ) ;
#23814=EDGE_CURVE ( 'NONE', #27203, #10039, #31606, .T. ) ;
#23826=CARTESIAN_POINT ( 'NONE',  ( 0.000000000000000000, 0.000000000000000000, 0.000000000000000000 ) ) ;
#23839=B_SPLINE_CURVE_WITH_KNOTS ( 'NONE', 3,
 ( #14300, #19350, #16332, #1128, #5975, #26542, #19169, #1315 ),
 .UNSPECIFIED., .F., .F.,
 ( 4, 2, 2, 4 ),
 ( 2.024520226902067482E-07, 0.001261135997420257965, 0.001891602770119041712, 0.002522069542817825458 ),
 .UNSPECIFIED. ) ;
#23848=CARTESIAN_POINT ( 'NONE',  ( 0.000000000000000000, 1.699438267350499521, -9.241976615262139205 ) ) ;
#23857=EDGE_CURVE ( 'NONE', #29226, #31221, #18232, .T. ) ;
#23871=ORIENTED_EDGE ( 'NONE', *, *, #14425, .F. ) ;
#23874=PLANE ( 'NONE',  #8089 ) ;
#23890=EDGE_CURVE ( 'NONE', #14922, #31656, #28123, .T. ) ;
#23892=ORIENTED_EDGE ( 'NONE', *, *, #25048, .F. ) ;
#23900=CARTESIAN_POINT ( 'NONE',  ( 0.000000000000000000, 0.000000000000000000, 0.000000000000000000 ) ) ;
#23908=ORIENTED_EDGE ( 'NONE', *, *, #28299, .F. ) ;
#23915=CARTESIAN_POINT ( 'NONE',  ( 0.7632845268398871230, -5.538577986808947529, 6.772677083992368452 ) ) ;
#23919=ORIENTED_EDGE ( 'NONE', *, *, #18586, .F. ) ;
#23932=CYLINDRICAL_SURFACE ( 'NONE', #31619, 11.00000000000000000 ) ;
#23933=EDGE_CURVE ( 'NONE', #14830, #4619, #18802, .T. ) ;
#23937=ORIENTED_EDGE ( 'NONE', *, *, #20205, .T. ) ;
#23950=DIRECTION ( 'NONE',  ( -1.000000000000000000, -0.000000000000000000, -0.000000000000000000 ) ) ;
#23960=ORIENTED_EDGE ( 'NONE', *, *, #32831, .F. ) ;
#23967=LINE ( 'NONE', #31852, #22493 ) ;
#23968=ORIENTED_EDGE ( 'NONE', *, *, #10018, .T. ) ;
#23971=DIRECTION ( 'NONE',  ( -1.000000000000000000, 0.000000000000000000, 0.000000000000000000 ) ) ;
#23991=AXIS2_PLACEMENT_3D ( 'NONE', #22967, #22670, #5108 ) ;
#24017=DIRECTION ( 'NONE',  ( 0.000000000000000000, 0.000000000000000000, 1.000000000000000000 ) ) ;
#24034=CARTESIAN_POINT ( 'NONE',  ( 3.249999999999999556, 4.472189673936786569, 8.264486777890123648 ) ) ;
#24035=CIRCLE ( 'NONE', #30490, 11.00000000000000000 ) ;
#24042=AXIS2_PLACEMENT_3D ( 'NONE', #16748, #29632, #32321 ) ;
#24045=CARTESIAN_POINT ( 'NONE',  ( 0.08034252266852373592, -10.71005054582363414, 1.301095883299237643 ) ) ;
#24046=ADVANCED_FACE ( 'NONE', ( #6970 ), #1640, .F. ) ;
#24049=FACE_OUTER_BOUND ( 'NONE', #4086, .T. ) ;
#24053=CARTESIAN_POINT ( 'NONE',  ( 3.249999999999999556, -6.478011392632939902, 6.807171995660557862 ) ) ;
#24062=CARTESIAN_POINT ( 'NONE',  ( 2.589202905186827053, -4.126870756446547439, 9.453729690310151312 ) ) ;
#24069=CARTESIAN_POINT ( 'NONE',  ( 0.000000000000000000, 10.90201369670498366, 1.464956435139577851 ) ) ;
#24072=CARTESIAN_POINT ( 'NONE',  ( 0.3045633657615061107, -6.808202580038380525, -7.698316278340186614 ) ) ;
#24073=CARTESIAN_POINT ( 'NONE',  ( -5.749676575031998027, 0.000000000000000000, -6.923700951379999857 ) ) ;
#24097=CARTESIAN_POINT ( 'NONE',  ( 0.000000000000000000, 0.000000000000000000, 0.000000000000000000 ) ) ;
#24100=ORIENTED_EDGE ( 'NONE', *, *, #18186, .F. ) ;
#24103=CARTESIAN_POINT ( 'NONE',  ( 2.274274201627370040, 7.958834565715812381, -7.593217523255793466 ) ) ;
#24110=LINE ( 'NONE', #29296, #18781 ) ;
#24115=CARTESIAN_POINT ( 'NONE',  ( 0.000000000000000000, 0.000000000000000000, 0.000000000000000000 ) ) ;
#24123=ORIENTED_EDGE ( 'NONE', *, *, #23710, .F. ) ;
#24124=VECTOR ( 'NONE', #16255, 1000.000000000000000 ) ;
#24130=VERTEX_POINT ( 'NONE', #30749 ) ;
#24134=EDGE_LOOP ( 'NONE', ( #13613, #27304, #15491, #4992 ) ) ;
#24143=CIRCLE ( 'NONE', #9732, 4.000000000000002665 ) ;
#24149=ORIENTED_EDGE ( 'NONE', *, *, #23585, .F. ) ;
#24173=VECTOR ( 'NONE', #4541, 1000.000000000000000 ) ;
#24194=ORIENTED_EDGE ( 'NONE', *, *, #18188, .T. ) ;
#24198=CARTESIAN_POINT ( 'NONE',  ( 2.274274201625318348, -5.222868219166783454, -9.680994141368850947 ) ) ;
#24199=CIRCLE ( 'NONE', #9788, 8.749000000000002331 ) ;
#24204=DIRECTION ( 'NONE',  ( 0.000000000000000000, 0.000000000000000000, 1.000000000000000000 ) ) ;
#24205=CARTESIAN_POINT ( 'NONE',  ( 2.589202987961075397, -2.218054364314524740, -10.07394153291407335 ) ) ;
#24213=CARTESIAN_POINT ( 'NONE',  ( 3.249999999999999556, 2.223716399045691183, -8.461683424509292450 ) ) ;
#24217=DIRECTION ( 'NONE',  ( 0.000000000000000000, -2.309263891220325604E-14, 1.000000000000000000 ) ) ;
#24236=CARTESIAN_POINT ( 'NONE',  ( 0.000000000000000000, 0.000000000000000000, 0.000000000000000000 ) ) ;
#24241=ORIENTED_EDGE ( 'NONE', *, *, #2198, .T. ) ;
#24247=ORIENTED_EDGE ( 'NONE', *, *, #21104, .F. ) ;
#24252=EDGE_CURVE ( 'NONE', #28862, #2488, #26037, .T. ) ;
#24261=ORIENTED_EDGE ( 'NONE', *, *, #14851, .T. ) ;
#24268=EDGE_CURVE ( 'NONE', #16746, #12234, #11862, .T. ) ;
#24271=VERTEX_POINT ( 'NONE', #16315 ) ;
#24274=ORIENTED_EDGE ( 'NONE', *, *, #14851, .F. ) ;
#24275=ORIENTED_EDGE ( 'NONE', *, *, #30707, .T. ) ;
#24282=DIRECTION ( 'NONE',  ( 0.000000000000000000, 0.000000000000000000, -1.000000000000000000 ) ) ;
#24288=CARTESIAN_POINT ( 'NONE',  ( 3.063284526839889832, 3.174628368996186278, -8.152713396088721254 ) ) ;
#24293=ORIENTED_EDGE ( 'NONE', *, *, #27142, .T. ) ;
#24295=ADVANCED_BREP_SHAPE_REPRESENTATION ( '', ( #10563, #2865 ), #7630 ) ;
#24306=EDGE_LOOP ( 'NONE', ( #21876, #20946, #2245, #32511, #4013 ) ) ;
#24307=ORIENTED_EDGE ( 'NONE', *, *, #24501, .F. ) ;
#24319=ORIENTED_EDGE ( 'NONE', *, *, #14425, .T. ) ;
#24335=VERTEX_POINT ( 'NONE', #26192 ) ;
#24336=ADVANCED_FACE ( 'NONE', ( #3301 ), #32025, .T. ) ;
#24343=ORIENTED_EDGE ( 'NONE', *, *, #7407, .T. ) ;
#24346=DIRECTION ( 'NONE',  ( -1.000000000000000000, 0.000000000000000000, 0.000000000000000000 ) ) ;
#24362=CARTESIAN_POINT ( 'NONE',  ( 0.5640491561247187313, 9.516580665849673437, 0.6680154998105086728 ) ) ;
#24365=DIRECTION ( 'NONE',  ( 0.000000000000000000, 0.000000000000000000, 1.000000000000000000 ) ) ;
#24375=CARTESIAN_POINT ( 'NONE',  ( 0.5640492482715756539, -5.053269777829524578, -8.091724846341634247 ) ) ;
#24382=EDGE_LOOP ( 'NONE', ( #6250, #30506 ) ) ;
#24412=ORIENTED_EDGE ( 'NONE', *, *, #32430, .F. ) ;
#24420=CARTESIAN_POINT ( 'NONE',  ( 2.592584512317752665, -10.27797909967270229, 0.9926283730659328786 ) ) ;
#24423=ORIENTED_EDGE ( 'NONE', *, *, #29639, .F. ) ;
#24433=ORIENTED_EDGE ( 'NONE', *, *, #22927, .F. ) ;
#24436=DIRECTION ( 'NONE',  ( 1.000000000000000000, -0.000000000000000000, -0.000000000000000000 ) ) ;
#24439=CARTESIAN_POINT ( 'NONE',  ( 0.7632845268398883443, -7.360373001730875053, -4.729683950898950329 ) ) ;
#24441=CARTESIAN_POINT ( 'NONE',  ( 0.5704035821693400621, 0.6538686328479551557, 9.519055809315281280 ) ) ;
#24449=ORIENTED_EDGE ( 'NONE', *, *, #31684, .F. ) ;
#24450=LINE ( 'NONE', #22142, #18766 ) ;
#24456=ORIENTED_EDGE ( 'NONE', *, *, #6491, .T. ) ;
#24458=ORIENTED_EDGE ( 'NONE', *, *, #11240, .F. ) ;
#24463=DIRECTION ( 'NONE',  ( 0.000000000000000000, 0.000000000000000000, 1.000000000000000000 ) ) ;
#24470=DIRECTION ( 'NONE',  ( 0.000000000000000000, 0.000000000000000000, 1.000000000000000000 ) ) ;
#24477=EDGE_CURVE ( 'NONE', #14922, #12461, #9734, .T. ) ;
#24481=DIRECTION ( 'NONE',  ( -1.000000000000000000, -0.000000000000000000, -0.000000000000000000 ) ) ;
#24482=CARTESIAN_POINT ( 'NONE',  ( 0.000000000000000000, 0.000000000000000000, -6.999999999999998224 ) ) ;
#24486=DIRECTION ( 'NONE',  ( 0.000000000000000000, 0.000000000000000000, 1.000000000000000000 ) ) ;
#24491=DIRECTION ( 'NONE',  ( -1.000000000000000000, -0.000000000000000000, -0.000000000000000000 ) ) ;
#24494=B_SPLINE_CURVE_WITH_KNOTS ( 'NONE', 3,
 ( #16810, #9592, #29335, #3959 ),
 .UNSPECIFIED., .F., .F.,
 ( 4, 4 ),
 ( 0.002128777998666837260, 0.002455751998630970826 ),
 .UNSPECIFIED. ) ;
#24501=EDGE_CURVE ( 'NONE', #10426, #8063, #29504, .T. ) ;
#24505=ORIENTED_EDGE ( 'NONE', *, *, #28741, .T. ) ;
#24506=FACE_OUTER_BOUND ( 'NONE', #7978, .T. ) ;
#24516=ORIENTED_EDGE ( 'NONE', *, *, #1543, .F. ) ;
#24535=DIRECTION ( 'NONE',  ( 0.000000000000000000, 0.000000000000000000, -1.000000000000000000 ) ) ;
#24541=CARTESIAN_POINT ( 'NONE',  ( 2.274274201621893976, 10.90201369671108722, -1.464956435144929570 ) ) ;
#24565=CIRCLE ( 'NONE', #23527, 8.749000000000002331 ) ;
#24596=CARTESIAN_POINT ( 'NONE',  ( 2.970200582152835445, -7.065646041987108994, 5.831559621424839079 ) ) ;
#24603=CARTESIAN_POINT ( 'NONE',  ( 0.1574692247319860738, 1.187839595765007639, 10.55579611470142964 ) ) ;
#24612=VERTEX_POINT ( 'NONE', #23166 ) ;
#24626=VERTEX_POINT ( 'NONE', #762 ) ;
#24628=CARTESIAN_POINT ( 'NONE',  ( 0.1574692253523927998, -2.132217800985108269, 10.40622129948746810 ) ) ;
#24633=CARTESIAN_POINT ( 'NONE',  ( 2.970200414845727277, 2.288523046052883814, -8.870914041987591148 ) ) ;
#24643=DIRECTION ( 'NONE',  ( -1.000000000000000000, 0.000000000000000000, 0.000000000000000000 ) ) ;
#24649=DIRECTION ( 'NONE',  ( -1.000000000000000000, -0.000000000000000000, -0.000000000000000000 ) ) ;
#24653=ORIENTED_EDGE ( 'NONE', *, *, #23710, .T. ) ;
#24660=AXIS2_PLACEMENT_3D ( 'NONE', #134, #20354, #3479 ) ;
#24672=EDGE_CURVE ( 'NONE', #25199, #31261, #11338, .T. ) ;
#24673=LINE ( 'NONE', #14651, #9694 ) ;
#24682=EDGE_CURVE ( 'NONE', #17637, #22462, #1205, .T. ) ;
#24690=AXIS2_PLACEMENT_3D ( 'NONE', #28774, #31313, #32308 ) ;
#24699=FACE_OUTER_BOUND ( 'NONE', #10986, .T. ) ;
#24710=CARTESIAN_POINT ( 'NONE',  ( 2.864531114197726769, 8.105385692883681159, -5.073635298885059264 ) ) ;
#24718=AXIS2_PLACEMENT_3D ( 'NONE', #12165, #6818, #7171 ) ;
#24723=AXIS2_PLACEMENT_3D ( 'NONE', #19428, #29621, #1879 ) ;
#24730=CARTESIAN_POINT ( 'NONE',  ( 0.6791197464446973031, -0.5477823182330034957, -9.138998021039025588 ) ) ;
#24738=CARTESIAN_POINT ( 'NONE',  ( 2.661997753583457360, -10.09011512947411937, -0.9074203448823074947 ) ) ;
#24743=EDGE_CURVE ( 'NONE', #26011, #6812, #5487, .T. ) ;
#24748=AXIS2_PLACEMENT_3D ( 'NONE', #21116, #16056, #3707 ) ;
#24752=DIRECTION ( 'NONE',  ( 0.000000000000000000, -0.3090169943749350168, -0.9510565162951576390 ) ) ;
#24763=EDGE_CURVE ( 'NONE', #25765, #22691, #28986, .T. ) ;
#24766=LINE ( 'NONE', #30585, #32570 ) ;
#24772=CYLINDRICAL_SURFACE ( 'NONE', #694, 6.000000000000000888 ) ;
#24778=DIRECTION ( 'NONE',  ( 0.000000000000000000, 0.000000000000000000, 1.000000000000000000 ) ) ;
#24788=CARTESIAN_POINT ( 'NONE',  ( 2.592584925146038888, -7.731606906650699607, 6.844296717724891010 ) ) ;
#24791=DIRECTION ( 'NONE',  ( 0.000000000000000000, 0.000000000000000000, 1.000000000000000000 ) ) ;
#24798=EDGE_CURVE ( 'NONE', #12771, #19976, #32191, .T. ) ;
#24801=EDGE_CURVE ( 'NONE', #30416, #7918, #11365, .T. ) ;
#24805=VERTEX_POINT ( 'NONE', #16929 ) ;
#24809=DIRECTION ( 'NONE',  ( -1.000000000000000000, 0.000000000000000000, 0.000000000000000000 ) ) ;
#24812=ORIENTED_EDGE ( 'NONE', *, *, #19281, .F. ) ;
#24828=CARTESIAN_POINT ( 'NONE',  ( 2.274274201625316572, -7.958834565716716547, -7.593217523260693547 ) ) ;
#24835=EDGE_CURVE ( 'NONE', #32538, #16234, #18403, .T. ) ;
#24841=CARTESIAN_POINT ( 'NONE',  ( 0.000000000000000000, 0.000000000000000000, 0.000000000000000000 ) ) ;
#24844=CARTESIAN_POINT ( 'NONE',  ( 2.680481146936424253, 8.652652323859461703, 5.199347632287054211 ) ) ;
#24885=ORIENTED_EDGE ( 'NONE', *, *, #27341, .T. ) ;
#24891=DIRECTION ( 'NONE',  ( 1.000000000000000000, -0.000000000000000000, -0.000000000000000000 ) ) ;
#24903=ORIENTED_EDGE ( 'NONE', *, *, #7824, .F. ) ;
#24906=CYLINDRICAL_SURFACE ( 'NONE', #19285, 6.000000000000000888 ) ;
#24911=CARTESIAN_POINT ( 'NONE',  ( 2.970200448039785002, -3.362738345035427567, -8.521880193013316784 ) ) ;
#24913=DIRECTION ( 'NONE',  ( 0.000000000000000000, 0.000000000000000000, -1.000000000000000000 ) ) ;
#24921=FACE_OUTER_BOUND ( 'NONE', #18550, .T. ) ;
#24942=CARTESIAN_POINT ( 'NONE',  ( 2.864531019710236048, -8.868883597856992651, -3.575186956654084369 ) ) ;
#24953=ORIENTED_EDGE ( 'NONE', *, *, #2198, .F. ) ;
#24954=B_SPLINE_CURVE_WITH_KNOTS ( 'NONE', 3,
 ( #19819, #7119, #32380, #22488, #20006, #17463, #9284, #19501 ),
 .UNSPECIFIED., .F., .F.,
 ( 4, 2, 2, 4 ),
 ( 5.099451029784244903E-07, 0.001229189612673438564, 0.001843529446458668647, 0.002457869280243898946 ),
 .UNSPECIFIED. ) ;
#24959=ORIENTED_EDGE ( 'NONE', *, *, #28831, .F. ) ;
#24963=FACE_OUTER_BOUND ( 'NONE', #10778, .T. ) ;
#24991=ORIENTED_EDGE ( 'NONE', *, *, #23043, .T. ) ;
#24997=FACE_OUTER_BOUND ( 'NONE', #19226, .T. ) ;
#25018=DIRECTION ( 'NONE',  ( 0.000000000000000000, 0.000000000000000000, 1.000000000000000000 ) ) ;
#25039=VERTEX_POINT ( 'NONE', #28470 ) ;
#25048=EDGE_CURVE ( 'NONE', #22885, #24805, #7748, .T. ) ;
#25051=ORIENTED_EDGE ( 'NONE', *, *, #3348, .T. ) ;
#25063=DIRECTION ( 'NONE',  ( -1.000000000000000000, -0.000000000000000000, 0.000000000000000000 ) ) ;
#25080=DIRECTION ( 'NONE',  ( -1.000000000000000000, -0.000000000000000000, -0.000000000000000000 ) ) ;
#25088=CARTESIAN_POINT ( 'NONE',  ( 0.5032040568826982030, 5.109302080990191897, 8.283195248915165010 ) ) ;
#25096=CARTESIAN_POINT ( 'NONE',  ( 3.063284526839887167, -8.152713396088739017, -3.174628368996162298 ) ) ;
#25097=AXIS2_PLACEMENT_3D ( 'NONE', #14029, #13847, #31784 ) ;
#25112=AXIS2_PLACEMENT_3D ( 'NONE', #28928, #3056, #31787 ) ;
#25119=ORIENTED_EDGE ( 'NONE', *, *, #18951, .T. ) ;
#25126=ORIENTED_EDGE ( 'NONE', *, *, #13264, .F. ) ;
#25133=AXIS2_PLACEMENT_3D ( 'NONE', #27602, #1888, #32962 ) ;
#25137=PLANE ( 'NONE',  #25643 ) ;
#25150=CARTESIAN_POINT ( 'NONE',  ( 0.6903270996310453267, 7.668283427123773421, 4.902115053686892487 ) ) ;
#25174=VERTEX_POINT ( 'NONE', #23915 ) ;
#25177=CIRCLE ( 'NONE', #10764, 10.94895958125474245 ) ;
#25179=FACE_OUTER_BOUND ( 'NONE', #25944, .T. ) ;
#25180=CIRCLE ( 'NONE', #14469, 10.94895958125474245 ) ;
#25195=ORIENTED_EDGE ( 'NONE', *, *, #22518, .F. ) ;
#25199=VERTEX_POINT ( 'NONE', #29619 ) ;
#25200=AXIS2_PLACEMENT_3D ( 'NONE', #15792, #15625, #6092 ) ;
#25208=CARTESIAN_POINT ( 'NONE',  ( 3.249999999999999556, 8.152713396088806519, -3.174628368995990879 ) ) ;
#25211=EDGE_CURVE ( 'NONE', #22521, #14763, #31692, .T. ) ;
#25212=CARTESIAN_POINT ( 'NONE',  ( 0.7082655507077595392, -8.722704248566902407, 2.275631959094134515 ) ) ;
#25213=EDGE_CURVE ( 'NONE', #7687, #7219, #30303, .T. ) ;
#25217=ADVANCED_FACE ( 'NONE', ( #4040 ), #13863, .T. ) ;
#25220=CARTESIAN_POINT ( 'NONE',  ( 1.624999999999999778, 1.464956435139694646, -10.90201369670497122 ) ) ;
#25236=CYLINDRICAL_SURFACE ( 'NONE', #6976, 4.000000000000001776 ) ;
#25241=ORIENTED_EDGE ( 'NONE', *, *, #8931, .T. ) ;
#25255=AXIS2_PLACEMENT_3D ( 'NONE', #28589, #667, #3661 ) ;
#25256=DIRECTION ( 'NONE',  ( 1.000000000000000000, -0.000000000000000000, -0.000000000000000000 ) ) ;
#25308=AXIS2_PLACEMENT_3D ( 'NONE', #27481, #5233, #14758 ) ;
#25316=DIRECTION ( 'NONE',  ( 0.000000000000000000, 1.224646799147353207E-16, 1.000000000000000000 ) ) ;
#25327=CARTESIAN_POINT ( 'NONE',  ( 3.249999999999999556, -9.241976615262146311, -1.699438267350472209 ) ) ;
#25331=CARTESIAN_POINT ( 'NONE',  ( 0.04285674552576868024, -9.518400180040705649, 5.235784774550934273 ) ) ;
#25335=DIRECTION ( 'NONE',  ( 0.000000000000000000, 1.224646799147353207E-16, 1.000000000000000000 ) ) ;
#25337=EDGE_CURVE ( 'NONE', #24271, #10493, #20481, .T. ) ;
#25347=LINE ( 'NONE', #28330, #17044 ) ;
#25348=CARTESIAN_POINT ( 'NONE',  ( 2.357330058169020415, 7.915524238820739633, 7.401770933800242425 ) ) ;
#25349=EDGE_CURVE ( 'NONE', #30676, #23697, #5191, .T. ) ;
#25352=LINE ( 'NONE', #2460, #28934 ) ;
#25356=VERTEX_POINT ( 'NONE', #6204 ) ;
#25358=EDGE_CURVE ( 'NONE', #5275, #31435, #9696, .T. ) ;
#25359=ORIENTED_EDGE ( 'NONE', *, *, #17871, .T. ) ;
#25363=ORIENTED_EDGE ( 'NONE', *, *, #24801, .T. ) ;
#25367=CARTESIAN_POINT ( 'NONE',  ( 3.063284526839887167, 0.000000000000000000, 0.000000000000000000 ) ) ;
#25377=ORIENTED_EDGE ( 'NONE', *, *, #17033, .F. ) ;
#25390=LINE ( 'NONE', #11556, #26779 ) ;
#25394=CARTESIAN_POINT ( 'NONE',  ( 0.7632845268398871230, 6.772677083992467928, -5.538577986808824960 ) ) ;
#25398=CARTESIAN_POINT ( 'NONE',  ( 0.1574692247322762029, -1.187839595764517142, -10.55579611470083634 ) ) ;
#25415=EDGE_CURVE ( 'NONE', #20676, #18033, #14586, .T. ) ;
#25423=CARTESIAN_POINT ( 'NONE',  ( 2.970200582150003932, 7.065646041994371629, -5.831559621433123120 ) ) ;
#25439=ORIENTED_EDGE ( 'NONE', *, *, #28198, .T. ) ;
#25454=CARTESIAN_POINT ( 'NONE',  ( 0.5664946525141408840, -9.241976615262153416, 2.300561732649529567 ) ) ;
#25466=CARTESIAN_POINT ( 'NONE',  ( 0.7632845268398876781, -3.174628368996014860, -8.152713396088786979 ) ) ;
#25475=ADVANCED_FACE ( 'NONE', ( #4849 ), #29772, .T. ) ;
#25481=CARTESIAN_POINT ( 'NONE',  ( 0.3997463082871472451, -9.773321362167809667, 2.273557229425371418 ) ) ;
#25493=CARTESIAN_POINT ( 'NONE',  ( 3.063284526839887167, 7.360373001730918574, 4.729683950898899703 ) ) ;
#25494=ORIENTED_EDGE ( 'NONE', *, *, #20031, .F. ) ;
#25503=CYLINDRICAL_SURFACE ( 'NONE', #12388, 8.749000000000002331 ) ;
#25516=EDGE_CURVE ( 'NONE', #6718, #22462, #12330, .T. ) ;
#25524=CARTESIAN_POINT ( 'NONE',  ( 0.000000000000000000, 1.425064293572489094, -10.85582367538892790 ) ) ;
#25534=EDGE_CURVE ( 'NONE', #25039, #15781, #15217, .T. ) ;
#25540=DIRECTION ( 'NONE',  ( 0.000000000000000000, 0.000000000000000000, 1.000000000000000000 ) ) ;
#25542=DIRECTION ( 'NONE',  ( 0.000000000000000000, 0.000000000000000000, 1.000000000000000000 ) ) ;
#25547=CARTESIAN_POINT ( 'NONE',  ( 0.000000000000000000, 9.620177616658057929, -5.227991826303984624 ) ) ;
#25549=B_SPLINE_CURVE_WITH_KNOTS ( 'NONE', 3,
 ( #16858, #16691, #29087, #4008, #24375, #21711, #26902, #19197 ),
 .UNSPECIFIED., .F., .F.,
 ( 4, 2, 2, 4 ),
 ( 5.099451029798772576E-07, 0.001229189835650483162, 0.001843529780924232616, 0.002457869726197984238 ),
 .UNSPECIFIED. ) ;
#25550=EDGE_LOOP ( 'NONE', ( #6782, #15515, #12529, #14412, #13855 ) ) ;
#25552=CARTESIAN_POINT ( 'NONE',  ( 0.08034252266852319468, -1.301095883299200562, -10.71005054582364302 ) ) ;
#25554=DIRECTION ( 'NONE',  ( 0.000000000000000000, 0.000000000000000000, 1.000000000000000000 ) ) ;
#25561=CARTESIAN_POINT ( 'NONE',  ( 3.249999999999999556, -5.538577986808848941, -6.772677083992448388 ) ) ;
#25565=VERTEX_POINT ( 'NONE', #30622 ) ;
#25567=DIRECTION ( 'NONE',  ( 1.000000000000000000, -0.000000000000000000, -0.000000000000000000 ) ) ;
#25571=CARTESIAN_POINT ( 'NONE',  ( 2.661997913519438264, 2.255009087902927867, 9.876677602395371736 ) ) ;
#25574=CARTESIAN_POINT ( 'NONE',  ( 1.624999999999999778, -9.680994141368733708, -5.222868219166961978 ) ) ;
#25580=EDGE_CURVE ( 'NONE', #30676, #3168, #26849, .T. ) ;
#25586=EDGE_LOOP ( 'NONE', ( #28819, #4082, #18700, #1485 ) ) ;
#25603=CARTESIAN_POINT ( 'NONE',  ( 2.274274201625327230, 7.593217523260696211, -7.958834565716686349 ) ) ;
#25607=AXIS2_PLACEMENT_3D ( 'NONE', #18315, #28671, #31209 ) ;
#25612=CIRCLE ( 'NONE', #21335, 6.000000000000000888 ) ;
#25623=EDGE_CURVE ( 'NONE', #15369, #12234, #29870, .T. ) ;
#25629=ORIENTED_EDGE ( 'NONE', *, *, #613, .T. ) ;
#25630=ORIENTED_EDGE ( 'NONE', *, *, #30040, .F. ) ;
#25639=CARTESIAN_POINT ( 'NONE',  ( 1.624999999999999778, -1.975651141462315907, 10.82112760146735475 ) ) ;
#25643=AXIS2_PLACEMENT_3D ( 'NONE', #12446, #7594, #22960 ) ;
#25650=DIRECTION ( 'NONE',  ( 0.000000000000000000, 0.000000000000000000, 1.000000000000000000 ) ) ;
#25662=( NAMED_UNIT ( * ) PLANE_ANGLE_UNIT ( ) SI_UNIT ( $, .RADIAN. ) );
#25668=ORIENTED_EDGE ( 'NONE', *, *, #20402, .F. ) ;
#25697=EDGE_CURVE ( 'NONE', #29923, #4178, #16208, .T. ) ;
#25701=VECTOR ( 'NONE', #3561, 1000.000000000000000 ) ;
#25706=EDGE_LOOP ( 'NONE', ( #31810, #2380, #14244, #32051 ) ) ;
#25717=ADVANCED_FACE ( 'NONE', ( #23731 ), #31918, .T. ) ;
#25721=FACE_BOUND ( 'NONE', #24382, .T. ) ;
#25724=FACE_OUTER_BOUND ( 'NONE', #3457, .T. ) ;
#25733=CARTESIAN_POINT ( 'NONE',  ( 4.888486331236938389E-17, -10.76487093102066517, 1.999317321091457655 ) ) ;
#25735=VERTEX_POINT ( 'NONE', #16008 ) ;
#25739=AXIS2_PLACEMENT_3D ( 'NONE', #4349, #30270, #14197 ) ;
#25740=CARTESIAN_POINT ( 'NONE',  ( 2.440333710190775829, -10.46055952248794796, -2.130583817698489479 ) ) ;
#25751=CARTESIAN_POINT ( 'NONE',  ( 0.7632845268398871230, 0.000000000000000000, 0.000000000000000000 ) ) ;
#25765=VERTEX_POINT ( 'NONE', #12319 ) ;
#25802=AXIS2_PLACEMENT_3D ( 'NONE', #26474, #3573, #28972 ) ;
#25803=FACE_OUTER_BOUND ( 'NONE', #8623, .T. ) ;
#25806=LINE ( 'NONE', #15092, #7576 ) ;
#25809=AXIS2_PLACEMENT_3D ( 'NONE', #18152, #18004, #28191 ) ;
#25820=CIRCLE ( 'NONE', #3932, 8.749000000000002331 ) ;
#25831=CARTESIAN_POINT ( 'NONE',  ( 2.440333653308765172, 4.424884217119425145, 9.715096239907426323 ) ) ;
#25854=ORIENTED_EDGE ( 'NONE', *, *, #31917, .T. ) ;
#25859=ORIENTED_EDGE ( 'NONE', *, *, #30420, .T. ) ;
#25865=ORIENTED_EDGE ( 'NONE', *, *, #27142, .F. ) ;
#25871=CARTESIAN_POINT ( 'NONE',  ( 0.000000000000000000, 0.000000000000000000, 0.000000000000000000 ) ) ;
#25873=DIRECTION ( 'NONE',  ( -1.000000000000000000, 0.000000000000000000, -0.000000000000000000 ) ) ;
#25880=CARTESIAN_POINT ( 'NONE',  ( 0.5640491561200821069, -0.6680154998155144463, 9.516580665864458055 ) ) ;
#25895=B_SPLINE_CURVE_WITH_KNOTS ( 'NONE', 3,
 ( #25466, #2576, #14913, #12592, #12428, #30685, #22946, #28138 ),
 .UNSPECIFIED., .F., .F.,
 ( 4, 2, 2, 4 ),
 ( 2.213836054352509658E-07, 0.001227982086136112207, 0.001841862437401450012, 0.002455742788666787600 ),
 .UNSPECIFIED. ) ;
#25897=CARTESIAN_POINT ( 'NONE',  ( 2.795120610037679754, -0.7443816538093332991, -9.728666380661904256 ) ) ;
#25909=DIRECTION ( 'NONE',  ( 0.000000000000000000, 0.000000000000000000, 1.000000000000000000 ) ) ;
#25919=VERTEX_POINT ( 'NONE', #31445 ) ;
#25922=CARTESIAN_POINT ( 'NONE',  ( 3.063284526839889388, 2.223716399045570391, 8.461683424509315543 ) ) ;
#25923=CARTESIAN_POINT ( 'NONE',  ( 2.274274201625319236, -9.680994141368833183, 5.222868219166820758 ) ) ;
#25928=EDGE_CURVE ( 'NONE', #22995, #4279, #29451, .T. ) ;
#25938=EDGE_LOOP ( 'NONE', ( #28030, #23770 ) ) ;
#25939=ORIENTED_EDGE ( 'NONE', *, *, #31935, .F. ) ;
#25940=LINE ( 'NONE', #26580, #7641 ) ;
#25944=EDGE_LOOP ( 'NONE', ( #15874, #17501, #8980, #33034 ) ) ;
#25945=FACE_OUTER_BOUND ( 'NONE', #26679, .T. ) ;
#25959=CARTESIAN_POINT ( 'NONE',  ( 0.000000000000000000, -10.76487093102063319, -1.999317321091613753 ) ) ;
#25968=CARTESIAN_POINT ( 'NONE',  ( 2.866494652520772846, -9.241976615239517301, 2.300561732649529123 ) ) ;
#25978=ORIENTED_EDGE ( 'NONE', *, *, #4476, .T. ) ;
#25987=B_SPLINE_CURVE_WITH_KNOTS ( 'NONE', 3,
 ( #348, #5681, #13335, #13516, #20735, #15532, #10521, #8348 ),
 .UNSPECIFIED., .F., .F.,
 ( 4, 2, 2, 4 ),
 ( 5.099451029802972801E-07, 0.001229189612685836199, 0.001843529446477266400, 0.002457869280268696818 ),
 .UNSPECIFIED. ) ;
#25997=CARTESIAN_POINT ( 'NONE',  ( -3.449949199999996274, 0.000000000000000000, 0.000000000000000000 ) ) ;
#25999=ORIENTED_EDGE ( 'NONE', *, *, #28017, .T. ) ;
#26005=ADVANCED_FACE ( 'NONE', ( #32295 ), #16718, .T. ) ;
#26011=VERTEX_POINT ( 'NONE', #8860 ) ;
#26016=ORIENTED_EDGE ( 'NONE', *, *, #27973, .T. ) ;
#26017=CARTESIAN_POINT ( 'NONE',  ( 0.4008809018342579522, 9.770170320898831307, 2.274078661686000924 ) ) ;
#26037=LINE ( 'NONE', #2998, #141 ) ;
#26044=FACE_OUTER_BOUND ( 'NONE', #12247, .T. ) ;
#26048=ORIENTED_EDGE ( 'NONE', *, *, #19705, .F. ) ;
#26049=DIRECTION ( 'NONE',  ( -1.000000000000000000, 0.000000000000000000, 0.000000000000000000 ) ) ;
#26052=EDGE_CURVE ( 'NONE', #10585, #9751, #24199, .T. ) ;
#26058=CARTESIAN_POINT ( 'NONE',  ( -3.690938403952409329E-13, 7.533794289458907834, 7.944914065997345176 ) ) ;
#26060=CARTESIAN_POINT ( 'NONE',  ( 2.274274201625316572, -7.958834565716716547, -7.593217523260693547 ) ) ;
#26071=CARTESIAN_POINT ( 'NONE',  ( 2.274274201627287884, 5.222868219167418502, -9.680994141364108074 ) ) ;
#26072=CARTESIAN_POINT ( 'NONE',  ( 3.249999999999999556, -7.360373001730883047, -4.729683950898953881 ) ) ;
#26090=DIRECTION ( 'NONE',  ( 0.000000000000000000, 0.000000000000000000, -1.000000000000000000 ) ) ;
#26093=DIRECTION ( 'NONE',  ( 1.000000000000000000, -0.000000000000000000, -0.000000000000000000 ) ) ;
#26117=DIRECTION ( 'NONE',  ( -1.000000000000000000, 0.000000000000000000, 0.000000000000000000 ) ) ;
#26125=DIRECTION ( 'NONE',  ( 0.000000000000000000, 0.000000000000000000, -1.000000000000000000 ) ) ;
#26128=CARTESIAN_POINT ( 'NONE',  ( 0.000000000000000000, 6.807171995660584507, 6.478011392632914145 ) ) ;
#26130=VERTEX_POINT ( 'NONE', #3028 ) ;
#26132=DIRECTION ( 'NONE',  ( 1.000000000000000000, 0.000000000000000000, 0.000000000000000000 ) ) ;
#26146=CARTESIAN_POINT ( 'NONE',  ( 2.274274201625327230, 9.680994141368847394, -5.222868219166750592 ) ) ;
#26149=ORIENTED_EDGE ( 'NONE', *, *, #21253, .T. ) ;
#26164=AXIS2_PLACEMENT_3D ( 'NONE', #15465, #30733, #28036 ) ;
#26173=AXIS2_PLACEMENT_3D ( 'NONE', #18288, #31186, #13109 ) ;
#26192=CARTESIAN_POINT ( 'NONE',  ( -3.690938403952409329E-13, 7.533794289458907834, 7.944914065997345176 ) ) ;
#26203=ORIENTED_EDGE ( 'NONE', *, *, #32400, .T. ) ;
#26204=DIRECTION ( 'NONE',  ( 1.000000000000000000, 0.000000000000000000, 0.000000000000000000 ) ) ;
#26233=EDGE_CURVE ( 'NONE', #27498, #16275, #3345, .T. ) ;
#26237=B_SPLINE_CURVE_WITH_KNOTS ( 'NONE', 3,
 ( #29486, #1737, #27295, #6581, #29660, #6741, #11935, #27127 ),
 .UNSPECIFIED., .F., .F.,
 ( 4, 2, 2, 4 ),
 ( 2.197717205396726239E-07, 0.001262070444981969576, 0.001892995781612684262, 0.002523921118243398730 ),
 .UNSPECIFIED. ) ;
#26252=ORIENTED_EDGE ( 'NONE', *, *, #28789, .T. ) ;
#26253=AXIS2_PLACEMENT_3D ( 'NONE', #3916, #1059, #5755 ) ;
#26257=CIRCLE ( 'NONE', #11833, 4.000000000000001776 ) ;
#26264=AXIS2_PLACEMENT_3D ( 'NONE', #19758, #4719, #22615 ) ;
#26266=DIRECTION ( 'NONE',  ( 0.000000000000000000, 0.000000000000000000, 1.000000000000000000 ) ) ;
#26270=DIRECTION ( 'NONE',  ( 1.000000000000000000, 0.000000000000000000, 0.000000000000000000 ) ) ;
#26272=CIRCLE ( 'NONE', #11844, 6.000000000000001776 ) ;
#26273=VECTOR ( 'NONE', #4823, 1000.000000000000000 ) ;
#26297=AXIS2_PLACEMENT_3D ( 'NONE', #11225, #8732, #16402 ) ;
#26301=CARTESIAN_POINT ( 'NONE',  ( 1.624999999999999778, 9.680994141368771011, 5.222868219166891812 ) ) ;
#26309=AXIS2_PLACEMENT_3D ( 'NONE', #23826, #11283, #26652 ) ;
#26320=AXIS2_PLACEMENT_3D ( 'NONE', #29692, #19655, #11621 ) ;
#26340=DIRECTION ( 'NONE',  ( 0.000000000000000000, 1.000000000000000000, 3.469446951953612611E-15 ) ) ;
#26343=ORIENTED_EDGE ( 'NONE', *, *, #1570, .F. ) ;
#26345=AXIS2_PLACEMENT_3D ( 'NONE', #14049, #13560, #26756 ) ;
#26346=ADVANCED_FACE ( 'NONE', ( #29573 ), #27045, .T. ) ;
#26358=CARTESIAN_POINT ( 'NONE',  ( 2.274274201621893976, 1.464956435144894931, 10.90201369671109610 ) ) ;
#26359=CARTESIAN_POINT ( 'NONE',  ( 0.7632845268398871230, 8.461683424509313767, 2.223716399045601921 ) ) ;
#26364=AXIS2_PLACEMENT_3D ( 'NONE', #16467, #27790, #29699 ) ;
#26392=CIRCLE ( 'NONE', #14622, 8.999999999999998224 ) ;
#26393=CIRCLE ( 'NONE', #9807, 11.00000000000000000 ) ;
#26400=DIRECTION ( 'NONE',  ( 0.000000000000000000, 0.000000000000000000, -1.000000000000000000 ) ) ;
#26406=CARTESIAN_POINT ( 'NONE',  ( -7.000050800000000351, 7.347880794884120722E-16, 6.000000000000000888 ) ) ;
#26412=EDGE_LOOP ( 'NONE', ( #1162, #29833, #11841, #18142 ) ) ;
#26426=CARTESIAN_POINT ( 'NONE',  ( 2.795120501772739630, -8.308193303464506130, -5.116149273377909701 ) ) ;
#26432=CARTESIAN_POINT ( 'NONE',  ( 0.000000000000000000, 4.762163868918412923, -9.915734732513168836 ) ) ;
#26451=CARTESIAN_POINT ( 'NONE',  ( 0.000000000000000000, 0.000000000000000000, 0.000000000000000000 ) ) ;
#26466=ORIENTED_EDGE ( 'NONE', *, *, #12571, .T. ) ;
#26468=CARTESIAN_POINT ( 'NONE',  ( 0.7632845268398871230, 8.461683424509313767, 2.223716399045601921 ) ) ;
#26474=CARTESIAN_POINT ( 'NONE',  ( 0.7632845268398871230, 0.000000000000000000, 0.000000000000000000 ) ) ;
#26490=EDGE_CURVE ( 'NONE', #4375, #28862, #18287, .T. ) ;
#26491=CARTESIAN_POINT ( 'NONE',  ( 2.274274201625327230, 10.90201369670498543, 1.464956435139579183 ) ) ;
#26497=VERTEX_POINT ( 'NONE', #26523 ) ;
#26506=EDGE_CURVE ( 'NONE', #2670, #7224, #31069, .T. ) ;
#26508=CARTESIAN_POINT ( 'NONE',  ( 0.7632845268398871230, 2.223716399045691183, -8.461683424509292450 ) ) ;
#26512=CARTESIAN_POINT ( 'NONE',  ( 0.7632845268398871230, -8.461683424509331530, 2.223716399045538861 ) ) ;
#26514=CARTESIAN_POINT ( 'NONE',  ( 3.249999999999999556, 0.000000000000000000, 0.000000000000000000 ) ) ;
#26521=DIRECTION ( 'NONE',  ( 1.000000000000000000, -0.000000000000000000, -0.000000000000000000 ) ) ;
#26523=CARTESIAN_POINT ( 'NONE',  ( 0.7632845268398871230, 4.729683950898978750, -7.360373001730866171 ) ) ;
#26538=EDGE_CURVE ( 'NONE', #3978, #8056, #17053, .T. ) ;
#26540=EDGE_CURVE ( 'NONE', #25174, #32970, #31117, .T. ) ;
#26542=CARTESIAN_POINT ( 'NONE',  ( 2.437082316315975383, -1.217322776604802037, 10.59788678609686308 ) ) ;
#26543=CARTESIAN_POINT ( 'NONE',  ( 2.274274201625327230, -4.762163868918204201, -9.915734732513268312 ) ) ;
#26546=CARTESIAN_POINT ( 'NONE',  ( 0.3045633657612867307, 6.808202580038980045, 7.698316278340386454 ) ) ;
#26547=CARTESIAN_POINT ( 'NONE',  ( -3.691385125341854500E-13, 10.85582367538961179, -1.425064293572943619 ) ) ;
#26550=ORIENTED_EDGE ( 'NONE', *, *, #23429, .T. ) ;
#26553=CARTESIAN_POINT ( 'NONE',  ( 0.7632845268398888994, -6.772677083992417302, 5.538577986808867593 ) ) ;
#26554=ORIENTED_EDGE ( 'NONE', *, *, #29176, .F. ) ;
#26556=DIRECTION ( 'NONE',  ( -1.000000000000000000, -0.000000000000000000, 0.000000000000000000 ) ) ;
#26566=CARTESIAN_POINT ( 'NONE',  ( 0.1606232843927789256, -10.56438947505147929, -1.177222770084765502 ) ) ;
#26572=ADVANCED_FACE ( 'NONE', ( #28551, #13467 ), #23686, .F. ) ;
#26574=EDGE_CURVE ( 'NONE', #32326, #20387, #7387, .T. ) ;
#26576=VERTEX_POINT ( 'NONE', #6884 ) ;
#26578=ORIENTED_EDGE ( 'NONE', *, *, #3720, .F. ) ;
#26580=CARTESIAN_POINT ( 'NONE',  ( 3.249999999999999556, 8.461683424509345741, -2.223716399045483350 ) ) ;
#26602=EDGE_LOOP ( 'NONE', ( #24123, #24343, #2947, #12864 ) ) ;
#26616=DIRECTION ( 'NONE',  ( -1.000000000000000000, -0.000000000000000000, -0.000000000000000000 ) ) ;
#26628=DIRECTION ( 'NONE',  ( 0.000000000000000000, -1.000000000000000000, -1.040834085586083626E-14 ) ) ;
#26632=EDGE_CURVE ( 'NONE', #31261, #3782, #21664, .T. ) ;
#26634=VERTEX_POINT ( 'NONE', #19962 ) ;
#26635=ADVANCED_FACE ( 'NONE', ( #17576 ), #1912, .T. ) ;
#26651=ORIENTED_EDGE ( 'NONE', *, *, #32746, .F. ) ;
#26652=DIRECTION ( 'NONE',  ( 0.000000000000000000, 0.000000000000000000, -1.000000000000000000 ) ) ;
#26666=CARTESIAN_POINT ( 'NONE',  ( -10.00000000000000000, 0.000000000000000000, 0.000000000000000000 ) ) ;
#26671=AXIS2_PLACEMENT_3D ( 'NONE', #391, #26117, #23772 ) ;
#26673=CARTESIAN_POINT ( 'NONE',  ( 3.249999999999999556, -8.461683424509331530, 2.223716399045538861 ) ) ;
#26679=EDGE_LOOP ( 'NONE', ( #29395, #23810, #19295, #9744, #29543 ) ) ;
#26692=VECTOR ( 'NONE', #10510, 1000.000000000000000 ) ;
#26699=CARTESIAN_POINT ( 'NONE',  ( 2.437082469501516080, -2.117184480729032092, -10.45536235038316519 ) ) ;
#26700=PLANE ( 'NONE',  #11432 ) ;
#26701=AXIS2_PLACEMENT_3D ( 'NONE', #8043, #30816, #18242 ) ;
#26711=CARTESIAN_POINT ( 'NONE',  ( 3.249999999999999556, -8.461683424509297780, -2.223716399045661873 ) ) ;
#26716=CARTESIAN_POINT ( 'NONE',  ( 3.249999999999999556, 1.699438267350499521, -9.241976615262139205 ) ) ;
#26730=CARTESIAN_POINT ( 'NONE',  ( 0.3045634671936391369, -10.22982953726848265, 0.9829946734954320142 ) ) ;
#26736=DIRECTION ( 'NONE',  ( 0.000000000000000000, 0.000000000000000000, -1.000000000000000000 ) ) ;
#26748=AXIS2_PLACEMENT_3D ( 'NONE', #27532, #27854, #4630 ) ;
#26756=DIRECTION ( 'NONE',  ( 0.000000000000000000, 0.000000000000000000, 1.000000000000000000 ) ) ;
#26760=ORIENTED_EDGE ( 'NONE', *, *, #32831, .T. ) ;
#26761=CARTESIAN_POINT ( 'NONE',  ( 0.7632845268398871230, 0.000000000000000000, 0.000000000000000000 ) ) ;
#26762=VECTOR ( 'NONE', #26521, 1000.000000000000000 ) ;
#26764=DIRECTION ( 'NONE',  ( 0.000000000000000000, 0.000000000000000000, -1.000000000000000000 ) ) ;
#26767=AXIS2_PLACEMENT_3D ( 'NONE', #28411, #8007, #10672 ) ;
#26776=ORIENTED_EDGE ( 'NONE', *, *, #29892, .T. ) ;
#26779=VECTOR ( 'NONE', #5005, 1000.000000000000000 ) ;
#26781=DIRECTION ( 'NONE',  ( 1.000000000000000000, -0.000000000000000000, -0.000000000000000000 ) ) ;
#26785=B_SPLINE_CURVE_WITH_KNOTS ( 'NONE', 3,
 ( #2082, #22466, #30502, #32683, #9764, #7586, #30187, #9929 ),
 .UNSPECIFIED., .F., .F.,
 ( 4, 2, 2, 4 ),
 ( 2.213836054414765521E-07, 0.001227982086136578848, 0.001841862437402150407, 0.002455742788667721749 ),
 .UNSPECIFIED. ) ;
#26794=AXIS2_PLACEMENT_3D ( 'NONE', #17355, #4644, #25018 ) ;
#26796=CARTESIAN_POINT ( 'NONE',  ( 0.6728002192015016814, -5.823680980849866629, 7.058361986489762430 ) ) ;
#26799=AXIS2_PLACEMENT_3D ( 'NONE', #27618, #27278, #9722 ) ;
#26804=AXIS2_PLACEMENT_3D ( 'NONE', #2784, #2973, #104 ) ;
#26820=VERTEX_POINT ( 'NONE', #25959 ) ;
#26822=CARTESIAN_POINT ( 'NONE',  ( 0.6791197550704605179, 2.303133748654099033, -8.860977624947469877 ) ) ;
#26825=DIRECTION ( 'NONE',  ( 0.000000000000000000, 0.000000000000000000, 1.000000000000000000 ) ) ;
#26849=CIRCLE ( 'NONE', #20993, 11.00000000000000000 ) ;
#26851=CARTESIAN_POINT ( 'NONE',  ( 3.063284526839887167, -4.729683950898817102, -7.360373001730970977 ) ) ;
#26877=EDGE_CURVE ( 'NONE', #29734, #30501, #28274, .T. ) ;
#26901=CARTESIAN_POINT ( 'NONE',  ( 0.7632845268398871230, -8.734705317681623171, -0.4999240074895356933 ) ) ;
#26902=CARTESIAN_POINT ( 'NONE',  ( 0.7212197917546229187, -4.829101774923286072, -7.537903528366462602 ) ) ;
#26906=ADVANCED_FACE ( 'NONE', ( #10227 ), #4890, .T. ) ;
#26910=EDGE_CURVE ( 'NONE', #660, #6261, #10406, .T. ) ;
#26940=FACE_OUTER_BOUND ( 'NONE', #20141, .T. ) ;
#26952=DIRECTION ( 'NONE',  ( 0.000000000000000000, 0.000000000000000000, -1.000000000000000000 ) ) ;
#26961=ORIENTED_EDGE ( 'NONE', *, *, #33077, .T. ) ;
#26971=CARTESIAN_POINT ( 'NONE',  ( -8.049676575031998738, 0.000000000000000000, 0.000000000000000000 ) ) ;
#26980=CYLINDRICAL_SURFACE ( 'NONE', #17840, 11.00000000000000000 ) ;
#26981=DIRECTION ( 'NONE',  ( -1.000000000000000000, 0.000000000000000000, 0.000000000000000000 ) ) ;
#26982=ORIENTED_EDGE ( 'NONE', *, *, #25415, .T. ) ;
#26999=CARTESIAN_POINT ( 'NONE',  ( 3.249999999999999556, 8.475820894092974456, 4.057423117305423155 ) ) ;
#27000=CARTESIAN_POINT ( 'NONE',  ( 2.795120465735310589, 2.298374178341501040, -9.482538569693103270 ) ) ;
#27002=CARTESIAN_POINT ( 'NONE',  ( 1.661358730909628482E-15, -10.85582367538893322, -1.425064293572451790 ) ) ;
#27003=EDGE_CURVE ( 'NONE', #8635, #32283, #17787, .T. ) ;
#27004=FACE_OUTER_BOUND ( 'NONE', #19882, .T. ) ;
#27045=CYLINDRICAL_SURFACE ( 'NONE', #15072, 8.749000000000002331 ) ;
#27058=EDGE_CURVE ( 'NONE', #9130, #7398, #12437, .T. ) ;
#27071=ORIENTED_EDGE ( 'NONE', *, *, #3809, .T. ) ;
#27079=CARTESIAN_POINT ( 'NONE',  ( 2.795120667414443982, 6.320583870825355000, 7.433119754671740687 ) ) ;
#27081=B_SPLINE_CURVE_WITH_KNOTS ( 'NONE', 3,
 ( #23773, #1380, #21423, #16553, #15908, #13722, #13384, #8724 ),
 .UNSPECIFIED., .F., .F.,
 ( 4, 2, 2, 4 ),
 ( 2.494123547463239299E-07, 0.001262099805913989656, 0.001893025002693609444, 0.002523950199473229232 ),
 .UNSPECIFIED. ) ;
#27087=CARTESIAN_POINT ( 'NONE',  ( 2.592584712405585634, -2.232024585011552542, 10.08167743096629287 ) ) ;
#27094=DIRECTION ( 'NONE',  ( 0.000000000000000000, 0.000000000000000000, 1.000000000000000000 ) ) ;
#27098=ORIENTED_EDGE ( 'NONE', *, *, #7504, .F. ) ;
#27099=CARTESIAN_POINT ( 'NONE',  ( 3.020080146456703751, -8.942241244950249524, 0.5244911560275880014 ) ) ;
#27102=ADVANCED_FACE ( 'NONE', ( #10855 ), #13999, .T. ) ;
#27107=VERTEX_POINT ( 'NONE', #26071 ) ;
#27115=CARTESIAN_POINT ( 'NONE',  ( 2.661997781067676705, -9.315861390595078007, -3.981025027156597229 ) ) ;
#27120=FACE_OUTER_BOUND ( 'NONE', #12425, .T. ) ;
#27126=EDGE_CURVE ( 'NONE', #6261, #31435, #1231, .T. ) ;
#27127=CARTESIAN_POINT ( 'NONE',  ( 3.063284526842892319, -5.538577986798981279, -6.772677083981775148 ) ) ;
#27136=DIRECTION ( 'NONE',  ( 1.000000000000000000, 0.000000000000000000, 0.000000000000000000 ) ) ;
#27138=DIRECTION ( 'NONE',  ( 0.000000000000000000, 0.000000000000000000, -1.000000000000000000 ) ) ;
#27142=EDGE_CURVE ( 'NONE', #32109, #31656, #14016, .T. ) ;
#27144=CARTESIAN_POINT ( 'NONE',  ( 0.6791197550704917152, -2.303133748654007995, 8.860977624947331321 ) ) ;
#27145=CARTESIAN_POINT ( 'NONE',  ( 0.7632845268398871230, 2.223716399045691183, -8.461683424509292450 ) ) ;
#27187=CARTESIAN_POINT ( 'NONE',  ( 1.624999999999999778, 10.82112760146736363, 1.975651141462276827 ) ) ;
#27190=CARTESIAN_POINT ( 'NONE',  ( -10.00000000000000000, 0.000000000000000000, 0.000000000000000000 ) ) ;
#27202=DIRECTION ( 'NONE',  ( -1.000000000000000000, 0.000000000000000000, -0.000000000000000000 ) ) ;
#27203=VERTEX_POINT ( 'NONE', #32573 ) ;
#27224=CARTESIAN_POINT ( 'NONE',  ( -3.691385125341854500E-13, 10.85582367538961179, -1.425064293572943619 ) ) ;
#27232=DIRECTION ( 'NONE',  ( 0.000000000000000000, 0.000000000000000000, -1.000000000000000000 ) ) ;
#27239=CARTESIAN_POINT ( 'NONE',  ( -7.000050800000000351, 0.000000000000000000, 0.000000000000000000 ) ) ;
#27241=DIRECTION ( 'NONE',  ( 0.000000000000000000, 0.000000000000000000, 1.000000000000000000 ) ) ;
#27250=CYLINDRICAL_SURFACE ( 'NONE', #24723, 4.000000000000001776 ) ;
#27251=ORIENTED_EDGE ( 'NONE', *, *, #4679, .T. ) ;
#27255=AXIS2_PLACEMENT_3D ( 'NONE', #21123, #11223, #26125 ) ;
#27264=ORIENTED_EDGE ( 'NONE', *, *, #2119, .F. ) ;
#27278=DIRECTION ( 'NONE',  ( -1.000000000000000000, -0.000000000000000000, -0.000000000000000000 ) ) ;
#27295=CARTESIAN_POINT ( 'NONE',  ( 2.592584925146038888, -6.844296717724863477, -7.731606906650728028 ) ) ;
#27299=CARTESIAN_POINT ( 'NONE',  ( 2.976845970491565296, -5.822399416825358109, 7.079702685456860323 ) ) ;
#27304=ORIENTED_EDGE ( 'NONE', *, *, #14733, .T. ) ;
#27308=DIRECTION ( 'NONE',  ( 1.000000000000000000, 0.000000000000000000, 0.000000000000000000 ) ) ;
#27316=EDGE_CURVE ( 'NONE', #6218, #1608, #27388, .T. ) ;
#27320=CIRCLE ( 'NONE', #5958, 4.000000000000002665 ) ;
#27335=CARTESIAN_POINT ( 'NONE',  ( 2.942345435796908326, 8.982973658106383041, 2.300561732649640589 ) ) ;
#27336=CARTESIAN_POINT ( 'NONE',  ( 0.000000000000000000, -1.699438267350306120, -9.241976615262172956 ) ) ;
#27338=CARTESIAN_POINT ( 'NONE',  ( 9.101556641444268791, 0.000000000000000000, -3.895301350492843540 ) ) ;
#27341=EDGE_CURVE ( 'NONE', #22797, #23619, #4982, .T. ) ;
#27345=AXIS2_PLACEMENT_3D ( 'NONE', #5477, #10637, #28700 ) ;
#27353=VERTEX_POINT ( 'NONE', #25493 ) ;
#27358=ORIENTED_EDGE ( 'NONE', *, *, #26538, .F. ) ;
#27388=LINE ( 'NONE', #24213, #16700 ) ;
#27401=ORIENTED_EDGE ( 'NONE', *, *, #12334, .T. ) ;
#27406=AXIS2_PLACEMENT_3D ( 'NONE', #14286, #24481, #29537 ) ;
#27407=AXIS2_PLACEMENT_3D ( 'NONE', #15031, #25063, #6852 ) ;
#27408=FACE_BOUND ( 'NONE', #16880, .T. ) ;
#27409=DIRECTION ( 'NONE',  ( 0.000000000000000000, 0.000000000000000000, 1.000000000000000000 ) ) ;
#27415=CARTESIAN_POINT ( 'NONE',  ( 2.970200390936400758, 9.143933199846960846, -0.5647484630024097729 ) ) ;
#27426=ORIENTED_EDGE ( 'NONE', *, *, #1848, .F. ) ;
#27430=CYLINDRICAL_SURFACE ( 'NONE', #19487, 8.749000000000002331 ) ;
#27441=CARTESIAN_POINT ( 'NONE',  ( 0.3076690219785659930, 7.713510465966315621, 6.806638167507657045 ) ) ;
#27451=ORIENTED_EDGE ( 'NONE', *, *, #27341, .F. ) ;
#27472=CARTESIAN_POINT ( 'NONE',  ( 0.000000000000000000, -4.057423117305452465, 8.475820894092962021 ) ) ;
#27481=CARTESIAN_POINT ( 'NONE',  ( 0.000000000000000000, 0.000000000000000000, 0.000000000000000000 ) ) ;
#27486=ORIENTED_EDGE ( 'NONE', *, *, #11240, .T. ) ;
#27490=CARTESIAN_POINT ( 'NONE',  ( 3.249999999999999556, 6.772677083992387992, 5.538577986808924436 ) ) ;
#27498=VERTEX_POINT ( 'NONE', #2963 ) ;
#27504=DIRECTION ( 'NONE',  ( -1.000000000000000000, 0.000000000000000000, -0.000000000000000000 ) ) ;
#27505=DIRECTION ( 'NONE',  ( 1.000000000000000000, 0.000000000000000000, -0.000000000000000000 ) ) ;
#27511=B_SPLINE_CURVE_WITH_KNOTS ( 'NONE', 3,
 ( #2029, #29937, #27441, #12201, #9876, #30283, #22401, #32619 ),
 .UNSPECIFIED., .F., .F.,
 ( 4, 2, 2, 4 ),
 ( 5.099451029799539141E-07, 0.001229190215600031548, 0.001843530350848556279, 0.002457870486097081010 ),
 .UNSPECIFIED. ) ;
#27532=CARTESIAN_POINT ( 'NONE',  ( 3.249999999999999556, 0.000000000000000000, 0.000000000000000000 ) ) ;
#27535=EDGE_CURVE ( 'NONE', #4750, #8629, #4278, .T. ) ;
#27540=DIRECTION ( 'NONE',  ( 0.000000000000000000, 0.000000000000000000, 1.000000000000000000 ) ) ;
#27544=CARTESIAN_POINT ( 'NONE',  ( 0.3076688720859502846, 0.9727984658936051909, -10.24120291390721427 ) ) ;
#27547=DIRECTION ( 'NONE',  ( 0.000000000000000000, 0.000000000000000000, 1.000000000000000000 ) ) ;
#27561=CARTESIAN_POINT ( 'NONE',  ( 3.249999999999999556, 6.807171995660674213, -6.478011392632816445 ) ) ;
#27572=CARTESIAN_POINT ( 'NONE',  ( 2.592584512312228195, 10.27797909968510126, -0.9926283730736131794 ) ) ;
#27577=ORIENTED_EDGE ( 'NONE', *, *, #8777, .T. ) ;
#27585=CARTESIAN_POINT ( 'NONE',  ( 3.020080256209073610, 5.680439424473828325, 6.926136578651334474 ) ) ;
#27592=CARTESIAN_POINT ( 'NONE',  ( 10.25005080000000035, 0.000000000000000000, 3.499999999999999556 ) ) ;
#27602=CARTESIAN_POINT ( 'NONE',  ( 3.249999999999999556, 0.000000000000000000, 0.000000000000000000 ) ) ;
#27605=ORIENTED_EDGE ( 'NONE', *, *, #9210, .F. ) ;
#27608=ORIENTED_EDGE ( 'NONE', *, *, #30438, .T. ) ;
#27614=CARTESIAN_POINT ( 'NONE',  ( 0.000000000000000000, 5.227991826304090317, 9.620177616658001085 ) ) ;
#27618=CARTESIAN_POINT ( 'NONE',  ( 0.000000000000000000, 0.000000000000000000, 0.000000000000000000 ) ) ;
#27628=CARTESIAN_POINT ( 'NONE',  ( 0.7632845268398873451, -5.538577986808840059, -6.772677083992440394 ) ) ;
#27652=DIRECTION ( 'NONE',  ( 1.000000000000000000, -0.000000000000000000, -0.000000000000000000 ) ) ;
#27657=EDGE_CURVE ( 'NONE', #16174, #10288, #26237, .T. ) ;
#27666=ORIENTED_EDGE ( 'NONE', *, *, #24477, .T. ) ;
#27674=ORIENTED_EDGE ( 'NONE', *, *, #21268, .F. ) ;
#27679=DIRECTION ( 'NONE',  ( -1.000000000000000000, 0.000000000000000000, 0.000000000000000000 ) ) ;
#27680=ORIENTED_EDGE ( 'NONE', *, *, #4662, .F. ) ;
#27683=LINE ( 'NONE', #14654, #29428 ) ;
#27691=CARTESIAN_POINT ( 'NONE',  ( 0.000000000000000000, -9.884132761439094139, 4.709950686174575907 ) ) ;
#27700=ORIENTED_EDGE ( 'NONE', *, *, #18777, .T. ) ;
#27705=LINE ( 'NONE', #25208, #23654 ) ;
#27714=DIRECTION ( 'NONE',  ( 0.000000000000000000, 0.000000000000000000, -1.000000000000000000 ) ) ;
#27730=ORIENTED_EDGE ( 'NONE', *, *, #10095, .T. ) ;
#27753=CARTESIAN_POINT ( 'NONE',  ( -10.00000000000000000, 0.000000000000000000, 0.000000000000000000 ) ) ;
#27754=ORIENTED_EDGE ( 'NONE', *, *, #19914, .T. ) ;
#27763=CARTESIAN_POINT ( 'NONE',  ( 0.6728001243864736303, 4.913284922774382224, 7.719803900020800747 ) ) ;
#27764=ORIENTED_EDGE ( 'NONE', *, *, #31997, .F. ) ;
#27790=DIRECTION ( 'NONE',  ( 1.000000000000000000, -0.000000000000000000, -0.000000000000000000 ) ) ;
#27798=VECTOR ( 'NONE', #24346, 1000.000000000000000 ) ;
#27803=CARTESIAN_POINT ( 'NONE',  ( -8.049676575031998738, 8.479088208360996928E-16, 6.923700951379997193 ) ) ;
#27806=CARTESIAN_POINT ( 'NONE',  ( 3.249999999999999556, -8.475820894092944258, -4.057423117305486215 ) ) ;
#27814=FACE_OUTER_BOUND ( 'NONE', #32829, .T. ) ;
#27823=DIRECTION ( 'NONE',  ( 0.000000000000000000, 0.000000000000000000, -1.000000000000000000 ) ) ;
#27833=FACE_OUTER_BOUND ( 'NONE', #2540, .T. ) ;
#27835=ORIENTED_EDGE ( 'NONE', *, *, #4219, .T. ) ;
#27837=B_SPLINE_CURVE_WITH_KNOTS ( 'NONE', 3,
 ( #4529, #14529, #14343, #24738, #32603, #17386, #7004, #4029 ),
 .UNSPECIFIED., .F., .F.,
 ( 4, 2, 2, 4 ),
 ( 2.024520226902067482E-07, 0.001261135997420258399, 0.001891602770119042579, 0.002522069542817826325 ),
 .UNSPECIFIED. ) ;
#27838=ORIENTED_EDGE ( 'NONE', *, *, #16337, .F. ) ;
#27843=ORIENTED_EDGE ( 'NONE', *, *, #7921, .F. ) ;
#27847=AXIS2_PLACEMENT_3D ( 'NONE', #8793, #16456, #31719 ) ;
#27849=ORIENTED_EDGE ( 'NONE', *, *, #18370, .F. ) ;
#27854=DIRECTION ( 'NONE',  ( -1.000000000000000000, 0.000000000000000000, -0.000000000000000000 ) ) ;
#27855=CARTESIAN_POINT ( 'NONE',  ( 0.000000000000000000, -1.425064293572261276, -10.85582367538895632 ) ) ;
#27857=AXIS2_PLACEMENT_3D ( 'NONE', #23900, #3540, #6190 ) ;
#27861=VECTOR ( 'NONE', #24891, 1000.000000000000000 ) ;
#27868=VECTOR ( 'NONE', #28955, 1000.000000000000000 ) ;
#27881=AXIS2_PLACEMENT_3D ( 'NONE', #8700, #3692, #26266 ) ;
#27884=CARTESIAN_POINT ( 'NONE',  ( 3.063284526839887167, -8.152713396088739017, -3.174628368996162298 ) ) ;
#27888=CIRCLE ( 'NONE', #26804, 8.749000000000002331 ) ;
#27891=FACE_OUTER_BOUND ( 'NONE', #5084, .T. ) ;
#27896=CARTESIAN_POINT ( 'NONE',  ( -10.00000000000000000, 0.000000000000000000, 0.000000000000000000 ) ) ;
#27897=CIRCLE ( 'NONE', #1226, 8.749000000000002331 ) ;
#27898=CYLINDRICAL_SURFACE ( 'NONE', #28962, 6.000000000000000888 ) ;
#27901=ORIENTED_EDGE ( 'NONE', *, *, #4820, .F. ) ;
#27912=DIRECTION ( 'NONE',  ( 0.000000000000000000, 0.000000000000000000, 1.000000000000000000 ) ) ;
#27915=AXIS2_PLACEMENT_3D ( 'NONE', #27561, #20550, #25540 ) ;
#27916=EDGE_LOOP ( 'NONE', ( #27451, #12834, #28739, #6105 ) ) ;
#27917=CARTESIAN_POINT ( 'NONE',  ( 0.000000000000000000, 4.709950686174755319, -9.884132761439010650 ) ) ;
#27919=AXIS2_PLACEMENT_3D ( 'NONE', #11184, #21570, #28749 ) ;
#27921=DIRECTION ( 'NONE',  ( 0.000000000000000000, 0.000000000000000000, -1.000000000000000000 ) ) ;
#27926=CARTESIAN_POINT ( 'NONE',  ( 2.274274201625327230, 0.000000000000000000, 0.000000000000000000 ) ) ;
#27928=AXIS2_PLACEMENT_3D ( 'NONE', #29346, #4904, #8805 ) ;
#27936=AXIS2_PLACEMENT_3D ( 'NONE', #27190, #17347, #27540 ) ;
#27952=EDGE_LOOP ( 'NONE', ( #20530, #23474, #12549, #16476, #20597 ) ) ;
#27955=DIRECTION ( 'NONE',  ( -1.000000000000000000, 0.000000000000000000, 0.000000000000000000 ) ) ;
#27956=FACE_OUTER_BOUND ( 'NONE', #11705, .T. ) ;
#27960=CARTESIAN_POINT ( 'NONE',  ( 0.000000000000000000, 0.000000000000000000, 0.000000000000000000 ) ) ;
#27973=EDGE_CURVE ( 'NONE', #12277, #2968, #6587, .T. ) ;
#27984=ORIENTED_EDGE ( 'NONE', *, *, #2829, .T. ) ;
#27990=CARTESIAN_POINT ( 'NONE',  ( 2.274274201625327230, 1.464956435139694868, -10.90201369670497122 ) ) ;
#27994=DIRECTION ( 'NONE',  ( -1.000000000000000000, -0.000000000000000000, 0.000000000000000000 ) ) ;
#28005=ADVANCED_FACE ( 'NONE', ( #18358 ), #623, .T. ) ;
#28017=EDGE_CURVE ( 'NONE', #21952, #5917, #8626, .T. ) ;
#28018=CARTESIAN_POINT ( 'NONE',  ( 0.000000000000000000, -9.241976615262146311, -1.699438267350472209 ) ) ;
#28019=ORIENTED_EDGE ( 'NONE', *, *, #2552, .F. ) ;
#28024=DIRECTION ( 'NONE',  ( -1.000000000000000000, 0.000000000000000000, 0.000000000000000000 ) ) ;
#28030=ORIENTED_EDGE ( 'NONE', *, *, #18528, .T. ) ;
#28034=ORIENTED_EDGE ( 'NONE', *, *, #12601, .T. ) ;
#28036=DIRECTION ( 'NONE',  ( 0.000000000000000000, 0.000000000000000000, 1.000000000000000000 ) ) ;
#28065=ORIENTED_EDGE ( 'NONE', *, *, #31082, .F. ) ;
#28070=DIRECTION ( 'NONE',  ( -1.000000000000000000, 0.000000000000000000, 0.000000000000000000 ) ) ;
#28087=CARTESIAN_POINT ( 'NONE',  ( 2.970200414851742021, -8.870914041964216068, -2.288523046050828569 ) ) ;
#28094=EDGE_CURVE ( 'NONE', #1557, #14743, #2340, .T. ) ;
#28096=DIRECTION ( 'NONE',  ( -1.000000000000000000, 0.000000000000000000, 0.000000000000000000 ) ) ;
#28123=LINE ( 'NONE', #18248, #12378 ) ;
#28137=ORIENTED_EDGE ( 'NONE', *, *, #22854, .F. ) ;
#28138=CARTESIAN_POINT ( 'NONE',  ( 0.000000000000000000, -4.709950686174546597, -9.884132761439110126 ) ) ;
#28142=VERTEX_POINT ( 'NONE', #26851 ) ;
#28149=ORIENTED_EDGE ( 'NONE', *, *, #9841, .F. ) ;
#28156=CARTESIAN_POINT ( 'NONE',  ( -3.691545173129016004E-13, 1.425064293572904539, 10.85582367538961535 ) ) ;
#28159=ADVANCED_FACE ( 'NONE', ( #14446 ), #19661, .T. ) ;
#28161=CARTESIAN_POINT ( 'NONE',  ( 0.000000000000000000, 0.000000000000000000, 0.000000000000000000 ) ) ;
#28168=ORIENTED_EDGE ( 'NONE', *, *, #11415, .F. ) ;
#28177=CARTESIAN_POINT ( 'NONE',  ( 3.249999999999999556, 0.000000000000000000, 0.000000000000000000 ) ) ;
#28183=ORIENTED_EDGE ( 'NONE', *, *, #22854, .T. ) ;
#28191=DIRECTION ( 'NONE',  ( 0.000000000000000000, 0.000000000000000000, -1.000000000000000000 ) ) ;
#28198=EDGE_CURVE ( 'NONE', #29792, #10525, #3416, .T. ) ;
#28200=DIRECTION ( 'NONE',  ( 0.000000000000000000, 0.000000000000000000, -1.000000000000000000 ) ) ;
#28205=ORIENTED_EDGE ( 'NONE', *, *, #22219, .F. ) ;
#28213=PRODUCT_DEFINITION ( 'UNKNOWN', '', #2373, #29298 ) ;
#28219=CARTESIAN_POINT ( 'NONE',  ( -4.599999999999996980, 1.224646799147353256E-15, 10.00000000000000178 ) ) ;
#28224=EDGE_CURVE ( 'NONE', #16893, #6314, #13821, .T. ) ;
#28230=DIRECTION ( 'NONE',  ( -1.000000000000000000, 0.000000000000000000, 0.000000000000000000 ) ) ;
#28237=DIRECTION ( 'NONE',  ( 0.000000000000000000, 0.8090169943749485615, -0.5877852522924714718 ) ) ;
#28240=DIRECTION ( 'NONE',  ( 0.000000000000000000, 0.000000000000000000, 1.000000000000000000 ) ) ;
#28266=ADVANCED_FACE ( 'NONE', ( #27833 ), #2604, .T. ) ;
#28274=LINE ( 'NONE', #529, #19367 ) ;
#28280=VECTOR ( 'NONE', #11598, 1000.000000000000000 ) ;
#28299=EDGE_CURVE ( 'NONE', #3652, #19151, #8103, .T. ) ;
#28304=ORIENTED_EDGE ( 'NONE', *, *, #21592, .T. ) ;
#28317=CARTESIAN_POINT ( 'NONE',  ( 2.274274201625327230, -10.90201369670499609, 1.464956435139503022 ) ) ;
#28325=B_SPLINE_CURVE_WITH_KNOTS ( 'NONE', 3,
 ( #21635, #19290, #29002, #18796, #9063, #14252, #8429, #29156 ),
 .UNSPECIFIED., .F., .F.,
 ( 4, 2, 2, 4 ),
 ( 2.213836054372184116E-07, 0.001261154818855338578, 0.001891621536480289894, 0.002522088254105241210 ),
 .UNSPECIFIED. ) ;
#28327=CARTESIAN_POINT ( 'NONE',  ( 3.249999999999999556, 0.000000000000000000, 0.000000000000000000 ) ) ;
#28330=CARTESIAN_POINT ( 'NONE',  ( 3.249999999999999556, -8.152713396088785203, 3.174628368996044170 ) ) ;
#28344=CARTESIAN_POINT ( 'NONE',  ( 0.7212197813410881064, -8.337493976400217832, -3.259817272377353969 ) ) ;
#28350=CARTESIAN_POINT ( 'NONE',  ( 0.7632845268448663623, 0.4999240074867329353, -8.734705317657697421 ) ) ;
#28362=EDGE_CURVE ( 'NONE', #14707, #29348, #15435, .T. ) ;
#28380=AXIS2_PLACEMENT_3D ( 'NONE', #32205, #8612, #21659 ) ;
#28383=CARTESIAN_POINT ( 'NONE',  ( 0.3076689118679163393, 9.439351442243307133, 4.089891983576743328 ) ) ;
#28385=ADVANCED_FACE ( 'NONE', ( #29664 ), #26980, .T. ) ;
#28395=EDGE_CURVE ( 'NONE', #11731, #26820, #8738, .T. ) ;
#28398=CARTESIAN_POINT ( 'NONE',  ( 3.063284526839887167, -6.772677083992345359, -5.538577986808975062 ) ) ;
#28406=ORIENTED_EDGE ( 'NONE', *, *, #851, .T. ) ;
#28408=VECTOR ( 'NONE', #14166, 1000.000000000000000 ) ;
#28411=CARTESIAN_POINT ( 'NONE',  ( 0.000000000000000000, 0.000000000000000000, 0.000000000000000000 ) ) ;
#28423=CYLINDRICAL_SURFACE ( 'NONE', #1209, 4.000000000000001776 ) ;
#28454=CARTESIAN_POINT ( 'NONE',  ( 2.274274201625315683, -4.762163868918371179, 9.915734732513216798 ) ) ;
#28456=DIRECTION ( 'NONE',  ( -1.000000000000000000, 0.000000000000000000, 0.000000000000000000 ) ) ;
#28463=AXIS2_PLACEMENT_3D ( 'NONE', #28018, #5114, #15291 ) ;
#28470=CARTESIAN_POINT ( 'NONE',  ( 3.063284526839887167, -0.4999240074895051067, 8.734705317681624948 ) ) ;
#28474=DIRECTION ( 'NONE',  ( -1.000000000000000000, -0.000000000000000000, -0.000000000000000000 ) ) ;
#28485=CIRCLE ( 'NONE', #7116, 4.000000000000001776 ) ;
#28491=CIRCLE ( 'NONE', #6591, 6.999999999999998224 ) ;
#28495=ORIENTED_EDGE ( 'NONE', *, *, #10100, .F. ) ;
#28496=VERTEX_POINT ( 'NONE', #8909 ) ;
#28502=CARTESIAN_POINT ( 'NONE',  ( 2.274274201620947622, 4.762163868927166810, 9.915734732518528105 ) ) ;
#28506=CARTESIAN_POINT ( 'NONE',  ( 0.7632845268398876781, -0.4999240074893807617, -8.734705317681624948 ) ) ;
#28536=CARTESIAN_POINT ( 'NONE',  ( 0.5640492184727915470, -8.844377740319856684, -3.576105523038093814 ) ) ;
#28537=ORIENTED_EDGE ( 'NONE', *, *, #11511, .F. ) ;
#28538=CARTESIAN_POINT ( 'NONE',  ( 0.3076690219785678804, 6.806638167507736092, -7.713510465966239238 ) ) ;
#28539=DIRECTION ( 'NONE',  ( 0.000000000000000000, 0.000000000000000000, -1.000000000000000000 ) ) ;
#28541=DIRECTION ( 'NONE',  ( -1.000000000000000000, 0.000000000000000000, 0.000000000000000000 ) ) ;
#28546=CARTESIAN_POINT ( 'NONE',  ( 0.7632845268398883443, -7.360373001730875053, -4.729683950898950329 ) ) ;
#28551=FACE_BOUND ( 'NONE', #11036, .T. ) ;
#28573=DIRECTION ( 'NONE',  ( 0.000000000000000000, 0.000000000000000000, 1.000000000000000000 ) ) ;
#28589=CARTESIAN_POINT ( 'NONE',  ( 3.249999999999999556, 9.241976615262160522, -1.699438267350404930 ) ) ;
#28590=CARTESIAN_POINT ( 'NONE',  ( 2.864530965498453430, 2.320611941139924195, 9.276519854389871256 ) ) ;
#28595=CARTESIAN_POINT ( 'NONE',  ( 2.592584839945472730, -8.898511132913942134, -5.238191131136724188 ) ) ;
#28599=ORIENTED_EDGE ( 'NONE', *, *, #30430, .F. ) ;
#28601=DIRECTION ( 'NONE',  ( 0.000000000000000000, 0.000000000000000000, -1.000000000000000000 ) ) ;
#28603=CARTESIAN_POINT ( 'NONE',  ( 0.5704035821694232178, -9.519055809314989958, 0.6538686328478395815 ) ) ;
#28618=ADVANCED_FACE ( 'NONE', ( #15088 ), #20280, .F. ) ;
#28619=CARTESIAN_POINT ( 'NONE',  ( 2.976845773540285567, -3.349682859779558264, 8.532418605434719083 ) ) ;
#28631=EDGE_LOOP ( 'NONE', ( #11385, #17213, #8951, #8469 ) ) ;
#28632=CARTESIAN_POINT ( 'NONE',  ( -5.750050799999999462, 0.000000000000000000, -6.000000000000001776 ) ) ;
#28646=DIRECTION ( 'NONE',  ( -1.000000000000000000, -0.000000000000000000, -0.000000000000000000 ) ) ;
#28656=ADVANCED_FACE ( 'NONE', ( #17770 ), #23128, .T. ) ;
#28657=DIRECTION ( 'NONE',  ( -1.000000000000000000, 0.000000000000000000, -0.000000000000000000 ) ) ;
#28659=DIRECTION ( 'NONE',  ( -1.000000000000000000, 0.000000000000000000, 0.000000000000000000 ) ) ;
#28671=DIRECTION ( 'NONE',  ( -1.000000000000000000, -0.000000000000000000, -0.000000000000000000 ) ) ;
#28679=VERTEX_POINT ( 'NONE', #539 ) ;
#28684=ORIENTED_EDGE ( 'NONE', *, *, #26910, .T. ) ;
#28688=DIRECTION ( 'NONE',  ( 0.000000000000000000, 0.000000000000000000, -1.000000000000000000 ) ) ;
#28700=DIRECTION ( 'NONE',  ( 0.000000000000000000, 0.000000000000000000, 1.000000000000000000 ) ) ;
#28704=ORIENTED_EDGE ( 'NONE', *, *, #31745, .F. ) ;
#28709=ORIENTED_EDGE ( 'NONE', *, *, #3904, .T. ) ;
#28711=ORIENTED_EDGE ( 'NONE', *, *, #10745, .T. ) ;
#28722=CYLINDRICAL_SURFACE ( 'NONE', #3237, 4.000000000000001776 ) ;
#28723=ORIENTED_EDGE ( 'NONE', *, *, #29209, .F. ) ;
#28731=VERTEX_POINT ( 'NONE', #23289 ) ;
#28732=DIRECTION ( 'NONE',  ( 1.000000000000000000, -0.000000000000000000, -0.000000000000000000 ) ) ;
#28737=CARTESIAN_POINT ( 'NONE',  ( 0.5640491561200829951, -9.516580665864454502, -0.6680154998155471979 ) ) ;
#28739=ORIENTED_EDGE ( 'NONE', *, *, #21346, .T. ) ;
#28741=EDGE_CURVE ( 'NONE', #2323, #22995, #9575, .T. ) ;
#28749=DIRECTION ( 'NONE',  ( 0.000000000000000000, 0.000000000000000000, -1.000000000000000000 ) ) ;
#28757=DIRECTION ( 'NONE',  ( 0.000000000000000000, 0.000000000000000000, 1.000000000000000000 ) ) ;
#28774=CARTESIAN_POINT ( 'NONE',  ( 0.000000000000000000, 0.000000000000000000, 0.000000000000000000 ) ) ;
#28776=CARTESIAN_POINT ( 'NONE',  ( 0.000000000000000000, 1.464956435139693758, -10.90201369670496945 ) ) ;
#28781=VERTEX_POINT ( 'NONE', #14857 ) ;
#28789=EDGE_CURVE ( 'NONE', #4162, #16869, #32165, .T. ) ;
#28800=CIRCLE ( 'NONE', #30974, 15.00000000000000355 ) ;
#28819=ORIENTED_EDGE ( 'NONE', *, *, #30438, .F. ) ;
#28821=ORIENTED_EDGE ( 'NONE', *, *, #4820, .T. ) ;
#28824=ORIENTED_EDGE ( 'NONE', *, *, #8233, .T. ) ;
#28831=EDGE_CURVE ( 'NONE', #3275, #19087, #3730, .T. ) ;
#28846=CIRCLE ( 'NONE', #9622, 6.000000000000001776 ) ;
#28853=VECTOR ( 'NONE', #20643, 1000.000000000000000 ) ;
#28859=CARTESIAN_POINT ( 'NONE',  ( 2.274274201625327230, 0.000000000000000000, 0.000000000000000000 ) ) ;
#28860=CARTESIAN_POINT ( 'NONE',  ( 3.063284526839890720, 8.461683424509336859, -2.223716399045483794 ) ) ;
#28862=VERTEX_POINT ( 'NONE', #7506 ) ;
#28867=ADVANCED_FACE ( 'NONE', ( #4842 ), #15995, .F. ) ;
#28869=VECTOR ( 'NONE', #10358, 1000.000000000000000 ) ;
#28877=CARTESIAN_POINT ( 'NONE',  ( 0.7632845268398871230, 8.734705317681626724, -0.4999240074894737984 ) ) ;
#28878=CARTESIAN_POINT ( 'NONE',  ( 2.437082531750065506, -7.858345965138736844, -7.214115859539328213 ) ) ;
#28904=EDGE_CURVE ( 'NONE', #26497, #7095, #14192, .T. ) ;
#28912=CARTESIAN_POINT ( 'NONE',  ( 0.7632845268398871230, -2.223716399045513548, -8.461683424509338636 ) ) ;
#28918=CARTESIAN_POINT ( 'NONE',  ( 3.249999999999999556, -6.807171995660538322, -6.478011392632959442 ) ) ;
#28928=CARTESIAN_POINT ( 'NONE',  ( 3.249999999999999556, 0.000000000000000000, 0.000000000000000000 ) ) ;
#28932=CARTESIAN_POINT ( 'NONE',  ( 2.357329973329931772, -4.593471141847137673, 9.815384016743307072 ) ) ;
#28934=VECTOR ( 'NONE', #20327, 1000.000000000000000 ) ;
#28942=EDGE_CURVE ( 'NONE', #24335, #5149, #13835, .T. ) ;
#28955=DIRECTION ( 'NONE',  ( -1.000000000000000000, 0.000000000000000000, 0.000000000000000000 ) ) ;
#28959=CARTESIAN_POINT ( 'NONE',  ( 0.1255855353732055757, -9.314797388894898944, 5.239665997526856245 ) ) ;
#28962=AXIS2_PLACEMENT_3D ( 'NONE', #17520, #2654, #27714 ) ;
#28964=ORIENTED_EDGE ( 'NONE', *, *, #18951, .F. ) ;
#28972=DIRECTION ( 'NONE',  ( 0.000000000000000000, 0.000000000000000000, 1.000000000000000000 ) ) ;
#28980=DIRECTION ( 'NONE',  ( -1.000000000000000000, -0.000000000000000000, -0.000000000000000000 ) ) ;
#28986=CIRCLE ( 'NONE', #16674, 6.000000000000000888 ) ;
#28993=DIRECTION ( 'NONE',  ( -1.000000000000000000, 0.000000000000000000, 0.000000000000000000 ) ) ;
#28994=EDGE_CURVE ( 'NONE', #29455, #25356, #31486, .T. ) ;
#28997=CARTESIAN_POINT ( 'NONE',  ( 2.589202797589367222, 10.26630467377258604, 1.003524335601056139 ) ) ;
#29002=CARTESIAN_POINT ( 'NONE',  ( 2.864531019710238269, 8.868883597856997980, 3.575186956654012427 ) ) ;
#29003=AXIS2_PLACEMENT_3D ( 'NONE', #11347, #28732, #3172 ) ;
#29014=ORIENTED_EDGE ( 'NONE', *, *, #2990, .T. ) ;
#29028=VECTOR ( 'NONE', #941, 1000.000000000000000 ) ;
#29035=CIRCLE ( 'NONE', #231, 4.000000000000001776 ) ;
#29036=VECTOR ( 'NONE', #1145, 1000.000000000000000 ) ;
#29049=CYLINDRICAL_SURFACE ( 'NONE', #1778, 4.000000000000001776 ) ;
#29055=ORIENTED_EDGE ( 'NONE', *, *, #16319, .F. ) ;
#29081=DIRECTION ( 'NONE',  ( 0.000000000000000000, -0.5877852522924624790, -0.8090169943749553338 ) ) ;
#29087=CARTESIAN_POINT ( 'NONE',  ( 0.3076689308762635688, -5.232617538234820564, -8.857103639579413823 ) ) ;
#29109=EDGE_CURVE ( 'NONE', #1745, #8635, #13320, .T. ) ;
#29132=ORIENTED_EDGE ( 'NONE', *, *, #28094, .T. ) ;
#29137=EDGE_CURVE ( 'NONE', #16174, #12210, #17985, .T. ) ;
#29156=CARTESIAN_POINT ( 'NONE',  ( 2.274274201625327230, 9.915734732513220351, 4.762163868918306342 ) ) ;
#29161=ORIENTED_EDGE ( 'NONE', *, *, #16890, .T. ) ;
#29162=B_SPLINE_CURVE_WITH_KNOTS ( 'NONE', 3,
 ( #6387, #14392, #32342, #11738, #16585, #26796, #21941, #3917 ),
 .UNSPECIFIED., .F., .F.,
 ( 4, 2, 2, 4 ),
 ( 5.099451029781804389E-07, 0.001229190215587242516, 0.001843530350829372839, 0.002457870486071503380 ),
 .UNSPECIFIED. ) ;
#29173=ORIENTED_EDGE ( 'NONE', *, *, #32319, .F. ) ;
#29176=EDGE_CURVE ( 'NONE', #14830, #8629, #17602, .T. ) ;
#29179=CARTESIAN_POINT ( 'NONE',  ( 2.592584839944457986, 5.238191131136629153, -8.898511132916340216 ) ) ;
#29192=ADVANCED_FACE ( 'NONE', ( #20813 ), #30872, .T. ) ;
#29207=CARTESIAN_POINT ( 'NONE',  ( 2.661997850953048417, 5.196702353893204673, 8.696442646092039652 ) ) ;
#29209=EDGE_CURVE ( 'NONE', #8190, #19301, #25347, .T. ) ;
#29212=CARTESIAN_POINT ( 'NONE',  ( 0.5704035821693393959, 9.519055809315281280, -0.6538686328479882404 ) ) ;
#29213=DIRECTION ( 'NONE',  ( 0.000000000000000000, 0.000000000000000000, 1.000000000000000000 ) ) ;
#29220=CARTESIAN_POINT ( 'NONE',  ( 2.976845726615121368, -2.305279507610546119, -8.871766062375181505 ) ) ;
#29226=VERTEX_POINT ( 'NONE', #286 ) ;
#29227=CARTESIAN_POINT ( 'NONE',  ( 0.000000000000000000, 4.057423117305515525, -8.475820894092930047 ) ) ;
#29237=ORIENTED_EDGE ( 'NONE', *, *, #26540, .T. ) ;
#29249=DIRECTION ( 'NONE',  ( -1.000000000000000000, 0.000000000000000000, -0.000000000000000000 ) ) ;
#29252=PLANE ( 'NONE',  #27857 ) ;
#29253=CARTESIAN_POINT ( 'NONE',  ( -10.00000000000000000, 0.000000000000000000, 0.000000000000000000 ) ) ;
#29269=ORIENTED_EDGE ( 'NONE', *, *, #24835, .T. ) ;
#29272=CARTESIAN_POINT ( 'NONE',  ( 3.249999999999999556, -6.772677083992345359, -5.538577986808975062 ) ) ;
#29278=CARTESIAN_POINT ( 'NONE',  ( 2.274274201627289216, 9.680994141364161365, 5.222868219167314585 ) ) ;
#29280=CARTESIAN_POINT ( 'NONE',  ( 0.7632845268451443621, 5.538577986791731078, -6.772677083973650092 ) ) ;
#29285=LINE ( 'NONE', #17200, #26273 ) ;
#29286=CARTESIAN_POINT ( 'NONE',  ( 0.000000000000000000, -7.958834565716711218, -7.593217523260666901 ) ) ;
#29288=ORIENTED_EDGE ( 'NONE', *, *, #22169, .T. ) ;
#29296=CARTESIAN_POINT ( 'NONE',  ( -7.000050800000000351, 7.347880794884120722E-16, 6.000000000000000888 ) ) ;
#29298=DESIGN_CONTEXT ( 'detailed design', #15890, 'design' ) ;
#29302=CARTESIAN_POINT ( 'NONE',  ( 3.250000000000001332, 0.000000000000000000, 0.000000000000000000 ) ) ;
#29317=ORIENTED_EDGE ( 'NONE', *, *, #29431, .F. ) ;
#29332=CARTESIAN_POINT ( 'NONE',  ( 0.7632845268398871230, 0.000000000000000000, 0.000000000000000000 ) ) ;
#29335=CARTESIAN_POINT ( 'NONE',  ( 0.04279322307214343535, 9.518551034997546623, 5.235773223809417232 ) ) ;
#29344=CIRCLE ( 'NONE', #1055, 4.000000000000001776 ) ;
#29346=CARTESIAN_POINT ( 'NONE',  ( 0.000000000000000000, 0.000000000000000000, 0.000000000000000000 ) ) ;
#29348=VERTEX_POINT ( 'NONE', #19975 ) ;
#29351=AXIS2_PLACEMENT_3D ( 'NONE', #19645, #13932, #11770 ) ;
#29352=VERTEX_POINT ( 'NONE', #17288 ) ;
#29367=CARTESIAN_POINT ( 'NONE',  ( 2.589203020517539144, -5.222514179739437878, -8.895471158038722237 ) ) ;
#29379=CYLINDRICAL_SURFACE ( 'NONE', #8651, 4.000000000000001776 ) ;
#29380=CARTESIAN_POINT ( 'NONE',  ( 2.274274201625327230, -9.915734732513254102, 4.762163868918234400 ) ) ;
#29386=ORIENTED_EDGE ( 'NONE', *, *, #5346, .F. ) ;
#29391=EDGE_CURVE ( 'NONE', #8063, #681, #24450, .T. ) ;
#29395=ORIENTED_EDGE ( 'NONE', *, *, #20606, .F. ) ;
#29399=ORIENTED_EDGE ( 'NONE', *, *, #19584, .T. ) ;
#29409=CARTESIAN_POINT ( 'NONE',  ( 0.3749743548326617271, -0.8908839545093775181, -10.05686762493553310 ) ) ;
#29410=CARTESIAN_POINT ( 'NONE',  ( 2.795120610031291530, 9.728666380680506265, -0.7443816538168457342 ) ) ;
#29414=DIRECTION ( 'NONE',  ( 0.000000000000000000, 0.000000000000000000, 1.000000000000000000 ) ) ;
#29425=VECTOR ( 'NONE', #11542, 1000.000000000000000 ) ;
#29426=VECTOR ( 'NONE', #21848, 1000.000000000000000 ) ;
#29427=CYLINDRICAL_SURFACE ( 'NONE', #23028, 4.000000000000001776 ) ;
#29428=VECTOR ( 'NONE', #19844, 1000.000000000000000 ) ;
#29431=EDGE_CURVE ( 'NONE', #14007, #4750, #640, .T. ) ;
#29436=CARTESIAN_POINT ( 'NONE',  ( 0.000000000000000000, -9.314797388894900720, 1.239665997526854468 ) ) ;
#29439=DIRECTION ( 'NONE',  ( -1.000000000000000000, -0.000000000000000000, -0.000000000000000000 ) ) ;
#29440=DIRECTION ( 'NONE',  ( -1.000000000000000000, -0.000000000000000000, -0.000000000000000000 ) ) ;
#29444=CARTESIAN_POINT ( 'NONE',  ( -18.30155664144426453, 4.770368330595423290E-16, 3.895301350492843540 ) ) ;
#29449=CYLINDRICAL_SURFACE ( 'NONE', #24042, 3.499999999999999556 ) ;
#29451=B_SPLINE_CURVE_WITH_KNOTS ( 'NONE', 3,
 ( #3693, #20759, #23414, #521, #20921, #31141, #8226, #18426 ),
 .UNSPECIFIED., .F., .F.,
 ( 4, 2, 2, 4 ),
 ( 2.737843117451997097E-07, 0.001228034957219390367, 0.001841915543673211444, 0.002455796130127031220 ),
 .UNSPECIFIED. ) ;
#29455=VERTEX_POINT ( 'NONE', #23129 ) ;
#29466=DIRECTION ( 'NONE',  ( 0.000000000000000000, 0.000000000000000000, 1.000000000000000000 ) ) ;
#29484=EDGE_CURVE ( 'NONE', #6718, #17929, #25806, .T. ) ;
#29485=AXIS2_PLACEMENT_3D ( 'NONE', #10393, #30809, #7877 ) ;
#29486=CARTESIAN_POINT ( 'NONE',  ( 2.274274201625327230, -7.593217523260523016, -7.958834565716851550 ) ) ;
#29497=CIRCLE ( 'NONE', #24690, 10.94895958125474245 ) ;
#29504=CIRCLE ( 'NONE', #18844, 8.749000000000002331 ) ;
#29512=CARTESIAN_POINT ( 'NONE',  ( 2.592584712403274150, 2.232024585009849016, -10.08167743097170543 ) ) ;
#29513=CIRCLE ( 'NONE', #11897, 4.000000000000001776 ) ;
#29523=AXIS2_PLACEMENT_3D ( 'NONE', #24236, #11858, #17205 ) ;
#29524=EDGE_CURVE ( 'NONE', #29226, #9973, #26272, .T. ) ;
#29527=CARTESIAN_POINT ( 'NONE',  ( 0.000000000000000000, 0.000000000000000000, 0.000000000000000000 ) ) ;
#29533=ORIENTED_EDGE ( 'NONE', *, *, #25358, .F. ) ;
#29537=DIRECTION ( 'NONE',  ( 0.000000000000000000, 0.000000000000000000, 1.000000000000000000 ) ) ;
#29543=ORIENTED_EDGE ( 'NONE', *, *, #1809, .T. ) ;
#29546=CARTESIAN_POINT ( 'NONE',  ( -1.433134780067091442E-16, -9.620177616658022401, 5.227991826304056566 ) ) ;
#29554=CARTESIAN_POINT ( 'NONE',  ( 0.7632845268398871230, 0.000000000000000000, 0.000000000000000000 ) ) ;
#29556=AXIS2_PLACEMENT_3D ( 'NONE', #21672, #32384, #31879 ) ;
#29559=VECTOR ( 'NONE', #4696, 1000.000000000000000 ) ;
#29569=CARTESIAN_POINT ( 'NONE',  ( 0.000000000000000000, 10.85582367538894211, 1.425064293572374963 ) ) ;
#29573=FACE_OUTER_BOUND ( 'NONE', #32070, .T. ) ;
#29576=ORIENTED_EDGE ( 'NONE', *, *, #6084, .T. ) ;
#29584=CYLINDRICAL_SURFACE ( 'NONE', #24718, 4.000000000000001776 ) ;
#29595=EDGE_CURVE ( 'NONE', #11257, #19641, #6059, .T. ) ;
#29602=FACE_OUTER_BOUND ( 'NONE', #31033, .T. ) ;
#29619=CARTESIAN_POINT ( 'NONE',  ( 5.084999606894402593E-16, -5.227991826304019263, -9.620177616658041941 ) ) ;
#29621=DIRECTION ( 'NONE',  ( -1.000000000000000000, 0.000000000000000000, -0.000000000000000000 ) ) ;
#29622=ORIENTED_EDGE ( 'NONE', *, *, #29484, .F. ) ;
#29631=ORIENTED_EDGE ( 'NONE', *, *, #29842, .F. ) ;
#29632=DIRECTION ( 'NONE',  ( -1.000000000000000000, 0.000000000000000000, 0.000000000000000000 ) ) ;
#29634=CARTESIAN_POINT ( 'NONE',  ( 2.274274201625327230, -10.90201369670499609, 1.464956435139503022 ) ) ;
#29639=EDGE_CURVE ( 'NONE', #10525, #7224, #21120, .T. ) ;
#29643=EDGE_LOOP ( 'NONE', ( #20331, #25859, #18163, #20625 ) ) ;
#29646=CARTESIAN_POINT ( 'NONE',  ( -1.348815490713419493E-16, -7.533794289458111137, 7.944914065997086716 ) ) ;
#29650=VERTEX_POINT ( 'NONE', #28959 ) ;
#29653=CARTESIAN_POINT ( 'NONE',  ( 0.7632845268451400322, 6.772677083973724699, 5.538577986791671570 ) ) ;
#29658=DIRECTION ( 'NONE',  ( 0.000000000000000000, 0.000000000000000000, -1.000000000000000000 ) ) ;
#29660=CARTESIAN_POINT ( 'NONE',  ( 2.857988133323936530, -6.150950518044163928, -7.318787950819745092 ) ) ;
#29664=FACE_OUTER_BOUND ( 'NONE', #5408, .T. ) ;
#29672=DIRECTION ( 'NONE',  ( -1.000000000000000000, -0.000000000000000000, 0.000000000000000000 ) ) ;
#29686=CARTESIAN_POINT ( 'NONE',  ( 2.440333830126093950, 5.258796312403019257, -9.290196408095376057 ) ) ;
#29692=CARTESIAN_POINT ( 'NONE',  ( 2.274274201625327230, 0.000000000000000000, 0.000000000000000000 ) ) ;
#29699=DIRECTION ( 'NONE',  ( 0.000000000000000000, -1.598721155460225418E-14, 1.000000000000000000 ) ) ;
#29700=CARTESIAN_POINT ( 'NONE',  ( 0.7632845268398876781, -8.734705317681624948, 0.4999240074894106822 ) ) ;
#29701=ORIENTED_EDGE ( 'NONE', *, *, #15698, .F. ) ;
#29709=VERTEX_POINT ( 'NONE', #725 ) ;
#29711=ADVANCED_FACE ( 'NONE', ( #31806 ), #8877, .F. ) ;
#29724=ORIENTED_EDGE ( 'NONE', *, *, #16435, .T. ) ;
#29729=DIRECTION ( 'NONE',  ( 0.000000000000000000, 0.000000000000000000, -1.000000000000000000 ) ) ;
#29734=VERTEX_POINT ( 'NONE', #22723 ) ;
#29744=EDGE_CURVE ( 'NONE', #4178, #11832, #25390, .T. ) ;
#29757=DIRECTION ( 'NONE',  ( 0.000000000000000000, 0.000000000000000000, 1.000000000000000000 ) ) ;
#29761=DIRECTION ( 'NONE',  ( 1.000000000000000000, -0.000000000000000000, -0.000000000000000000 ) ) ;
#29772=CYLINDRICAL_SURFACE ( 'NONE', #27407, 4.000000000000001776 ) ;
#29784=LINE ( 'NONE', #6860, #6914 ) ;
#29789=ORIENTED_EDGE ( 'NONE', *, *, #29999, .F. ) ;
#29792=VERTEX_POINT ( 'NONE', #7326 ) ;
#29812=DIRECTION ( 'NONE',  ( 0.000000000000000000, 0.000000000000000000, 1.000000000000000000 ) ) ;
#29819=ADVANCED_FACE ( 'NONE', ( #27891 ), #13163, .T. ) ;
#29825=B_SPLINE_CURVE_WITH_KNOTS ( 'NONE', 3,
 ( #18330, #600, #28538, #31222, #18492, #3050, #214, #17561 ),
 .UNSPECIFIED., .F., .F.,
 ( 4, 2, 2, 4 ),
 ( 5.099451029798974806E-07, 0.001229190215600040655, 0.001843530350848571675, 0.002457870486097102694 ),
 .UNSPECIFIED. ) ;
#29826=ORIENTED_EDGE ( 'NONE', *, *, #18528, .F. ) ;
#29827=CYLINDRICAL_SURFACE ( 'NONE', #22548, 4.000000000000001776 ) ;
#29833=ORIENTED_EDGE ( 'NONE', *, *, #7417, .T. ) ;
#29839=DIRECTION ( 'NONE',  ( 0.000000000000000000, 0.000000000000000000, -1.000000000000000000 ) ) ;
#29842=EDGE_CURVE ( 'NONE', #12277, #32002, #14081, .T. ) ;
#29843=CYLINDRICAL_SURFACE ( 'NONE', #17122, 4.000000000000001776 ) ;
#29847=DIRECTION ( 'NONE',  ( 0.000000000000000000, 0.000000000000000000, -1.000000000000000000 ) ) ;
#29859=ORIENTED_EDGE ( 'NONE', *, *, #26877, .T. ) ;
#29866=CARTESIAN_POINT ( 'NONE',  ( 3.249999999999999556, 9.241976615262133876, 1.699438267350532161 ) ) ;
#29869=DIRECTION ( 'NONE',  ( -1.000000000000000000, -0.000000000000000000, -0.000000000000000000 ) ) ;
#29870=B_SPLINE_CURVE_WITH_KNOTS ( 'NONE', 3,
 ( #30935, #8011, #192, #25923 ),
 .UNSPECIFIED., .F., .F.,
 ( 4, 4 ),
 ( 0.002129256371650449509, 0.002522096907598464846 ),
 .UNSPECIFIED. ) ;
#29881=LINE ( 'NONE', #9133, #29426 ) ;
#29882=CARTESIAN_POINT ( 'NONE',  ( 2.970200448039778784, -8.521880193013323890, 3.362738345035466647 ) ) ;
#29892=EDGE_CURVE ( 'NONE', #30559, #1994, #3726, .T. ) ;
#29900=CYLINDRICAL_SURFACE ( 'NONE', #16730, 4.000000000000000888 ) ;
#29912=FACE_OUTER_BOUND ( 'NONE', #22253, .T. ) ;
#29923=VERTEX_POINT ( 'NONE', #2838 ) ;
#29937=CARTESIAN_POINT ( 'NONE',  ( 0.1606233661178074201, 7.854816391752183158, 7.161985370896712055 ) ) ;
#29939=AXIS2_PLACEMENT_3D ( 'NONE', #22512, #30054, #22696 ) ;
#29944=CARTESIAN_POINT ( 'NONE',  ( 2.976845970491568405, 5.822399416825399854, -7.079702685456805256 ) ) ;
#29945=ORIENTED_EDGE ( 'NONE', *, *, #29987, .T. ) ;
#29951=B_SPLINE_CURVE_WITH_KNOTS ( 'NONE', 3,
 ( #18547, #26566, #31275, #8350, #28737, #16011, #30088, #26901 ),
 .UNSPECIFIED., .F., .F.,
 ( 4, 2, 2, 4 ),
 ( 5.099451029790481183E-07, 0.001229189590448580760, 0.001843529413121383674, 0.002457869235794186806 ),
 .UNSPECIFIED. ) ;
#29955=CARTESIAN_POINT ( 'NONE',  ( 3.063284526839887167, -7.360373001730951437, 4.729683950898845524 ) ) ;
#29960=EDGE_LOOP ( 'NONE', ( #8580, #4380, #23074, #18174 ) ) ;
#29967=CARTESIAN_POINT ( 'NONE',  ( 0.7632845268398871230, 0.000000000000000000, 0.000000000000000000 ) ) ;
#29972=EDGE_CURVE ( 'NONE', #8056, #27353, #18512, .T. ) ;
#29984=AXIS2_PLACEMENT_3D ( 'NONE', #19959, #12082, #4725 ) ;
#29987=EDGE_CURVE ( 'NONE', #32838, #29709, #25352, .T. ) ;
#29999=EDGE_CURVE ( 'NONE', #11786, #16905, #8641, .T. ) ;
#30002=EDGE_LOOP ( 'NONE', ( #15797, #9200, #4953, #30942, #20207, #15894 ) ) ;
#30003=CARTESIAN_POINT ( 'NONE',  ( 0.08034252392848015289, -2.072171912280144301, 10.58792409793185207 ) ) ;
#30012=DIRECTION ( 'NONE',  ( 0.000000000000000000, 0.000000000000000000, 1.000000000000000000 ) ) ;
#30025=LINE ( 'NONE', #4453, #30543 ) ;
#30034=VECTOR ( 'NONE', #2919, 1000.000000000000000 ) ;
#30040=EDGE_CURVE ( 'NONE', #10723, #979, #27888, .T. ) ;
#30041=AXIS2_PLACEMENT_3D ( 'NONE', #18873, #655, #1141 ) ;
#30054=DIRECTION ( 'NONE',  ( -1.000000000000000000, -0.000000000000000000, -0.000000000000000000 ) ) ;
#30062=AXIS2_PLACEMENT_3D ( 'NONE', #19306, #18988, #26825 ) ;
#30068=CARTESIAN_POINT ( 'NONE',  ( 0.5032039692148381205, 0.7352278974742033624, -9.704418393831362621 ) ) ;
#30071=AXIS2_PLACEMENT_3D ( 'NONE', #29227, #6166, #29081 ) ;
#30088=CARTESIAN_POINT ( 'NONE',  ( 0.7212197595511946613, -8.936767016217507020, -0.5238431420100763125 ) ) ;
#30092=ADVANCED_FACE ( 'NONE', ( #15300 ), #25503, .T. ) ;
#30105=LINE ( 'NONE', #12340, #27861 ) ;
#30121=ORIENTED_EDGE ( 'NONE', *, *, #6327, .T. ) ;
#30125=DIRECTION ( 'NONE',  ( -1.000000000000000000, 0.000000000000000000, -0.000000000000000000 ) ) ;
#30133=LINE ( 'NONE', #25574, #29559 ) ;
#30136=ORIENTED_EDGE ( 'NONE', *, *, #18186, .T. ) ;
#30143=ORIENTED_EDGE ( 'NONE', *, *, #31997, .T. ) ;
#30153=ORIENTED_EDGE ( 'NONE', *, *, #2829, .F. ) ;
#30159=CARTESIAN_POINT ( 'NONE',  ( 2.357329994281668117, 10.64078702437731749, -2.053141773251354163 ) ) ;
#30161=ORIENTED_EDGE ( 'NONE', *, *, #3348, .F. ) ;
#30169=ORIENTED_EDGE ( 'NONE', *, *, #14855, .F. ) ;
#30174=DIRECTION ( 'NONE',  ( -1.000000000000000000, 0.000000000000000000, 0.000000000000000000 ) ) ;
#30180=ORIENTED_EDGE ( 'NONE', *, *, #29484, .T. ) ;
#30187=CARTESIAN_POINT ( 'NONE',  ( 0.08034253207385326501, 9.783802610460172744, -4.547003328335167183 ) ) ;
#30191=DIRECTION ( 'NONE',  ( 0.000000000000000000, 0.000000000000000000, 1.000000000000000000 ) ) ;
#30207=CARTESIAN_POINT ( 'NONE',  ( 0.6791198108364597807, 3.345077512921651675, 8.522429291907608118 ) ) ;
#30218=ADVANCED_FACE ( 'NONE', ( #13610 ), #32355, .F. ) ;
#30227=ADVANCED_FACE ( 'NONE', ( #24963 ), #29827, .T. ) ;
#30241=VERTEX_POINT ( 'NONE', #32852 ) ;
#30243=ORIENTED_EDGE ( 'NONE', *, *, #20393, .F. ) ;
#30249=ORIENTED_EDGE ( 'NONE', *, *, #10067, .T. ) ;
#30254=EDGE_CURVE ( 'NONE', #15147, #14743, #11321, .T. ) ;
#30258=CARTESIAN_POINT ( 'NONE',  ( 0.1606233164486133569, 9.238724727304104434, -5.257199111574238692 ) ) ;
#30263=DIRECTION ( 'NONE',  ( -1.000000000000000000, 0.000000000000000000, 0.000000000000000000 ) ) ;
#30270=DIRECTION ( 'NONE',  ( 1.000000000000000000, -0.000000000000000000, -0.000000000000000000 ) ) ;
#30277=DIRECTION ( 'NONE',  ( 0.000000000000000000, -9.769962616701377556E-15, 1.000000000000000000 ) ) ;
#30283=CARTESIAN_POINT ( 'NONE',  ( 0.6728002192067888965, 7.058361986476102246, 5.823680980834201826 ) ) ;
#30291=ORIENTED_EDGE ( 'NONE', *, *, #9757, .T. ) ;
#30292=CARTESIAN_POINT ( 'NONE',  ( -4.599999999999996092, 0.000000000000000000, 0.000000000000000000 ) ) ;
#30301=DIRECTION ( 'NONE',  ( 0.000000000000000000, 0.000000000000000000, -1.000000000000000000 ) ) ;
#30303=B_SPLINE_CURVE_WITH_KNOTS ( 'NONE', 3,
 ( #6352, #1197, #11394, #11549, #24072, #31626, #3700, #18929 ),
 .UNSPECIFIED., .F., .F.,
 ( 4, 2, 2, 4 ),
 ( 2.737843117464296545E-07, 0.001228034957219389283, 0.001841915543673210576, 0.002455796130127032087 ),
 .UNSPECIFIED. ) ;
#30336=ORIENTED_EDGE ( 'NONE', *, *, #2119, .T. ) ;
#30363=CARTESIAN_POINT ( 'NONE',  ( 2.661997627134203626, 7.629706518865846832, 6.664939678585187544 ) ) ;
#30368=FACE_OUTER_BOUND ( 'NONE', #31593, .T. ) ;
#30371=EDGE_LOOP ( 'NONE', ( #94, #32627, #17414, #30586 ) ) ;
#30373=CARTESIAN_POINT ( 'NONE',  ( 0.7632845268398871230, -8.152713396088739017, -3.174628368996162298 ) ) ;
#30375=DIRECTION ( 'NONE',  ( 1.000000000000000000, -0.000000000000000000, -0.000000000000000000 ) ) ;
#30379=VERTEX_POINT ( 'NONE', #20472 ) ;
#30383=CARTESIAN_POINT ( 'NONE',  ( 0.5640491561247281682, 0.6680154998105966024, -9.516580665849634357 ) ) ;
#30395=EDGE_CURVE ( 'NONE', #28862, #4581, #20876, .T. ) ;
#30410=VERTEX_POINT ( 'NONE', #18100 ) ;
#30411=CARTESIAN_POINT ( 'NONE',  ( 0.000000000000000000, 1.975651141462391402, -10.82112760146734054 ) ) ;
#30416=VERTEX_POINT ( 'NONE', #23296 ) ;
#30420=EDGE_CURVE ( 'NONE', #26576, #29348, #9716, .T. ) ;
#30430=EDGE_CURVE ( 'NONE', #15369, #29650, #15914, .T. ) ;
#30437=ORIENTED_EDGE ( 'NONE', *, *, #1883, .T. ) ;
#30438=EDGE_CURVE ( 'NONE', #3978, #27203, #8401, .T. ) ;
#30439=CARTESIAN_POINT ( 'NONE',  ( 0.2582728410551998199, -8.984109560031233954, 5.239665997526856245 ) ) ;
#30441=AXIS2_PLACEMENT_3D ( 'NONE', #14916, #10076, #20288 ) ;
#30446=TOROIDAL_SURFACE ( 'NONE', #1607, 3.895301350492843540, 15.00000000000000178 ) ;
#30460=DIRECTION ( 'NONE',  ( 0.000000000000000000, 0.000000000000000000, -1.000000000000000000 ) ) ;
#30462=CARTESIAN_POINT ( 'NONE',  ( 2.976845726615124921, 8.871766062375177953, -2.305279507610514145 ) ) ;
#30471=ADVANCED_FACE ( 'NONE', ( #21431 ), #13879, .T. ) ;
#30474=CARTESIAN_POINT ( 'NONE',  ( 0.000000000000000000, -9.620177616657944242, -5.227991826304196010 ) ) ;
#30490=AXIS2_PLACEMENT_3D ( 'NONE', #4884, #15065, #2910 ) ;
#30499=ORIENTED_EDGE ( 'NONE', *, *, #19635, .F. ) ;
#30501=VERTEX_POINT ( 'NONE', #29280 ) ;
#30502=CARTESIAN_POINT ( 'NONE',  ( 0.5704036742842228946, 8.851103337321323039, -3.563415854978401853 ) ) ;
#30506=ORIENTED_EDGE ( 'NONE', *, *, #27126, .T. ) ;
#30509=CYLINDRICAL_SURFACE ( 'NONE', #6940, 4.000000000000001776 ) ;
#30513=AXIS2_PLACEMENT_3D ( 'NONE', #15968, #3958, #8938 ) ;
#30518=AXIS2_PLACEMENT_3D ( 'NONE', #3655, #13811, #24017 ) ;
#30532=ORIENTED_EDGE ( 'NONE', *, *, #15698, .T. ) ;
#30543=VECTOR ( 'NONE', #11970, 1000.000000000000000 ) ;
#30544=AXIS2_PLACEMENT_3D ( 'NONE', #11576, #1238, #32160 ) ;
#30549=AXIS2_PLACEMENT_3D ( 'NONE', #9544, #17421, #12394 ) ;
#30552=AXIS2_PLACEMENT_3D ( 'NONE', #864, #5845, #26736 ) ;
#30557=VECTOR ( 'NONE', #8725, 1000.000000000000000 ) ;
#30559=VERTEX_POINT ( 'NONE', #3891 ) ;
#30570=AXIS2_PLACEMENT_3D ( 'NONE', #27338, #6775, #22674 ) ;
#30585=CARTESIAN_POINT ( 'NONE',  ( 3.249999999999999556, -0.4999240074893822605, -8.734705317681632053 ) ) ;
#30586=ORIENTED_EDGE ( 'NONE', *, *, #22518, .T. ) ;
#30593=CARTESIAN_POINT ( 'NONE',  ( 0.3045634635876931506, -10.03290811084029954, -2.226307684702790723 ) ) ;
#30596=ORIENTED_EDGE ( 'NONE', *, *, #25623, .F. ) ;
#30599=DIRECTION ( 'NONE',  ( -1.000000000000000000, 0.000000000000000000, 0.000000000000000000 ) ) ;
#30614=AXIS2_PLACEMENT_3D ( 'NONE', #17250, #9885, #26952 ) ;
#30616=CARTESIAN_POINT ( 'NONE',  ( 2.274274201625327230, -10.82112760146734765, -1.975651141462354543 ) ) ;
#30617=EDGE_CURVE ( 'NONE', #17653, #12775, #4388, .T. ) ;
#30621=CIRCLE ( 'NONE', #12983, 8.749000000000002331 ) ;
#30622=CARTESIAN_POINT ( 'NONE',  ( 3.063284526839887167, 4.729683950898978750, -7.360373001730866171 ) ) ;
#30633=EDGE_CURVE ( 'NONE', #3483, #31221, #31645, .T. ) ;
#30650=CARTESIAN_POINT ( 'NONE',  ( 1.624999999999999778, 1.975651141462390070, -10.82112760146734232 ) ) ;
#30651=EDGE_LOOP ( 'NONE', ( #17325, #11481, #24293, #9028 ) ) ;
#30663=CARTESIAN_POINT ( 'NONE',  ( -8.049676575031998738, 0.000000000000000000, -6.923700951379997193 ) ) ;
#30676=VERTEX_POINT ( 'NONE', #22602 ) ;
#30685=CARTESIAN_POINT ( 'NONE',  ( 0.1574692293613783600, -4.391622967207749362, -9.672096048330562468 ) ) ;
#30690=EDGE_LOOP ( 'NONE', ( #11679, #16005, #22644, #13758, #29859 ) ) ;
#30707=EDGE_CURVE ( 'NONE', #30379, #689, #6547, .T. ) ;
#30718=LINE ( 'NONE', #20988, #10343 ) ;
#30721=CARTESIAN_POINT ( 'NONE',  ( 2.274274201625327230, 7.958834565716768061, 7.593217523260608282 ) ) ;
#30722=ADVANCED_FACE ( 'NONE', ( #16751 ), #24772, .T. ) ;
#30725=DIRECTION ( 'NONE',  ( -1.000000000000000000, 0.000000000000000000, 0.000000000000000000 ) ) ;
#30733=DIRECTION ( 'NONE',  ( -1.000000000000000000, -0.000000000000000000, -0.000000000000000000 ) ) ;
#30739=DIRECTION ( 'NONE',  ( -1.000000000000000000, 0.000000000000000000, 0.000000000000000000 ) ) ;
#30740=EDGE_LOOP ( 'NONE', ( #8766, #14326, #18536, #6445 ) ) ;
#30745=ADVANCED_FACE ( 'NONE', ( #19747 ), #32814, .F. ) ;
#30749=CARTESIAN_POINT ( 'NONE',  ( 0.000000000000000000, 1.999317321091499400, 10.76487093102065451 ) ) ;
#30755=FACE_OUTER_BOUND ( 'NONE', #25586, .T. ) ;
#30757=ORIENTED_EDGE ( 'NONE', *, *, #851, .F. ) ;
#30760=EDGE_CURVE ( 'NONE', #17637, #3652, #19270, .T. ) ;
#30762=CARTESIAN_POINT ( 'NONE',  ( 0.5032040285356975673, 9.002252291012739605, 3.698073368192989818 ) ) ;
#30767=CARTESIAN_POINT ( 'NONE',  ( 0.08034252392847902879, -10.58792409793185030, -2.072171912280182493 ) ) ;
#30769=EDGE_LOOP ( 'NONE', ( #26578, #18439, #21420, #25119 ) ) ;
#30771=CYLINDRICAL_SURFACE ( 'NONE', #1127, 4.000000000000001776 ) ;
#30786=LINE ( 'NONE', #26711, #23115 ) ;
#30788=CARTESIAN_POINT ( 'NONE',  ( 2.274274201625315239, -10.82112760146740449, 1.975651141462185789 ) ) ;
#30789=B_SPLINE_CURVE_WITH_KNOTS ( 'NONE', 3,
 ( #10377, #20239, #20585, #352, #22903, #25423, #2377, #30793 ),
 .UNSPECIFIED., .F., .F.,
 ( 4, 2, 2, 4 ),
 ( 2.197717257069985215E-07, 0.001262070444977237251, 0.001892995781603003420, 0.002523921118228769373 ),
 .UNSPECIFIED. ) ;
#30790=DIRECTION ( 'NONE',  ( 0.000000000000000000, 0.000000000000000000, 1.000000000000000000 ) ) ;
#30793=CARTESIAN_POINT ( 'NONE',  ( 3.063284526839887167, 6.772677083992467928, -5.538577986808824960 ) ) ;
#30798=VERTEX_POINT ( 'NONE', #12707 ) ;
#30809=DIRECTION ( 'NONE',  ( -1.000000000000000000, -0.000000000000000000, 0.000000000000000000 ) ) ;
#30816=DIRECTION ( 'NONE',  ( -1.000000000000000000, -0.000000000000000000, -0.000000000000000000 ) ) ;
#30821=CARTESIAN_POINT ( 'NONE',  ( 2.785385763235068701, 9.518934100285017408, 2.300561732649628155 ) ) ;
#30833=ORIENTED_EDGE ( 'NONE', *, *, #12017, .T. ) ;
#30841=CARTESIAN_POINT ( 'NONE',  ( 2.864530875629067275, 0.6595692664038855790, -9.539603485476124689 ) ) ;
#30846=EDGE_CURVE ( 'NONE', #1971, #30410, #2836, .T. ) ;
#30863=ADVANCED_FACE ( 'NONE', ( #15875 ), #31432, .T. ) ;
#30872=CYLINDRICAL_SURFACE ( 'NONE', #25607, 11.00000000000000000 ) ;
#30878=ORIENTED_EDGE ( 'NONE', *, *, #9062, .F. ) ;
#30881=EDGE_CURVE ( 'NONE', #19151, #28496, #17663, .T. ) ;
#30888=DIRECTION ( 'NONE',  ( 1.000000000000000000, 0.000000000000000000, 0.000000000000000000 ) ) ;
#30889=CARTESIAN_POINT ( 'NONE',  ( 0.5032039771612139001, 9.456648240374295966, -2.299586922890421103 ) ) ;
#30894=DIRECTION ( 'NONE',  ( 0.000000000000000000, 0.000000000000000000, 1.000000000000000000 ) ) ;
#30902=ORIENTED_EDGE ( 'NONE', *, *, #25516, .T. ) ;
#30916=FACE_OUTER_BOUND ( 'NONE', #11433, .T. ) ;
#30935=CARTESIAN_POINT ( 'NONE',  ( 2.425585535379221280, -9.314797388879910045, 5.239665997526856245 ) ) ;
#30941=DIRECTION ( 'NONE',  ( -1.000000000000000000, -0.000000000000000000, -0.000000000000000000 ) ) ;
#30942=ORIENTED_EDGE ( 'NONE', *, *, #4041, .F. ) ;
#30943=CARTESIAN_POINT ( 'NONE',  ( 0.000000000000000000, 0.000000000000000000, 0.000000000000000000 ) ) ;
#30954=DIRECTION ( 'NONE',  ( -1.000000000000000000, 0.000000000000000000, 0.000000000000000000 ) ) ;
#30961=EDGE_CURVE ( 'NONE', #7524, #24271, #21498, .T. ) ;
#30969=AXIS2_PLACEMENT_3D ( 'NONE', #10367, #25567, #27921 ) ;
#30974=AXIS2_PLACEMENT_3D ( 'NONE', #29444, #6709, #16899 ) ;
#30978=CYLINDRICAL_SURFACE ( 'NONE', #1807, 11.00000000000000000 ) ;
#30986=DIRECTION ( 'NONE',  ( 0.000000000000000000, 0.000000000000000000, 1.000000000000000000 ) ) ;
#30995=ORIENTED_EDGE ( 'NONE', *, *, #17718, .T. ) ;
#31004=DIRECTION ( 'NONE',  ( 0.000000000000000000, 0.000000000000000000, -1.000000000000000000 ) ) ;
#31008=FACE_OUTER_BOUND ( 'NONE', #22143, .T. ) ;
#31011=CARTESIAN_POINT ( 'NONE',  ( 0.000000000000000000, -1.239665997526818053, -9.314797388894906049 ) ) ;
#31024=DIRECTION ( 'NONE',  ( 0.000000000000000000, 0.000000000000000000, -1.000000000000000000 ) ) ;
#31033=EDGE_LOOP ( 'NONE', ( #22442, #28723, #11101, #27835, #22950 ) ) ;
#31042=DIRECTION ( 'NONE',  ( 1.000000000000000000, 0.000000000000000000, 0.000000000000000000 ) ) ;
#31045=AXIS2_PLACEMENT_3D ( 'NONE', #15619, #13411, #16726 ) ;
#31059=EDGE_CURVE ( 'NONE', #32897, #2837, #9745, .T. ) ;
#31062=DIRECTION ( 'NONE',  ( -1.000000000000000000, 0.000000000000000000, 0.000000000000000000 ) ) ;
#31069=B_SPLINE_CURVE_WITH_KNOTS ( 'NONE', 3,
 ( #3622, #23206, #18160, #23350, #950, #23504, #11129, #16314 ),
 .UNSPECIFIED., .F., .F.,
 ( 4, 2, 2, 4 ),
 ( 5.099451029764644560E-07, 0.001229190215587238830, 0.001843530350829370671, 0.002457870486071502512 ),
 .UNSPECIFIED. ) ;
#31070=ORIENTED_EDGE ( 'NONE', *, *, #16235, .T. ) ;
#31082=EDGE_CURVE ( 'NONE', #1994, #20387, #23096, .T. ) ;
#31091=B_SPLINE_CURVE_WITH_KNOTS ( 'NONE', 3,
 ( #4599, #2085, #29512, #27000, #4251, #24633, #22157, #17110 ),
 .UNSPECIFIED., .F., .F.,
 ( 4, 2, 2, 4 ),
 ( 2.333100327429635409E-07, 0.001262083418496911602, 0.001893008472728995983, 0.002523933526961080580 ),
 .UNSPECIFIED. ) ;
#31104=EDGE_CURVE ( 'NONE', #1745, #10723, #2971, .T. ) ;
#31105=CARTESIAN_POINT ( 'NONE',  ( 0.08034253207417903220, -9.783802610459691351, 4.547003328334568550 ) ) ;
#31109=DIRECTION ( 'NONE',  ( -1.000000000000000000, 0.000000000000000000, 0.000000000000000000 ) ) ;
#31113=EDGE_LOOP ( 'NONE', ( #24953, #32389, #11037, #10620, #721 ) ) ;
#31117=CIRCLE ( 'NONE', #27345, 8.749000000000002331 ) ;
#31121=VECTOR ( 'NONE', #10561, 1000.000000000000000 ) ;
#31124=DIRECTION ( 'NONE',  ( -1.000000000000000000, 0.000000000000000000, 0.000000000000000000 ) ) ;
#31133=AXIS2_PLACEMENT_3D ( 'NONE', #10001, #28070, #15504 ) ;
#31141=CARTESIAN_POINT ( 'NONE',  ( 0.1574692421723833113, -7.841623826006576259, 7.165523657697594473 ) ) ;
#31145=CYLINDRICAL_SURFACE ( 'NONE', #31195, 4.000000000000001776 ) ;
#31166=ADVANCED_FACE ( 'NONE', ( #12823 ), #27898, .T. ) ;
#31170=EDGE_CURVE ( 'NONE', #26634, #26820, #22823, .T. ) ;
#31177=CIRCLE ( 'NONE', #21539, 8.749000000000002331 ) ;
#31182=ORIENTED_EDGE ( 'NONE', *, *, #22303, .F. ) ;
#31184=LINE ( 'NONE', #25639, #20369 ) ;
#31186=DIRECTION ( 'NONE',  ( 1.000000000000000000, 0.000000000000000000, 0.000000000000000000 ) ) ;
#31195=AXIS2_PLACEMENT_3D ( 'NONE', #8231, #5220, #23107 ) ;
#31209=DIRECTION ( 'NONE',  ( 0.000000000000000000, 0.000000000000000000, 1.000000000000000000 ) ) ;
#31221=VERTEX_POINT ( 'NONE', #28219 ) ;
#31222=CARTESIAN_POINT ( 'NONE',  ( 0.5032041927271373449, 6.298925283824191368, -7.418882907476054278 ) ) ;
#31244=DIRECTION ( 'NONE',  ( 0.000000000000000000, 0.000000000000000000, 1.000000000000000000 ) ) ;
#31256=CARTESIAN_POINT ( 'NONE',  ( 0.6791199890552586105, 5.814932665552513313, 7.071625480714526901 ) ) ;
#31260=DIRECTION ( 'NONE',  ( -1.000000000000000000, 0.000000000000000000, 0.000000000000000000 ) ) ;
#31261=VERTEX_POINT ( 'NONE', #16443 ) ;
#31275=CARTESIAN_POINT ( 'NONE',  ( 0.3076688720830436652, -10.24120291391357895, -0.9727984658976240873 ) ) ;
#31278=CARTESIAN_POINT ( 'NONE',  ( 3.020080204145390468, -7.542713057966098589, -4.831795131253294073 ) ) ;
#31286=VERTEX_POINT ( 'NONE', #14115 ) ;
#31313=DIRECTION ( 'NONE',  ( 1.000000000000000000, 0.000000000000000000, 0.000000000000000000 ) ) ;
#31325=ORIENTED_EDGE ( 'NONE', *, *, #32540, .F. ) ;
#31334=CARTESIAN_POINT ( 'NONE',  ( -10.00000000000000000, 0.000000000000000000, 0.000000000000000000 ) ) ;
#31346=EDGE_CURVE ( 'NONE', #25565, #29734, #4359, .T. ) ;
#31355=VERTEX_POINT ( 'NONE', #19638 ) ;
#31361=VERTEX_POINT ( 'NONE', #7409 ) ;
#31370=CARTESIAN_POINT ( 'NONE',  ( 0.000000000000000000, 0.000000000000000000, 0.000000000000000000 ) ) ;
#31375=CYLINDRICAL_SURFACE ( 'NONE', #14993, 4.000000000000001776 ) ;
#31402=CARTESIAN_POINT ( 'NONE',  ( 2.661997627134198741, -7.629706518865811304, -6.664939678585263927 ) ) ;
#31404=DIRECTION ( 'NONE',  ( -1.000000000000000000, 0.000000000000000000, 0.000000000000000000 ) ) ;
#31412=CARTESIAN_POINT ( 'NONE',  ( 3.249999999999999556, -4.057423117305330784, -8.475820894093018865 ) ) ;
#31416=EDGE_CURVE ( 'NONE', #11749, #7524, #18458, .T. ) ;
#31418=CARTESIAN_POINT ( 'NONE',  ( 0.000000000000000000, -9.884132761439094139, 4.709950686174575907 ) ) ;
#31422=CYLINDRICAL_SURFACE ( 'NONE', #11916, 4.000000000000001776 ) ;
#31432=CYLINDRICAL_SURFACE ( 'NONE', #32726, 8.749000000000002331 ) ;
#31435=VERTEX_POINT ( 'NONE', #12600 ) ;
#31445=CARTESIAN_POINT ( 'NONE',  ( 3.063284526839890720, 6.772677083992379110, 5.538577986808916442 ) ) ;
#31452=EDGE_CURVE ( 'NONE', #25735, #8635, #26785, .T. ) ;
#31468=ORIENTED_EDGE ( 'NONE', *, *, #9492, .T. ) ;
#31473=FACE_OUTER_BOUND ( 'NONE', #21088, .T. ) ;
#31475=DIRECTION ( 'NONE',  ( 0.000000000000000000, 0.000000000000000000, 1.000000000000000000 ) ) ;
#31486=CIRCLE ( 'NONE', #33087, 10.99999999999999822 ) ;
#31495=FACE_OUTER_BOUND ( 'NONE', #22293, .T. ) ;
#31501=ORIENTED_EDGE ( 'NONE', *, *, #2032, .T. ) ;
#31509=EDGE_LOOP ( 'NONE', ( #21955, #25363, #11360, #13767, #4911 ) ) ;
#31519=PLANE ( 'NONE',  #26309 ) ;
#31528=FACE_OUTER_BOUND ( 'NONE', #32434, .T. ) ;
#31529=AXIS2_PLACEMENT_3D ( 'NONE', #11851, #22062, #32281 ) ;
#31539=ORIENTED_EDGE ( 'NONE', *, *, #32319, .T. ) ;
#31543=CARTESIAN_POINT ( 'NONE',  ( 0.000000000000000000, -9.620177616657944242, -5.227991826304196010 ) ) ;
#31559=CARTESIAN_POINT ( 'NONE',  ( 2.976845824368062665, 4.933977349953576841, 7.725179967474386622 ) ) ;
#31561=ORIENTED_EDGE ( 'NONE', *, *, #11058, .T. ) ;
#31573=CARTESIAN_POINT ( 'NONE',  ( 0.6728001045953904136, -3.357496170320726225, 8.512517952474004446 ) ) ;
#31579=CIRCLE ( 'NONE', #5937, 4.000000000000001776 ) ;
#31590=CARTESIAN_POINT ( 'NONE',  ( 2.274274201625327230, -9.680994141368730155, -5.222868219166962866 ) ) ;
#31592=EDGE_CURVE ( 'NONE', #28679, #10493, #15026, .T. ) ;
#31593=EDGE_LOOP ( 'NONE', ( #6760, #27849, #6157, #3607, #3600 ) ) ;
#31599=ORIENTED_EDGE ( 'NONE', *, *, #29972, .T. ) ;
#31602=LINE ( 'NONE', #1173, #10728 ) ;
#31604=AXIS2_PLACEMENT_3D ( 'NONE', #4987, #12995, #28200 ) ;
#31606=CIRCLE ( 'NONE', #29984, 10.99999999999999822 ) ;
#31616=CARTESIAN_POINT ( 'NONE',  ( 0.7632845268398871230, -4.729683950898817102, -7.360373001730970977 ) ) ;
#31617=ORIENTED_EDGE ( 'NONE', *, *, #13464, .T. ) ;
#31618=AXIS2_PLACEMENT_3D ( 'NONE', #22832, #33035, #5278 ) ;
#31619=AXIS2_PLACEMENT_3D ( 'NONE', #18452, #28646, #1043 ) ;
#31626=CARTESIAN_POINT ( 'NONE',  ( 0.1574692421723846159, -7.165523657697560722, -7.841623826006603792 ) ) ;
#31632=ORIENTED_EDGE ( 'NONE', *, *, #4240, .T. ) ;
#31634=AXIS2_PLACEMENT_3D ( 'NONE', #26666, #24649, #17126 ) ;
#31638=EDGE_CURVE ( 'NONE', #30501, #26497, #7106, .T. ) ;
#31642=CARTESIAN_POINT ( 'NONE',  ( 0.000000000000000000, 7.593217523260693547, -7.958834565716684573 ) ) ;
#31645=CIRCLE ( 'NONE', #19379, 10.00000000000000355 ) ;
#31650=ORIENTED_EDGE ( 'NONE', *, *, #28299, .T. ) ;
#31656=VERTEX_POINT ( 'NONE', #6558 ) ;
#31659=CARTESIAN_POINT ( 'NONE',  ( -7.000050800000001239, 4.286263797015736102E-16, -3.499999999999999556 ) ) ;
#31668=EDGE_CURVE ( 'NONE', #2488, #9130, #9687, .T. ) ;
#31681=ORIENTED_EDGE ( 'NONE', *, *, #11617, .T. ) ;
#31682=CIRCLE ( 'NONE', #23138, 4.000000000000001776 ) ;
#31684=EDGE_CURVE ( 'NONE', #5744, #9758, #25180, .T. ) ;
#31692=CIRCLE ( 'NONE', #11925, 4.000000000000001776 ) ;
#31702=CARTESIAN_POINT ( 'NONE',  ( 0.08034252392815226240, 2.072171912279953343, -10.58792409793259992 ) ) ;
#31706=CARTESIAN_POINT ( 'NONE',  ( 0.5664946525207626982, 9.241976615239526183, 2.300561732649596181 ) ) ;
#31715=FACE_OUTER_BOUND ( 'NONE', #21482, .T. ) ;
#31719=DIRECTION ( 'NONE',  ( 0.000000000000000000, 0.000000000000000000, 1.000000000000000000 ) ) ;
#31725=ORIENTED_EDGE ( 'NONE', *, *, #18735, .F. ) ;
#31745=EDGE_CURVE ( 'NONE', #12210, #31785, #15564, .T. ) ;
#31752=CARTESIAN_POINT ( 'NONE',  ( 3.063284526839887167, -2.223716399045513992, -8.461683424509338636 ) ) ;
#31761=ORIENTED_EDGE ( 'NONE', *, *, #19665, .F. ) ;
#31764=DIRECTION ( 'NONE',  ( 0.000000000000000000, 0.000000000000000000, -1.000000000000000000 ) ) ;
#31780=DIRECTION ( 'NONE',  ( -1.000000000000000000, -0.000000000000000000, 0.000000000000000000 ) ) ;
#31784=DIRECTION ( 'NONE',  ( 0.000000000000000000, 0.000000000000000000, -1.000000000000000000 ) ) ;
#31785=VERTEX_POINT ( 'NONE', #29286 ) ;
#31787=DIRECTION ( 'NONE',  ( 0.000000000000000000, 0.000000000000000000, 1.000000000000000000 ) ) ;
#31798=CARTESIAN_POINT ( 'NONE',  ( 2.440333653313245144, -4.424884217110343521, -9.715096239900912423 ) ) ;
#31803=ORIENTED_EDGE ( 'NONE', *, *, #5679, .F. ) ;
#31806=FACE_OUTER_BOUND ( 'NONE', #13446, .T. ) ;
#31810=ORIENTED_EDGE ( 'NONE', *, *, #10780, .F. ) ;
#31828=CARTESIAN_POINT ( 'NONE',  ( 2.274274201625327230, 4.762163868918412923, -9.915734732513168836 ) ) ;
#31844=ORIENTED_EDGE ( 'NONE', *, *, #18359, .T. ) ;
#31849=CARTESIAN_POINT ( 'NONE',  ( 2.857987972556674805, -5.059832898186668260, 8.111531947321665825 ) ) ;
#31852=CARTESIAN_POINT ( 'NONE',  ( 1.624999999999999778, -9.680994141368808314, 5.222868219166822534 ) ) ;
#31869=EDGE_CURVE ( 'NONE', #11786, #22691, #10698, .T. ) ;
#31879=DIRECTION ( 'NONE',  ( 0.000000000000000000, 0.000000000000000000, 1.000000000000000000 ) ) ;
#31894=ORIENTED_EDGE ( 'NONE', *, *, #22464, .T. ) ;
#31907=ADVANCED_FACE ( 'NONE', ( #23097 ), #216, .T. ) ;
#31917=EDGE_CURVE ( 'NONE', #10741, #10253, #13064, .T. ) ;
#31918=CYLINDRICAL_SURFACE ( 'NONE', #13526, 6.999999999999998224 ) ;
#31929=ORIENTED_EDGE ( 'NONE', *, *, #20041, .T. ) ;
#31933=CARTESIAN_POINT ( 'NONE',  ( 0.5704035821694226627, -0.6538686328478068299, -9.519055809314993510 ) ) ;
#31934=CARTESIAN_POINT ( 'NONE',  ( 2.440333456259504707, 10.60697035673403654, -1.206185435486470281 ) ) ;
#31935=EDGE_CURVE ( 'NONE', #5744, #25356, #20401, .T. ) ;
#31941=ADVANCED_FACE ( 'NONE', ( #9002 ), #29252, .F. ) ;
#31946=ORIENTED_EDGE ( 'NONE', *, *, #32889, .F. ) ;
#31982=DIRECTION ( 'NONE',  ( 1.000000000000000000, -0.000000000000000000, -0.000000000000000000 ) ) ;
#31992=CARTESIAN_POINT ( 'NONE',  ( 2.357330058169011533, -7.401770933800293939, 7.915524238820718317 ) ) ;
#31997=EDGE_CURVE ( 'NONE', #6905, #32970, #19218, .T. ) ;
#32002=VERTEX_POINT ( 'NONE', #6336 ) ;
#32017=AXIS2_PLACEMENT_3D ( 'NONE', #2048, #16916, #29466 ) ;
#32025=CYLINDRICAL_SURFACE ( 'NONE', #31634, 11.00000000000000000 ) ;
#32050=DIRECTION ( 'NONE',  ( 1.000000000000000000, -0.000000000000000000, -0.000000000000000000 ) ) ;
#32051=ORIENTED_EDGE ( 'NONE', *, *, #5679, .T. ) ;
#32056=AXIS2_PLACEMENT_3D ( 'NONE', #24053, #12036, #1178 ) ;
#32063=LINE ( 'NONE', #19531, #18754 ) ;
#32070=EDGE_LOOP ( 'NONE', ( #6380, #2071, #3276, #10687 ) ) ;
#32074=CARTESIAN_POINT ( 'NONE',  ( 3.063284526839887167, 0.000000000000000000, 0.000000000000000000 ) ) ;
#32093=ORIENTED_EDGE ( 'NONE', *, *, #25415, .F. ) ;
#32094=ORIENTED_EDGE ( 'NONE', *, *, #886, .F. ) ;
#32109=VERTEX_POINT ( 'NONE', #10008 ) ;
#32114=CARTESIAN_POINT ( 'NONE',  ( 3.249999999999999556, 6.772677083992467928, -5.538577986808824960 ) ) ;
#32119=VECTOR ( 'NONE', #6410, 1000.000000000000000 ) ;
#32126=EDGE_CURVE ( 'NONE', #32283, #15594, #20943, .T. ) ;
#32129=CARTESIAN_POINT ( 'NONE',  ( 2.274274201625327230, 1.975651141462238858, 10.82112760146736896 ) ) ;
#32135=CIRCLE ( 'NONE', #111, 8.749000000000002331 ) ;
#32141=ORIENTED_EDGE ( 'NONE', *, *, #29595, .T. ) ;
#32143=VECTOR ( 'NONE', #10542, 1000.000000000000000 ) ;
#32158=CIRCLE ( 'NONE', #24748, 10.94895958125474245 ) ;
#32160=DIRECTION ( 'NONE',  ( 0.000000000000000000, 0.000000000000000000, -1.000000000000000000 ) ) ;
#32165=B_SPLINE_CURVE_WITH_KNOTS ( 'NONE', 3,
 ( #30616, #25740, #15025, #17539, #12539, #28087, #22745, #13039 ),
 .UNSPECIFIED., .F., .F.,
 ( 4, 2, 2, 4 ),
 ( 2.333100269167940293E-07, 0.001262083418509050764, 0.001893008472750115590, 0.002523933526991180634 ),
 .UNSPECIFIED. ) ;
#32167=CARTESIAN_POINT ( 'NONE',  ( 0.6791198416090081791, -7.715582677070901951, -4.928602827912293094 ) ) ;
#32168=ORIENTED_EDGE ( 'NONE', *, *, #32372, .F. ) ;
#32187=ORIENTED_EDGE ( 'NONE', *, *, #32126, .T. ) ;
#32188=ORIENTED_EDGE ( 'NONE', *, *, #461, .T. ) ;
#32191=CIRCLE ( 'NONE', #10815, 8.749000000000002331 ) ;
#32198=CARTESIAN_POINT ( 'NONE',  ( 3.249999999999999556, 5.538577986808899567, 6.772677083992407532 ) ) ;
#32202=CARTESIAN_POINT ( 'NONE',  ( 2.274274201627287884, 5.222868219167418502, -9.680994141364108074 ) ) ;
#32205=CARTESIAN_POINT ( 'NONE',  ( 0.7632845268398871230, 0.000000000000000000, 0.000000000000000000 ) ) ;
#32208=CARTESIAN_POINT ( 'NONE',  ( 0.000000000000000000, -7.533794289457995674, -7.944914065997195074 ) ) ;
#32218=CIRCLE ( 'NONE', #3392, 4.000000000000001776 ) ;
#32226=ORIENTED_EDGE ( 'NONE', *, *, #1848, .T. ) ;
#32232=LINE ( 'NONE', #4282, #27798 ) ;
#32241=CIRCLE ( 'NONE', #17198, 6.999999999999998224 ) ;
#32243=AXIS2_PLACEMENT_3D ( 'NONE', #10819, #11135, #8316 ) ;
#32248=AXIS2_PLACEMENT_3D ( 'NONE', #14035, #1865, #1675 ) ;
#32250=VERTEX_POINT ( 'NONE', #12057 ) ;
#32273=EDGE_LOOP ( 'NONE', ( #23892, #13273, #21089, #22264 ) ) ;
#32280=EDGE_CURVE ( 'NONE', #3978, #20330, #5464, .T. ) ;
#32281=DIRECTION ( 'NONE',  ( 0.000000000000000000, 0.000000000000000000, 1.000000000000000000 ) ) ;
#32282=CARTESIAN_POINT ( 'NONE',  ( 0.000000000000000000, 1.699438267350371179, 9.241976615262162298 ) ) ;
#32283=VERTEX_POINT ( 'NONE', #7026 ) ;
#32291=AXIS2_PLACEMENT_3D ( 'NONE', #9276, #24643, #24470 ) ;
#32295=FACE_OUTER_BOUND ( 'NONE', #30740, .T. ) ;
#32296=EDGE_LOOP ( 'NONE', ( #10608, #22504, #19754, #3526, #25668 ) ) ;
#32298=VERTEX_POINT ( 'NONE', #14213 ) ;
#32299=CARTESIAN_POINT ( 'NONE',  ( 2.440333863881506637, 7.210444323284797008, 7.872241054360181955 ) ) ;
#32308=DIRECTION ( 'NONE',  ( 0.000000000000000000, 0.000000000000000000, -1.000000000000000000 ) ) ;
#32317=CYLINDRICAL_SURFACE ( 'NONE', #19824, 8.749000000000002331 ) ;
#32319=EDGE_CURVE ( 'NONE', #14922, #12410, #30789, .T. ) ;
#32321=DIRECTION ( 'NONE',  ( 0.000000000000000000, 0.000000000000000000, 1.000000000000000000 ) ) ;
#32326=VERTEX_POINT ( 'NONE', #12550 ) ;
#32333=PLANE ( 'NONE',  #26264 ) ;
#32340=EDGE_CURVE ( 'NONE', #6932, #12461, #2685, .T. ) ;
#32342=CARTESIAN_POINT ( 'NONE',  ( 0.3076690219754980582, -6.806638167515089322, 7.713510465969206642 ) ) ;
#32345=B_SPLINE_CURVE_WITH_KNOTS ( 'NONE', 3,
 ( #1490, #11666, #24710, #1839, #12019, #22213, #32578, #32422 ),
 .UNSPECIFIED., .F., .F.,
 ( 4, 2, 2, 4 ),
 ( 2.304311362529371911E-07, 0.001261163669367343495, 0.001891630288482890618, 0.002522096907598437958 ),
 .UNSPECIFIED. ) ;
#32354=EDGE_LOOP ( 'NONE', ( #15741, #29826, #485, #32093 ) ) ;
#32355=PLANE ( 'NONE',  #16654 ) ;
#32362=ORIENTED_EDGE ( 'NONE', *, *, #29972, .F. ) ;
#32372=EDGE_CURVE ( 'NONE', #29650, #2323, #15185, .T. ) ;
#32380=CARTESIAN_POINT ( 'NONE',  ( 0.3076688774120017178, -2.239519426673731939, -10.04057401065164612 ) ) ;
#32384=DIRECTION ( 'NONE',  ( -1.000000000000000000, 0.000000000000000000, 0.000000000000000000 ) ) ;
#32389=ORIENTED_EDGE ( 'NONE', *, *, #6089, .F. ) ;
#32390=CARTESIAN_POINT ( 'NONE',  ( 2.425585535373192325, 9.314797388894900720, 5.239665997526921970 ) ) ;
#32400=EDGE_CURVE ( 'NONE', #660, #5275, #16133, .T. ) ;
#32403=DIRECTION ( 'NONE',  ( 1.000000000000000000, -0.000000000000000000, -0.000000000000000000 ) ) ;
#32422=CARTESIAN_POINT ( 'NONE',  ( 2.274274201625327230, 9.680994141368847394, -5.222868219166750592 ) ) ;
#32430=EDGE_CURVE ( 'NONE', #7224, #13047, #8666, .T. ) ;
#32434=EDGE_LOOP ( 'NONE', ( #21640, #20109, #17043, #28704 ) ) ;
#32439=B_SPLINE_CURVE_WITH_KNOTS ( 'NONE', 3,
 ( #7959, #23495, #21173, #30889, #20686, #10971, #16135, #23001 ),
 .UNSPECIFIED., .F., .F.,
 ( 4, 2, 2, 4 ),
 ( 5.099451029784175022E-07, 0.001229189612685845740, 0.001843529446477279411, 0.002457869280268713298 ),
 .UNSPECIFIED. ) ;
#32454=CARTESIAN_POINT ( 'NONE',  ( 0.000000000000000000, 6.478011392632983423, -6.807171995660517005 ) ) ;
#32473=ORIENTED_EDGE ( 'NONE', *, *, #33060, .T. ) ;
#32485=ADVANCED_FACE ( 'NONE', ( #11027 ), #28423, .T. ) ;
#32488=CARTESIAN_POINT ( 'NONE',  ( 2.274274201625327230, -1.464956435139465496, -10.90201369670500142 ) ) ;
#32491=DIRECTION ( 'NONE',  ( -1.000000000000000000, 0.000000000000000000, 0.000000000000000000 ) ) ;
#32495=ORIENTED_EDGE ( 'NONE', *, *, #29109, .F. ) ;
#32511=ORIENTED_EDGE ( 'NONE', *, *, #11185, .F. ) ;
#32538=VERTEX_POINT ( 'NONE', #5831 ) ;
#32540=EDGE_CURVE ( 'NONE', #31286, #29792, #1617, .T. ) ;
#32542=CARTESIAN_POINT ( 'NONE',  ( 3.063284526839887167, 7.360373001730918574, 4.729683950898899703 ) ) ;
#32545=CARTESIAN_POINT ( 'NONE',  ( 4.183205650141505458E-16, -1.999317321091424793, -10.76487093102067050 ) ) ;
#32553=CYLINDRICAL_SURFACE ( 'NONE', #29939, 11.00000000000000000 ) ;
#32557=B_SPLINE_CURVE_WITH_KNOTS ( 'NONE', 3,
 ( #22479, #17802, #5106, #14626, #9589, #9433, #14934, #12759 ),
 .UNSPECIFIED., .F., .F.,
 ( 4, 2, 2, 4 ),
 ( 2.737843117574031781E-07, 0.001228034957219863513, 0.001841915543673915958, 0.002455796130127969705 ),
 .UNSPECIFIED. ) ;
#32561=DIRECTION ( 'NONE',  ( 0.000000000000000000, 0.000000000000000000, -1.000000000000000000 ) ) ;
#32570=VECTOR ( 'NONE', #12665, 1000.000000000000000 ) ;
#32571=ORIENTED_EDGE ( 'NONE', *, *, #10196, .T. ) ;
#32573=CARTESIAN_POINT ( 'NONE',  ( 0.000000000000000000, 9.680994141368771011, 5.222868219166891812 ) ) ;
#32578=CARTESIAN_POINT ( 'NONE',  ( 2.357330042320761265, 9.485534025193874896, -5.240837896778860916 ) ) ;
#32603=CARTESIAN_POINT ( 'NONE',  ( 2.589202797589354788, -10.26630467377260558, -1.003524335601144291 ) ) ;
#32610=AXIS2_PLACEMENT_3D ( 'NONE', #29866, #22993, #20334 ) ;
#32613=CARTESIAN_POINT ( 'NONE',  ( 3.020080181664722030, -3.262125172866642053, -8.342499971020046701 ) ) ;
#32615=EDGE_CURVE ( 'NONE', #4162, #30798, #14684, .T. ) ;
#32619=CARTESIAN_POINT ( 'NONE',  ( 0.7632845268451400322, 6.772677083973724699, 5.538577986791671570 ) ) ;
#32626=DIRECTION ( 'NONE',  ( -1.000000000000000000, 0.000000000000000000, 0.000000000000000000 ) ) ;
#32627=ORIENTED_EDGE ( 'NONE', *, *, #15001, .T. ) ;
#32629=CARTESIAN_POINT ( 'NONE',  ( 2.795120610037678865, -9.728666380661900703, 0.7443816538093672719 ) ) ;
#32638=DIRECTION ( 'NONE',  ( -1.000000000000000000, 0.000000000000000000, -0.000000000000000000 ) ) ;
#32652=DIRECTION ( 'NONE',  ( -1.000000000000000000, 0.000000000000000000, 0.000000000000000000 ) ) ;
#32664=AXIS2_PLACEMENT_3D ( 'NONE', #1397, #11082, #21281 ) ;
#32668=ORIENTED_EDGE ( 'NONE', *, *, #8233, .F. ) ;
#32674=CIRCLE ( 'NONE', #13944, 8.749000000000002331 ) ;
#32683=CARTESIAN_POINT ( 'NONE',  ( 0.3749742847179772798, 9.289351359934663321, -3.955024136977240978 ) ) ;
#32694=DIRECTION ( 'NONE',  ( 0.000000000000000000, 0.000000000000000000, 1.000000000000000000 ) ) ;
#32698=CARTESIAN_POINT ( 'NONE',  ( 0.7632845268398871230, -6.772677083992345359, -5.538577986808975062 ) ) ;
#32701=DIRECTION ( 'NONE',  ( 1.000000000000000000, -0.000000000000000000, -0.000000000000000000 ) ) ;
#32706=ORIENTED_EDGE ( 'NONE', *, *, #22169, .F. ) ;
#32709=CIRCLE ( 'NONE', #1725, 10.99999999999999822 ) ;
#32716=CIRCLE ( 'NONE', #22562, 10.99999999999999822 ) ;
#32726=AXIS2_PLACEMENT_3D ( 'NONE', #18556, #31124, #13534 ) ;
#32727=ADVANCED_FACE ( 'NONE', ( #17867 ), #10335, .T. ) ;
#32738=ORIENTED_EDGE ( 'NONE', *, *, #26233, .T. ) ;
#32746=EDGE_CURVE ( 'NONE', #17929, #5917, #16783, .T. ) ;
#32762=VERTEX_POINT ( 'NONE', #9992 ) ;
#32772=CARTESIAN_POINT ( 'NONE',  ( 0.6728001243864745184, 7.719803900020854925, -4.913284922774296071 ) ) ;
#32777=DIRECTION ( 'NONE',  ( 0.000000000000000000, 0.000000000000000000, 1.000000000000000000 ) ) ;
#32789=VERTEX_POINT ( 'NONE', #2333 ) ;
#32795=CARTESIAN_POINT ( 'NONE',  ( 3.249999999999999556, 0.000000000000000000, 0.000000000000000000 ) ) ;
#32798=DIRECTION ( 'NONE',  ( -1.000000000000000000, -0.000000000000000000, 0.000000000000000000 ) ) ;
#32809=FACE_OUTER_BOUND ( 'NONE', #18306, .T. ) ;
#32813=ORIENTED_EDGE ( 'NONE', *, *, #23857, .T. ) ;
#32814=PLANE ( 'NONE',  #30614 ) ;
#32820=CARTESIAN_POINT ( 'NONE',  ( 0.3076689308780826138, 5.232617538234601184, 8.857103639574667397 ) ) ;
#32829=EDGE_LOOP ( 'NONE', ( #8035, #30180, #11224, #24885, #30336 ) ) ;
#32830=DIRECTION ( 'NONE',  ( 0.000000000000000000, 0.000000000000000000, 1.000000000000000000 ) ) ;
#32831=EDGE_CURVE ( 'NONE', #7759, #3542, #3884, .T. ) ;
#32838=VERTEX_POINT ( 'NONE', #12664 ) ;
#32844=DIRECTION ( 'NONE',  ( -1.000000000000000000, 0.000000000000000000, 0.000000000000000000 ) ) ;
#32850=CARTESIAN_POINT ( 'NONE',  ( -3.687551352559800218E-13, 10.76487093102146098, 1.999317321091203192 ) ) ;
#32852=CARTESIAN_POINT ( 'NONE',  ( 0.7632845268398876781, -3.174628368996014860, -8.152713396088786979 ) ) ;
#32857=DIRECTION ( 'NONE',  ( 0.000000000000000000, 0.000000000000000000, 1.000000000000000000 ) ) ;
#32862=ORIENTED_EDGE ( 'NONE', *, *, #5851, .T. ) ;
#32881=DIRECTION ( 'NONE',  ( -1.000000000000000000, 0.000000000000000000, -0.000000000000000000 ) ) ;
#32889=EDGE_CURVE ( 'NONE', #18983, #24335, #12413, .T. ) ;
#32897=VERTEX_POINT ( 'NONE', #5496 ) ;
#32922=ORIENTED_EDGE ( 'NONE', *, *, #13896, .F. ) ;
#32931=CARTESIAN_POINT ( 'NONE',  ( 0.7632845268398871230, -8.461683424509292450, -2.223716399045660985 ) ) ;
#32933=ORIENTED_EDGE ( 'NONE', *, *, #6928, .F. ) ;
#32960=CARTESIAN_POINT ( 'NONE',  ( 0.5982512417152469064, -7.989521869415790789, 5.029253150608139933 ) ) ;
#32962=DIRECTION ( 'NONE',  ( 0.000000000000000000, 0.000000000000000000, 1.000000000000000000 ) ) ;
#32968=ADVANCED_FACE ( 'NONE', ( #8950 ), #11482, .T. ) ;
#32970=VERTEX_POINT ( 'NONE', #3972 ) ;
#32971=ORIENTED_EDGE ( 'NONE', *, *, #7500, .F. ) ;
#32983=ORIENTED_EDGE ( 'NONE', *, *, #8777, .F. ) ;
#33002=ORIENTED_EDGE ( 'NONE', *, *, #811, .F. ) ;
#33034=ORIENTED_EDGE ( 'NONE', *, *, #17788, .F. ) ;
#33035=DIRECTION ( 'NONE',  ( 1.000000000000000000, -0.000000000000000000, -0.000000000000000000 ) ) ;
#33036=DIRECTION ( 'NONE',  ( 1.000000000000000000, -0.000000000000000000, 0.000000000000000000 ) ) ;
#33037=ORIENTED_EDGE ( 'NONE', *, *, #4219, .F. ) ;
#33060=EDGE_CURVE ( 'NONE', #25199, #17653, #22597, .T. ) ;
#33073=ORIENTED_EDGE ( 'NONE', *, *, #12415, .F. ) ;
#33077=EDGE_CURVE ( 'NONE', #25919, #16275, #21115, .T. ) ;
#33083=CARTESIAN_POINT ( 'NONE',  ( 3.020080146450412784, 0.5244911560323111122, 8.942241244976923298 ) ) ;
#33087=AXIS2_PLACEMENT_3D ( 'NONE', #14640, #14449, #12469 ) ;
#33127=COLOUR_RGB('Slate Gray', 0.72549020, 0.75294118, 0.79215686);
#33128=FILL_AREA_STYLE_COLOUR('',#33127);
#33129=FILL_AREA_STYLE('',(#33128));
#33130=SURFACE_STYLE_FILL_AREA(#33129);
#33131=SURFACE_SIDE_STYLE('',(#33130));
#33132=SURFACE_STYLE_USAGE(.BOTH.,#33131);
#33133=PRESENTATION_STYLE_ASSIGNMENT((#33132));
#33158=STYLED_ITEM('',(#33133),#10563);
#33159=MECHANICAL_DESIGN_GEOMETRIC_PRESENTATION_REPRESENTATION('',(#33158),#7630);
ENDSEC;
END-ISO-10303-21;
